ISO-10303-21;
HEADER;
FILE_DESCRIPTION (('STEP AP214'),
    '1' );
FILE_NAME ('pinion 3.step',
    '2026-10-27T17:59:55',
    ( '' ),
    ( '' ),
    'SwSTEP 2.0',
    'SolidWorks 2025',
    '' );
FILE_SCHEMA (( 'AUTOMOTIVE_DESIGN' ));
ENDSEC;

DATA;
#3=CARTESIAN_POINT ( 'NONE',  ( -25.21435515916043713, -23.92354251275954979, -25.00736669481013053 ) ) ;
#8=LINE ( 'NONE', #19590, #21176 ) ;
#9=CARTESIAN_POINT ( 'NONE',  ( -7.711401346138400115, 25.75361633141491424, -45.70592430511727144 ) ) ;
#11=CARTESIAN_POINT ( 'NONE',  ( -1.464342487929861214, -35.90631960086394514, 29.09292098541700611 ) ) ;
#21=CONICAL_SURFACE ( 'NONE', #3715, 34.60786435723138510, 0.8559913436420825139 ) ;
#23=VECTOR ( 'NONE', #27500, 1000.000000000000000 ) ;
#25=VECTOR ( 'NONE', #23229, 1000.000000000000000 ) ;
#29=( BOUNDED_SURFACE ( )  B_SPLINE_SURFACE ( 3, 1, ( 
 ( #18833, #10616 ),
 ( #3858, #14509 ),
 ( #27599, #23743 ),
 ( #7922, #12623 ) ),
 .UNSPECIFIED., .F., .F., .F. ) 
 B_SPLINE_SURFACE_WITH_KNOTS ( ( 4, 4 ),
 ( 2, 2 ),
 ( 0.000000000000000000, 1.000000000000000000 ),
 ( 0.000000000000000000, 1.000000000000000000 ),
 .UNSPECIFIED. ) 
 GEOMETRIC_REPRESENTATION_ITEM ( )  RATIONAL_B_SPLINE_SURFACE ( (
 ( 1.000000000000000000, 1.000000000000000000),
 ( 0.9934239774497837239, 0.8357310067453919133),
 ( 0.9934239774497837239, 0.8357310067453919133),
 ( 1.000000000000000000, 1.000000000000000000) ) ) 
 REPRESENTATION_ITEM ( '' )  SURFACE ( )  );
#35=B_SPLINE_CURVE_WITH_KNOTS ( 'NONE', 3,
 ( #6398, #19625, #8695, #17458, #4374, #21935, #7700, #20914, #16456, #5081 ),
 .UNSPECIFIED., .F., .F.,
 ( 4, 2, 2, 2, 4 ),
 ( 0.000000000000000000, 0.0003346267210630939765, 0.0006692534421261879529, 0.001003880163189281929, 0.001338506884252375906 ),
 .UNSPECIFIED. ) ;
#36=CARTESIAN_POINT ( 'NONE',  ( -1.058197053496162887, -25.48582931365496762, -38.06270006878843759 ) ) ;
#40=AXIS2_PLACEMENT_3D ( 'NONE', #19702, #25783, #12945 ) ;
#41=CARTESIAN_POINT ( 'NONE',  ( -22.34422965417124374, 26.20925041532892763, 27.39717383755251490 ) ) ;
#44=CARTESIAN_POINT ( 'NONE',  ( -8.259864102781671491, -47.98931516265581365, 22.52209142944983711 ) ) ;
#62=EDGE_LOOP ( 'NONE', ( #22452, #15366, #26764, #26750 ) ) ;
#64=ADVANCED_FACE ( 'NONE', ( #16053 ), #6020, .F. ) ;
#69=ORIENTED_EDGE ( 'NONE', *, *, #25818, .T. ) ;
#76=ORIENTED_EDGE ( 'NONE', *, *, #10432, .T. ) ;
#84=FACE_OUTER_BOUND ( 'NONE', #26105, .T. ) ;
#93=CARTESIAN_POINT ( 'NONE',  ( -25.21435515916043713, -34.05351380035337883, -6.169479169075319014 ) ) ;
#97=EDGE_LOOP ( 'NONE', ( #15926, #16768, #23788, #24002 ) ) ;
#99=EDGE_CURVE ( 'NONE', #10555, #9765, #28256, .T. ) ;
#107=CARTESIAN_POINT ( 'NONE',  ( -55.24390624410018802, -0.007245494385991085341, 0.007503127514277716827 ) ) ;
#113=CARTESIAN_POINT ( 'NONE',  ( -25.21435515916043357, 16.39063784838743132, -30.48034229288645136 ) ) ;
#120=ORIENTED_EDGE ( 'NONE', *, *, #24125, .T. ) ;
#124=CARTESIAN_POINT ( 'NONE',  ( -28.13707043255157103, -6.342158660426852279, 22.00298671236746273 ) ) ;
#134=LINE ( 'NONE', #9062, #397 ) ;
#136=CARTESIAN_POINT ( 'NONE',  ( -8.259864102781710571, 46.42816643551610412, 25.58601832199028436 ) ) ;
#140=EDGE_CURVE ( 'NONE', #22201, #4550, #16497, .T. ) ;
#145=ORIENTED_EDGE ( 'NONE', *, *, #25140, .T. ) ;
#150=EDGE_LOOP ( 'NONE', ( #7208, #20367, #2015, #26988 ) ) ;
#160=CARTESIAN_POINT ( 'NONE',  ( -1.583189561560256253, -2.490696082060189109, -46.33203782964460515 ) ) ;
#167=DIRECTION ( 'NONE',  ( 0.7563875759206388771, -0.1685564395263385584, -0.6320336713238493553 ) ) ;
#168=CARTESIAN_POINT ( 'NONE',  ( -20.24419206586953379, -24.70913649113841970, -16.36655224501358319 ) ) ;
#170=CARTESIAN_POINT ( 'NONE',  ( -22.23226125620943705, 29.33577758406451252, -11.82389163795220455 ) ) ;
#186=CARTESIAN_POINT ( 'NONE',  ( -20.90916690077964191, 34.84883504600978910, 18.74041620980130674 ) ) ;
#191=CARTESIAN_POINT ( 'NONE',  ( -55.25297051322618813, -0.01483298743815008106, -0.001818774723749387676 ) ) ;
#194=VERTEX_POINT ( 'NONE', #11141 ) ;
#197=CARTESIAN_POINT ( 'NONE',  ( -55.24728320129491266, 0.005114031043466756021, 0.01362040845703047127 ) ) ;
#199=CARTESIAN_POINT ( 'NONE',  ( -1.323830074806772839, 38.58891736138533446, -25.17121255494489418 ) ) ;
#210=CARTESIAN_POINT ( 'NONE',  ( -55.24198130335446422, -0.004276389980779660843, 0.008252882783648829434 ) ) ;
#214=CARTESIAN_POINT ( 'NONE',  ( -19.53423201713129842, 3.678323623448370869E-15, -28.92774122539760384 ) ) ;
#220=CARTESIAN_POINT ( 'NONE',  ( -21.41427618760446450, 1.815001260755841450, -30.75468365310879193 ) ) ;
#221=CARTESIAN_POINT ( 'NONE',  ( -1.031422197589711764, 45.78027046666443312, 1.530725436377622817 ) ) ;
#224=CARTESIAN_POINT ( 'NONE',  ( -22.23342874802669655, -24.24669006619387090, -20.31166691703116811 ) ) ;
#225=CARTESIAN_POINT ( 'NONE',  ( -55.24390624410018802, 0.009374879212967415429, 0.004572280736702902422 ) ) ;
#230=CARTESIAN_POINT ( 'NONE',  ( -2.904412668506678674, -47.56768199507435213, -2.864640348250463653 ) ) ;
#231=CARTESIAN_POINT ( 'NONE',  ( -20.20700224038492721, -27.82980252387812570, 10.08426345511618649 ) ) ;
#239=CARTESIAN_POINT ( 'NONE',  ( -55.25297051322618813, -0.01466904165775489814, 0.002853887643043841529 ) ) ;
#244=CARTESIAN_POINT ( 'NONE',  ( -7.078251931573406708, -11.16394717458641850, 50.86685171665422445 ) ) ;
#253=EDGE_CURVE ( 'NONE', #19163, #21576, #4177, .T. ) ;
#254=ORIENTED_EDGE ( 'NONE', *, *, #9034, .T. ) ;
#258=CARTESIAN_POINT ( 'NONE',  ( -20.21097721650786738, 29.61001326827675939, -0.3305964462498667822 ) ) ;
#261=EDGE_CURVE ( 'NONE', #22201, #20516, #2798, .T. ) ;
#266=CARTESIAN_POINT ( 'NONE',  ( -1.539763995773682614, -38.84665165401045073, 25.17088606276588791 ) ) ;
#267=CARTESIAN_POINT ( 'NONE',  ( -1.048171036023513247, 1.020520027229132598, -45.78635789057864969 ) ) ;
#270=ORIENTED_EDGE ( 'NONE', *, *, #4191, .F. ) ;
#271=CARTESIAN_POINT ( 'NONE',  ( -55.24198130335446422, 0.008252882783649323831, 0.004276389980779915848 ) ) ;
#283=CARTESIAN_POINT ( 'NONE',  ( -20.57838717382308147, -18.89542499756482741, 23.26537097894125594 ) ) ;
#284=CARTESIAN_POINT ( 'NONE',  ( -1.019300379054419947, -35.83762006677421397, -28.53917295602885318 ) ) ;
#287=EDGE_CURVE ( 'NONE', #27787, #26061, #35, .T. ) ;
#288=CARTESIAN_POINT ( 'NONE',  ( -1.048171036023500147, -1.020520027228813298, 45.78635789057867100 ) ) ;
#297=CARTESIAN_POINT ( 'NONE',  ( -1.113427685306983550, -12.28784199929904730, 44.18561238466750041 ) ) ;
#298=CARTESIAN_POINT ( 'NONE',  ( -20.20700224038492721, -28.44216453106542986, -8.199606986804219844 ) ) ;
#306=ORIENTED_EDGE ( 'NONE', *, *, #5781, .T. ) ;
#312=CARTESIAN_POINT ( 'NONE',  ( -1.046935749540015115, 37.78548154587994645, -25.87617179820928826 ) ) ;
#316=CARTESIAN_POINT ( 'NONE',  ( -20.38016308990357928, -18.69911008768351479, -23.16952666206578826 ) ) ;
#325=CARTESIAN_POINT ( 'NONE',  ( -1.619063947482201282, 43.26576862488434472, -16.67502769180576649 ) ) ;
#331=CARTESIAN_POINT ( 'NONE',  ( -4.473127245936431073, 37.94261489385763753, 31.51789735524151226 ) ) ;
#357=B_SPLINE_CURVE_WITH_KNOTS ( 'NONE', 3,
 ( #19510, #22251, #9143, #17897, #28277, #17341, #26130 ),
 .UNSPECIFIED., .F., .F.,
 ( 4, 3, 4 ),
 ( 0.000000000000000000, 0.006568092053401790135, 0.02506242213020846640 ),
 .UNSPECIFIED. ) ;
#358=CARTESIAN_POINT ( 'NONE',  ( -25.21435515916043002, 23.92354251275938992, -25.00736669481030106 ) ) ;
#363=CARTESIAN_POINT ( 'NONE',  ( -6.574463467970653063, 20.55340846381200848, 47.03022655117382556 ) ) ;
#366=ORIENTED_EDGE ( 'NONE', *, *, #21501, .T. ) ;
#374=VECTOR ( 'NONE', #5725, 1000.000000000000000 ) ;
#375=EDGE_CURVE ( 'NONE', #9976, #3267, #7611, .T. ) ;
#377=CARTESIAN_POINT ( 'NONE',  ( -1.113548883309548376, 45.82026503946953255, 1.968251867499028585 ) ) ;
#380=ADVANCED_FACE ( 'NONE', ( #10939 ), #22761, .F. ) ;
#383=CARTESIAN_POINT ( 'NONE',  ( -1.239374126674604337, -16.50008610789329921, -42.99367564261275021 ) ) ;
#384=VERTEX_POINT ( 'NONE', #15379 ) ;
#386=CARTESIAN_POINT ( 'NONE',  ( -28.41354790283022069, 23.16239616762931064, -1.249099604787157425 ) ) ;
#388=CARTESIAN_POINT ( 'NONE',  ( -10.86508079875782329, -46.07061504567103327, -22.20099862734805996 ) ) ;
#389=CARTESIAN_POINT ( 'NONE',  ( -1.463510566862830986, 16.57250862017420090, -43.13857742234511505 ) ) ;
#392=B_SPLINE_CURVE_WITH_KNOTS ( 'NONE', 3,
 ( #24535, #6970, #24240, #26380, #19904, #11274, #17740, #26517, #26809, #22059 ),
 .UNSPECIFIED., .F., .F.,
 ( 4, 2, 2, 2, 4 ),
 ( 4.336808689942017255E-19, 0.0003346267210630946812, 0.0006692534421261889287, 0.001003880163189283230, 0.001338506884252377424 ),
 .UNSPECIFIED. ) ;
#394=B_SPLINE_CURVE_WITH_KNOTS ( 'NONE', 3,
 ( #14459, #12169, #11525, #17848, #8956, #17713, #6658, #15405 ),
 .UNSPECIFIED., .F., .F.,
 ( 4, 2, 2, 4 ),
 ( 2.214340075454938295E-16, 0.002761568181852865067, 0.005523136363705506355, 0.01104627272741079066 ),
 .UNSPECIFIED. ) ;
#396=CARTESIAN_POINT ( 'NONE',  ( -55.24300891470648622, 0.006048736206180948920, -0.007734635432132875611 ) ) ;
#397=VECTOR ( 'NONE', #413, 1000.000000000000114 ) ;
#405=CARTESIAN_POINT ( 'NONE',  ( -1.050230347699842692, 5.964912479342754695E-15, -45.79907861674080749 ) ) ;
#409=CARTESIAN_POINT ( 'NONE',  ( -20.21097721712959228, -29.61001327235739566, -0.3305963429841727863 ) ) ;
#413=DIRECTION ( 'NONE',  ( 0.7637818620346800147, -0.6068965246771045319, -0.2198041754873859832 ) ) ;
#415=CARTESIAN_POINT ( 'NONE',  ( -1.619063947482197729, 38.92136151114943488, 25.20140673341330739 ) ) ;
#416=( BOUNDED_SURFACE ( )  B_SPLINE_SURFACE ( 3, 1, ( 
 ( #23177, #18546 ),
 ( #1262, #20412 ),
 ( #15948, #22887 ),
 ( #3145, #12211 ) ),
 .UNSPECIFIED., .F., .F., .F. ) 
 B_SPLINE_SURFACE_WITH_KNOTS ( ( 4, 4 ),
 ( 2, 2 ),
 ( 0.000000000000000000, 1.000000000000000000 ),
 ( 0.000000000000000000, 1.000000000000000000 ),
 .UNSPECIFIED. ) 
 GEOMETRIC_REPRESENTATION_ITEM ( )  RATIONAL_B_SPLINE_SURFACE ( (
 ( 1.000000000000000000, 1.000000000000000000),
 ( 0.9593753223639863714, 0.9995975284513187731),
 ( 0.9593753223639863714, 0.9995975284513187731),
 ( 1.000000000000000000, 1.000000000000000000) ) ) 
 REPRESENTATION_ITEM ( '' )  SURFACE ( )  );
#433=FACE_OUTER_BOUND ( 'NONE', #2313, .T. ) ;
#445=CARTESIAN_POINT ( 'NONE',  ( -20.57838717382308147, 16.28767523336157552, 25.16001208503087838 ) ) ;
#451=ORIENTED_EDGE ( 'NONE', *, *, #25516, .F. ) ;
#456=EDGE_LOOP ( 'NONE', ( #7870, #6919, #10973, #27044 ) ) ;
#460=EDGE_CURVE ( 'NONE', #21703, #19144, #134, .T. ) ;
#464=B_SPLINE_CURVE_WITH_KNOTS ( 'NONE', 3,
 ( #6253, #23690, #8010, #3941 ),
 .UNSPECIFIED., .F., .F.,
 ( 4, 4 ),
 ( 0.0009910334943225120648, 0.001982023823822943315 ),
 .UNSPECIFIED. ) ;
#465=CARTESIAN_POINT ( 'NONE',  ( -20.57838717382308502, 28.96176188950218844, -7.715628353033780584 ) ) ;
#472=ORIENTED_EDGE ( 'NONE', *, *, #26439, .F. ) ;
#479=CARTESIAN_POINT ( 'NONE',  ( -22.23342874802668234, -26.81018246605525590, 16.78332232459670337 ) ) ;
#481=CARTESIAN_POINT ( 'NONE',  ( -20.20700224038492721, -10.08426345511609235, -27.82980252387815767 ) ) ;
#499=DIRECTION ( 'NONE',  ( -0.7563875759206388771, -0.5490129373055306905, -0.3556158456312839555 ) ) ;
#502=CARTESIAN_POINT ( 'NONE',  ( -55.24390624410018802, -0.001811362924359030029, -0.01027195578987783083 ) ) ;
#503=CARTESIAN_POINT ( 'NONE',  ( -20.47566338032521216, -16.24827550219808003, 25.06314818626711372 ) ) ;
#509=DIRECTION ( 'NONE',  ( 0.7563875759206388771, 0.03500244528122559151, -0.6531865459554678788 ) ) ;
#514=ORIENTED_EDGE ( 'NONE', *, *, #11989, .T. ) ;
#515=CARTESIAN_POINT ( 'NONE',  ( -23.77929240705204705, 26.20227034809557054, -25.06639637888430272 ) ) ;
#524=CARTESIAN_POINT ( 'NONE',  ( -1.058473599757830286, -15.81436910992550438, -42.99101666105224240 ) ) ;
#529=ORIENTED_EDGE ( 'NONE', *, *, #3330, .T. ) ;
#533=B_SPLINE_CURVE_WITH_KNOTS ( 'NONE', 3,
 ( #405, #17949, #26593, #834, #2856, #9186, #26735, #267, #4869, #25041 ),
 .UNSPECIFIED., .F., .F.,
 ( 4, 3, 3, 4 ),
 ( 0.001530725384384652287, 0.001531419946797919589, 0.002296279302920155134, 0.003061450627205758099 ),
 .UNSPECIFIED. ) ;
#536=CARTESIAN_POINT ( 'NONE',  ( -25.21435515916043713, -34.05351380035337883, -6.169479169075319014 ) ) ;
#541=CARTESIAN_POINT ( 'NONE',  ( -55.24271866751342941, -0.001425019990781919424, 0.009388511352197656881 ) ) ;
#549=CARTESIAN_POINT ( 'NONE',  ( -25.21435515916043002, 23.92354251275938992, -25.00736669481030106 ) ) ;
#551=CARTESIAN_POINT ( 'NONE',  ( -55.24271866751342941, -0.009388511352199774979, 0.001425019990778933097 ) ) ;
#565=VERTEX_POINT ( 'NONE', #13653 ) ;
#572=CARTESIAN_POINT ( 'NONE',  ( -55.25719721206881729, -0.01115102788683311301, 0.0006290797159230496292 ) ) ;
#583=CARTESIAN_POINT ( 'NONE',  ( -1.019300379054419947, -45.76814864815092676, -2.023851374322514829 ) ) ;
#600=VERTEX_POINT ( 'NONE', #5452 ) ;
#602=CARTESIAN_POINT ( 'NONE',  ( -1.048994561756802169, 45.79144455904140898, 0.7655149579825029083 ) ) ;
#607=VERTEX_POINT ( 'NONE', #25482 ) ;
#609=LINE ( 'NONE', #20463, #14259 ) ;
#625=( BOUNDED_SURFACE ( )  B_SPLINE_SURFACE ( 3, 1, ( 
 ( #16688, #27896 ),
 ( #10072, #14794 ),
 ( #25481, #19255 ),
 ( #7780, #16955 ) ),
 .UNSPECIFIED., .F., .F., .F. ) 
 B_SPLINE_SURFACE_WITH_KNOTS ( ( 4, 4 ),
 ( 2, 2 ),
 ( 0.000000000000000000, 1.000000000000000000 ),
 ( 0.000000000000000000, 1.000000000000000000 ),
 .UNSPECIFIED. ) 
 GEOMETRIC_REPRESENTATION_ITEM ( )  RATIONAL_B_SPLINE_SURFACE ( (
 ( 1.000000000000000000, 1.000000000000000000),
 ( 0.7789835883360578528, 0.9689951854195403280),
 ( 0.7789835883360578528, 0.9689951854195403280),
 ( 1.000000000000000000, 1.000000000000000000) ) ) 
 REPRESENTATION_ITEM ( '' )  SURFACE ( )  );
#632=CARTESIAN_POINT ( 'NONE',  ( -1.058473599757814521, 15.81436910992580991, 42.99101666105212161 ) ) ;
#635=DIRECTION ( 'NONE',  ( 1.000000000000000000, -6.938893903907226837E-18, 1.734723475976806709E-18 ) ) ;
#644=CARTESIAN_POINT ( 'NONE',  ( -15.02187109954784106, 45.60876405941888123, -8.264310930412539946 ) ) ;
#646=CARTESIAN_POINT ( 'NONE',  ( -25.21435515916043002, 4.655591116594353984, -34.29329011225956947 ) ) ;
#647=CARTESIAN_POINT ( 'NONE',  ( -55.24271866751342941, 0.008488649505343330570, 0.004256484107795472684 ) ) ;
#650=CARTESIAN_POINT ( 'NONE',  ( -24.53239521893645048, 22.94500969220232633, -24.99972072650149713 ) ) ;
#651=CARTESIAN_POINT ( 'NONE',  ( -1.048994561756802391, 27.53485040342894408, -36.59609844253136401 ) ) ;
#657=CARTESIAN_POINT ( 'NONE',  ( -2.911734481061403645, 17.36785190846042681, 44.38410240830284437 ) ) ;
#658=ADVANCED_FACE ( 'NONE', ( #5307 ), #7111, .F. ) ;
#659=CARTESIAN_POINT ( 'NONE',  ( -1.619063947482197729, -43.26576862488445130, -16.67502769180545386 ) ) ;
#661=EDGE_LOOP ( 'NONE', ( #13887, #8286, #21471, #8177 ) ) ;
#662=ORIENTED_EDGE ( 'NONE', *, *, #9978, .F. ) ;
#667=ORIENTED_EDGE ( 'NONE', *, *, #20614, .T. ) ;
#673=ORIENTED_EDGE ( 'NONE', *, *, #10366, .F. ) ;
#676=EDGE_CURVE ( 'NONE', #6702, #27834, #5901, .T. ) ;
#687=ORIENTED_EDGE ( 'NONE', *, *, #26528, .T. ) ;
#690=FACE_OUTER_BOUND ( 'NONE', #725, .T. ) ;
#710=VERTEX_POINT ( 'NONE', #21415 ) ;
#711=VERTEX_POINT ( 'NONE', #19533 ) ;
#720=CARTESIAN_POINT ( 'NONE',  ( -1.031422197589711987, 28.14735071801795740, 36.13727897780095333 ) ) ;
#725=EDGE_LOOP ( 'NONE', ( #2704, #27015 ) ) ;
#726=CARTESIAN_POINT ( 'NONE',  ( -1.048994561756802169, -43.31369460697986540, -14.87838255483240246 ) ) ;
#733=VERTEX_POINT ( 'NONE', #24017 ) ;
#739=EDGE_LOOP ( 'NONE', ( #19600, #26923, #1375, #15922 ) ) ;
#742=ORIENTED_EDGE ( 'NONE', *, *, #24451, .T. ) ;
#745=CARTESIAN_POINT ( 'NONE',  ( -1.048171036023497260, 37.64178826568608116, -26.08692787913882327 ) ) ;
#749=CARTESIAN_POINT ( 'NONE',  ( -25.21435515916043357, 16.39063784838743132, -30.48034229288645136 ) ) ;
#750=FACE_OUTER_BOUND ( 'NONE', #3616, .T. ) ;
#753=CARTESIAN_POINT ( 'NONE',  ( -4.780792508754321268, 25.98388465890140964, 42.16805077400930202 ) ) ;
#756=CARTESIAN_POINT ( 'NONE',  ( -23.77929240705207192, -35.68044874544700207, -6.464423883190233866 ) ) ;
#758=DIRECTION ( 'NONE',  ( -0.7563875759206388771, -0.03500244528123461207, -0.6531865459554673237 ) ) ;
#764=CARTESIAN_POINT ( 'NONE',  ( -28.41354790283022069, -8.345538364877233661, -21.64275480268745255 ) ) ;
#768=CARTESIAN_POINT ( 'NONE',  ( -1.045287976400365970, 15.59869763335156101, 43.05558670614217931 ) ) ;
#770=CARTESIAN_POINT ( 'NONE',  ( -55.24390624410018802, 0.004896917417128144288, 0.009209468562451129242 ) ) ;
#789=CARTESIAN_POINT ( 'NONE',  ( -25.21435515916043713, -34.05351380035328646, 6.169479169075816394 ) ) ;
#795=ORIENTED_EDGE ( 'NONE', *, *, #1305, .T. ) ;
#799=CARTESIAN_POINT ( 'NONE',  ( -6.588769196390767746, -51.10255870850473769, -4.956336548259470121 ) ) ;
#801=CARTESIAN_POINT ( 'NONE',  ( -55.25297051322618813, 0.01466904165775178431, 0.002853887643042449414 ) ) ;
#808=CARTESIAN_POINT ( 'NONE',  ( -55.24390624410018802, 0.009209468562451588944, -0.004896917417127890151 ) ) ;
#811=FACE_OUTER_BOUND ( 'NONE', #27029, .T. ) ;
#816=CARTESIAN_POINT ( 'NONE',  ( -55.24390624410018802, -0.004896917417131185259, 0.009209468562452437224 ) ) ;
#834=CARTESIAN_POINT ( 'NONE',  ( -1.050230346682677007, 0.0006945978175690684661, -45.79907861045643358 ) ) ;
#840=CARTESIAN_POINT ( 'NONE',  ( -20.21097721650785672, -29.61001326827676294, 0.3305964462500739498 ) ) ;
#853=EDGE_LOOP ( 'NONE', ( #27414, #15523, #25287, #28098 ) ) ;
#860=DIRECTION ( 'NONE',  ( 1.000000000000000000, -6.938893903907226837E-18, 1.734723475976806709E-18 ) ) ;
#866=DIRECTION ( 'NONE',  ( 0.7637818620346800147, 0.2198041754873883424, -0.6068965246771037547 ) ) ;
#867=CARTESIAN_POINT ( 'NONE',  ( -1.050231094221207417, -36.90262059116448512, 27.12595454131546191 ) ) ;
#874=DIRECTION ( 'NONE',  ( 1.000000000000000000, -6.938893903907226837E-18, 1.734723475976806709E-18 ) ) ;
#880=ADVANCED_FACE ( 'NONE', ( #16493 ), #5242, .F. ) ;
#904=CARTESIAN_POINT ( 'NONE',  ( -21.41430102051751660, -25.94791611261628717, -16.60879216503625244 ) ) ;
#909=EDGE_CURVE ( 'NONE', #3564, #1317, #19633, .T. ) ;
#912=ADVANCED_FACE ( 'NONE', ( #1233 ), #3229, .F. ) ;
#913=ORIENTED_EDGE ( 'NONE', *, *, #10709, .F. ) ;
#914=DIRECTION ( 'NONE',  ( 0.000000000000000000, 5.223019709707975211E-21, -1.000000000000000000 ) ) ;
#916=CARTESIAN_POINT ( 'NONE',  ( -1.045287976400365970, 28.14015102489882736, 36.12803364096558312 ) ) ;
#920=B_SPLINE_CURVE_WITH_KNOTS ( 'NONE', 3,
 ( #12975, #27954, #17427, #28364, #25950, #10834 ),
 .UNSPECIFIED., .F., .F.,
 ( 4, 2, 4 ),
 ( 1.734723475976807094E-18, 0.0004335151646191503279, 0.0008670303292382989212 ),
 .UNSPECIFIED. ) ;
#934=VECTOR ( 'NONE', #15204, 1000.000000000000114 ) ;
#937=EDGE_LOOP ( 'NONE', ( #2335, #18121, #2579, #3275 ) ) ;
#942=CARTESIAN_POINT ( 'NONE',  ( -20.20700224038492721, -24.51628800869035274, 16.58740185276737122 ) ) ;
#944=CARTESIAN_POINT ( 'NONE',  ( -7.078251931573400491, 20.86696228105224549, -47.71415099571811425 ) ) ;
#947=EDGE_CURVE ( 'NONE', #1416, #19279, #2081, .T. ) ;
#958=B_SPLINE_CURVE_WITH_KNOTS ( 'NONE', 3,
 ( #5013, #22156, #9356, #22449, #11489, #22599 ),
 .UNSPECIFIED., .F., .F.,
 ( 4, 2, 4 ),
 ( 1.447636874611986795E-16, 0.003570751334075636125, 0.007141502668151127400 ),
 .UNSPECIFIED. ) ;
#963=CARTESIAN_POINT ( 'NONE',  ( -55.24300891470650754, -0.002702093572892964434, 0.009439835024158798812 ) ) ;
#966=CARTESIAN_POINT ( 'NONE',  ( -1.031422197589711987, 37.93675465142509040, 25.67058493451400381 ) ) ;
#970=ORIENTED_EDGE ( 'NONE', *, *, #27106, .F. ) ;
#974=ORIENTED_EDGE ( 'NONE', *, *, #4787, .T. ) ;
#978=PLANE ( 'NONE',  #18447 ) ;
#983=CONICAL_SURFACE ( 'NONE', #7413, 34.60786435723138510, 0.8559913436420825139 ) ;
#984=CARTESIAN_POINT ( 'NONE',  ( -20.57838717382308147, 7.715628353033680220, -28.96176188950220975 ) ) ;
#996=ORIENTED_EDGE ( 'NONE', *, *, #15714, .T. ) ;
#1000=ORIENTED_EDGE ( 'NONE', *, *, #7940, .T. ) ;
#1009=ORIENTED_EDGE ( 'NONE', *, *, #12133, .F. ) ;
#1011=CARTESIAN_POINT ( 'NONE',  ( -1.239374126674604337, 42.99367564261301311, 16.50008610789253893 ) ) ;
#1021=CARTESIAN_POINT ( 'NONE',  ( -1.619063947482194177, 35.99532424477422410, 29.22875152547716482 ) ) ;
#1024=CARTESIAN_POINT ( 'NONE',  ( -1.050230346682665239, -45.79907861045645490, -0.0006945978174090946524 ) ) ;
#1035=VECTOR ( 'NONE', #20009, 1000.000000000000114 ) ;
#1036=EDGE_LOOP ( 'NONE', ( #12535, #4918, #20028, #24513 ) ) ;
#1043=CARTESIAN_POINT ( 'NONE',  ( -2.265401668238139266, -17.02144111536849636, 43.82493763960401623 ) ) ;
#1045=CONICAL_SURFACE ( 'NONE', #16695, 53.53553390275978785, 0.7853981625000051592 ) ;
#1048=CARTESIAN_POINT ( 'NONE',  ( -8.786685647604894456, 37.00619870957989832, 38.68584556812258768 ) ) ;
#1066=EDGE_LOOP ( 'NONE', ( #5349, #11502, #21928, #16662 ) ) ;
#1070=EDGE_LOOP ( 'NONE', ( #17805, #6885, #23534, #12703 ) ) ;
#1072=ORIENTED_EDGE ( 'NONE', *, *, #22607, .T. ) ;
#1077=CARTESIAN_POINT ( 'NONE',  ( -1.031422197589716205, -28.14735071801717936, 36.13727897780158571 ) ) ;
#1081=CARTESIAN_POINT ( 'NONE',  ( -1.323439229708136100, 25.17120723334093313, -38.58845475799776636 ) ) ;
#1083=CARTESIAN_POINT ( 'NONE',  ( -1.048994561756786625, -13.42228657661154401, -43.78680886990936472 ) ) ;
#1084=CARTESIAN_POINT ( 'NONE',  ( -21.41430102051744910, -7.777552968935554034, 29.81033373822135246 ) ) ;
#1088=CARTESIAN_POINT ( 'NONE',  ( -1.046936909428682005, -25.87632113675133283, 37.78538189376536849 ) ) ;
#1096=CARTESIAN_POINT ( 'NONE',  ( -9.156249394959706578, -53.90509764945135629, -8.027840202793747437 ) ) ;
#1097=CARTESIAN_POINT ( 'NONE',  ( -1.019300379054419947, 28.53917295602898463, -35.83762006677410028 ) ) ;
#1098=ORIENTED_EDGE ( 'NONE', *, *, #9233, .F. ) ;
#1102=( BOUNDED_SURFACE ( )  B_SPLINE_SURFACE ( 3, 1, ( 
 ( #17013, #15264 ),
 ( #24360, #15545 ),
 ( #20022, #26212 ),
 ( #13250, #6515 ) ),
 .UNSPECIFIED., .F., .F., .F. ) 
 B_SPLINE_SURFACE_WITH_KNOTS ( ( 4, 4 ),
 ( 2, 2 ),
 ( 0.000000000000000000, 1.000000000000000000 ),
 ( 0.000000000000000000, 1.000000000000000000 ),
 .UNSPECIFIED. ) 
 GEOMETRIC_REPRESENTATION_ITEM ( )  RATIONAL_B_SPLINE_SURFACE ( (
 ( 1.000000000000000000, 1.000000000000000000),
 ( 0.9934239774497838349, 0.8357310067453913582),
 ( 0.9934239774497838349, 0.8357310067453913582),
 ( 1.000000000000000000, 1.000000000000000000) ) ) 
 REPRESENTATION_ITEM ( '' )  SURFACE ( )  );
#1103=VECTOR ( 'NONE', #24555, 1000.000000000000114 ) ;
#1118=CARTESIAN_POINT ( 'NONE',  ( -1.050230346682671678, -14.15335421912552860, 43.55729751025877761 ) ) ;
#1122=ORIENTED_EDGE ( 'NONE', *, *, #14095, .T. ) ;
#1125=CARTESIAN_POINT ( 'NONE',  ( -55.24390624410018802, 0.009374879212971231821, -0.004572280736701976080 ) ) ;
#1132=FACE_OUTER_BOUND ( 'NONE', #8743, .T. ) ;
#1135=CARTESIAN_POINT ( 'NONE',  ( -20.47566338032530098, -23.19796701701852015, 18.81547714195498244 ) ) ;
#1136=CARTESIAN_POINT ( 'NONE',  ( -20.47566338032515532, 28.85746366088581283, 7.708089572830123082 ) ) ;
#1138=CARTESIAN_POINT ( 'NONE',  ( -1.583189561560252701, -44.83405390829663872, 11.94859433442948493 ) ) ;
#1140=CARTESIAN_POINT ( 'NONE',  ( -55.25719721206881729, 0.009391134844729439810, -0.006045473558784624467 ) ) ;
#1142=FACE_OUTER_BOUND ( 'NONE', #17437, .T. ) ;
#1143=( BOUNDED_SURFACE ( )  B_SPLINE_SURFACE ( 3, 1, ( 
 ( #11515, #18262 ),
 ( #13957, #1011 ),
 ( #3315, #18573 ),
 ( #16412, #23053 ) ),
 .UNSPECIFIED., .F., .F., .F. ) 
 B_SPLINE_SURFACE_WITH_KNOTS ( ( 4, 4 ),
 ( 2, 2 ),
 ( 0.000000000000000000, 1.000000000000000000 ),
 ( 0.000000000000000000, 1.000000000000000000 ),
 .UNSPECIFIED. ) 
 GEOMETRIC_REPRESENTATION_ITEM ( )  RATIONAL_B_SPLINE_SURFACE ( (
 ( 1.000000000000000000, 1.000000000000000000),
 ( 0.9934239774497837239, 0.8357310067453919133),
 ( 0.9934239774497837239, 0.8357310067453919133),
 ( 1.000000000000000000, 1.000000000000000000) ) ) 
 REPRESENTATION_ITEM ( '' )  SURFACE ( )  );
#1149=ORIENTED_EDGE ( 'NONE', *, *, #16963, .T. ) ;
#1162=ORIENTED_EDGE ( 'NONE', *, *, #14150, .T. ) ;
#1164=B_SPLINE_CURVE_WITH_KNOTS ( 'NONE', 3,
 ( #19899, #17735, #36, #20034, #8829, #17865, #4639, #17590, #26371, #26512 ),
 .UNSPECIFIED., .F., .F.,
 ( 4, 2, 2, 2, 4 ),
 ( 2.825996620262520077E-16, 0.0003346187017559037265, 0.0006692374035115249099, 0.001003856105267145931, 0.001338474807022767060 ),
 .UNSPECIFIED. ) ;
#1167=CARTESIAN_POINT ( 'NONE',  ( -1.049817751779873021, 13.66628317065048392, 43.71287583013712208 ) ) ;
#1168=CARTESIAN_POINT ( 'NONE',  ( -2.265401668238144151, 36.42007794497294526, 29.73100299756526965 ) ) ;
#1171=CARTESIAN_POINT ( 'NONE',  ( -1.583189561560256253, 43.29471907393742924, -16.68617981233717273 ) ) ;
#1172=DIRECTION ( 'NONE',  ( 1.000000000000000000, -6.938893903907226837E-18, 1.734723475976806709E-18 ) ) ;
#1182=ORIENTED_EDGE ( 'NONE', *, *, #12882, .F. ) ;
#1183=EDGE_CURVE ( 'NONE', #15497, #4557, #4435, .T. ) ;
#1185=DIRECTION ( 'NONE',  ( 0.000000000000000000, 5.223019709707975211E-21, -1.000000000000000000 ) ) ;
#1188=CARTESIAN_POINT ( 'NONE',  ( -1.619063947482197729, -2.489035965909835557, 46.30105812165550816 ) ) ;
#1189=EDGE_CURVE ( 'NONE', #25057, #6702, #19268, .T. ) ;
#1190=CARTESIAN_POINT ( 'NONE',  ( -2.904412668506668016, 25.64203923793632356, 40.16685646686180178 ) ) ;
#1197=CARTESIAN_POINT ( 'NONE',  ( -20.57838717382308147, -1.611677988432151709, 29.92853265176832878 ) ) ;
#1201=CARTESIAN_POINT ( 'NONE',  ( -1.539760825549689294, 16.63252404870416257, 43.19716078875421772 ) ) ;
#1205=CARTESIAN_POINT ( 'NONE',  ( -25.21435515916025594, 1.749597353048488237E-16, -4.373993382621220594E-17 ) ) ;
#1207=ORIENTED_EDGE ( 'NONE', *, *, #1389, .F. ) ;
#1212=CARTESIAN_POINT ( 'NONE',  ( -1.031422197589711987, 15.60268798220698727, 43.06660437151290211 ) ) ;
#1218=CARTESIAN_POINT ( 'NONE',  ( -1.045287976400383290, -12.68782741917353185, -44.00138577190637079 ) ) ;
#1220=ORIENTED_EDGE ( 'NONE', *, *, #1493, .F. ) ;
#1227=CARTESIAN_POINT ( 'NONE',  ( -55.25719721206881729, 0.01079965405819524257, -0.002847566758684156023 ) ) ;
#1229=CARTESIAN_POINT ( 'NONE',  ( -2.904412668506659578, -25.64203923793602868, -40.16685646686200073 ) ) ;
#1231=CARTESIAN_POINT ( 'NONE',  ( -1.031422197589716205, 28.14735071801795740, 36.13727897780097464 ) ) ;
#1233=FACE_OUTER_BOUND ( 'NONE', #15110, .T. ) ;
#1244=CARTESIAN_POINT ( 'NONE',  ( -1.583189561560252701, 11.94859433442964658, 44.83405390829658188 ) ) ;
#1246=CARTESIAN_POINT ( 'NONE',  ( -21.41430102051751305, 19.54553566814620069, 23.81424706376344247 ) ) ;
#1254=CARTESIAN_POINT ( 'NONE',  ( -20.20700224038492365, 8.199606986804329978, -28.44216453106539078 ) ) ;
#1255=CARTESIAN_POINT ( 'NONE',  ( -24.53237795827028478, -30.86653739599989521, 14.09663893005617119 ) ) ;
#1259=CARTESIAN_POINT ( 'NONE',  ( -20.47566338032527966, 27.87687989047307013, -10.72601609985035331 ) ) ;
#1262=CARTESIAN_POINT ( 'NONE',  ( -55.24198130335446422, 0.006617369590169233477, 0.006527480770975859110 ) ) ;
#1267=CARTESIAN_POINT ( 'NONE',  ( -20.20700224038492721, 28.44216453106548315, 8.199606986804035103 ) ) ;
#1271=CARTESIAN_POINT ( 'NONE',  ( -2.265401668238157473, 39.53028715828234851, -25.45016726748328040 ) ) ;
#1274=CARTESIAN_POINT ( 'NONE',  ( -8.786685647604894456, -23.24040270374358030, 48.22796981442792230 ) ) ;
#1277=CARTESIAN_POINT ( 'NONE',  ( -1.323830074806763957, 12.01461446423264690, 44.47857376182257383 ) ) ;
#1284=( NAMED_UNIT ( * ) PLANE_ANGLE_UNIT ( ) SI_UNIT ( $, .RADIAN. ) );
#1293=VERTEX_POINT ( 'NONE', #6897 ) ;
#1299=CARTESIAN_POINT ( 'NONE',  ( -4.178947244162636743, 48.81675275154077553, -3.367451375481286036 ) ) ;
#1300=CARTESIAN_POINT ( 'NONE',  ( -1.046936909428679119, -45.77873603877005593, 1.275306677858721649 ) ) ;
#1304=CARTESIAN_POINT ( 'NONE',  ( -20.57838717382308147, -28.96176188950224528, -7.715628353033566533 ) ) ;
#1305=EDGE_CURVE ( 'NONE', #3709, #21873, #15309, .T. ) ;
#1306=EDGE_CURVE ( 'NONE', #26104, #26383, #19462, .T. ) ;
#1315=ORIENTED_EDGE ( 'NONE', *, *, #6198, .F. ) ;
#1317=VERTEX_POINT ( 'NONE', #11066 ) ;
#1321=CARTESIAN_POINT ( 'NONE',  ( -55.25719721206881729, 0.01079965405819919254, 0.002847566758682530588 ) ) ;
#1324=CARTESIAN_POINT ( 'NONE',  ( -20.47566262905010248, -1.586617686065349808, 29.82700878811085232 ) ) ;
#1325=CARTESIAN_POINT ( 'NONE',  ( -1.259972190295304939, 2.243354636026407611, 45.95417440459613800 ) ) ;
#1333=CARTESIAN_POINT ( 'NONE',  ( -1.113548883309551485, -1.968251867498553409, 45.82026503946953255 ) ) ;
#1348=B_SPLINE_CURVE_WITH_KNOTS ( 'NONE', 3,
 ( #18015, #8682, #26804, #17869, #26515, #11406, #15424, #10990, #15565, #20326 ),
 .UNSPECIFIED., .F., .F.,
 ( 4, 2, 2, 2, 4 ),
 ( 2.913600445039318278E-16, 0.0003346187017559067080, 0.0006692374035115219826, 0.001003856105267137474, 0.001338474807022752748 ),
 .UNSPECIFIED. ) ;
#1350=CARTESIAN_POINT ( 'NONE',  ( -1.031422197589711987, -43.06660437151296605, 15.60268798220683273 ) ) ;
#1351=CARTESIAN_POINT ( 'NONE',  ( -22.23342874802668589, 24.24669006619402367, 20.31166691703097982 ) ) ;
#1353=CARTESIAN_POINT ( 'NONE',  ( -20.57838717382308147, 29.92853265176831812, -1.611677988432464126 ) ) ;
#1361=EDGE_CURVE ( 'NONE', #5981, #19211, #7343, .T. ) ;
#1362=CARTESIAN_POINT ( 'NONE',  ( -2.911734481061404534, -17.36785190846011417, -44.38410240830297226 ) ) ;
#1365=B_SPLINE_CURVE_WITH_KNOTS ( 'NONE', 3,
 ( #21938, #28258, #26530, #4092, #8558, #4376, #13429, #17324 ),
 .UNSPECIFIED., .F., .F.,
 ( 4, 2, 2, 4 ),
 ( 2.251264292202123005E-16, 0.002761568181852872006, 0.005523136363705519365, 0.01104627272741081322 ),
 .UNSPECIFIED. ) ;
#1371=CARTESIAN_POINT ( 'NONE',  ( -4.473127245936434626, 12.17046501147516224, -47.80062405537804437 ) ) ;
#1375=ORIENTED_EDGE ( 'NONE', *, *, #8006, .F. ) ;
#1380=CARTESIAN_POINT ( 'NONE',  ( -20.57838717382308147, 1.611677988432361097, -29.92853265176831812 ) ) ;
#1382=LINE ( 'NONE', #3688, #374 ) ;
#1383=CARTESIAN_POINT ( 'NONE',  ( -55.24728320129491266, -0.003868537197316565448, -0.01402509393918558236 ) ) ;
#1389=EDGE_CURVE ( 'NONE', #18251, #1487, #10971, .T. ) ;
#1393=DIRECTION ( 'NONE',  ( -0.7563875759206388771, -0.2351350468682952832, -0.6104009704506900835 ) ) ;
#1400=DIRECTION ( 'NONE',  ( 1.000000000000000000, -6.938893903907226837E-18, 1.734723475976806709E-18 ) ) ;
#1404=CARTESIAN_POINT ( 'NONE',  ( -1.323830074806765289, -28.92190886481839129, 35.86387698262947055 ) ) ;
#1406=CARTESIAN_POINT ( 'NONE',  ( -20.20700224038492010, -10.08426345511570332, 27.82980252387829623 ) ) ;
#1410=CIRCLE ( 'NONE', #21621, 34.60786435723138510 ) ;
#1412=CARTESIAN_POINT ( 'NONE',  ( -4.162674018437148682, 41.48630000627055381, -25.90909455705125453 ) ) ;
#1416=VERTEX_POINT ( 'NONE', #7914 ) ;
#1426=CARTESIAN_POINT ( 'NONE',  ( -18.41936578851719730, -37.37524689996168803, 20.09935324538230006 ) ) ;
#1433=CARTESIAN_POINT ( 'NONE',  ( -7.711401346138400115, 38.61705198405368122, -35.51061203065540894 ) ) ;
#1435=DIRECTION ( 'NONE',  ( -1.000000000000000000, 6.938893903907226837E-18, -1.734723475976806709E-18 ) ) ;
#1440=ORIENTED_EDGE ( 'NONE', *, *, #23420, .F. ) ;
#1472=CARTESIAN_POINT ( 'NONE',  ( -20.24419206586951603, 24.70913649113854049, 16.36655224501340555 ) ) ;
#1479=CARTESIAN_POINT ( 'NONE',  ( -55.25297051322618813, -0.01483298743814594547, 0.001818774723749421287 ) ) ;
#1485=CARTESIAN_POINT ( 'NONE',  ( -1.239374126674604337, -16.50008610789269170, 42.99367564261294206 ) ) ;
#1486=CARTESIAN_POINT ( 'NONE',  ( -1.050229599974477290, 26.71319688967688322, 37.20249516760145525 ) ) ;
#1487=VERTEX_POINT ( 'NONE', #4124 ) ;
#1493=EDGE_CURVE ( 'NONE', #26004, #9976, #25660, .T. ) ;
#1496=EDGE_CURVE ( 'NONE', #733, #1672, #24988, .T. ) ;
#1497=CARTESIAN_POINT ( 'NONE',  ( -20.57838717382308147, 1.611677988432778319, 29.92853265176829325 ) ) ;
#1501=CARTESIAN_POINT ( 'NONE',  ( -24.53237795827028123, -6.738475012719871593, 33.25734978085275628 ) ) ;
#1504=VECTOR ( 'NONE', #23787, 1000.000000000000114 ) ;
#1507=CARTESIAN_POINT ( 'NONE',  ( -1.619063947482197729, -38.92136151114925724, -25.20140673341360227 ) ) ;
#1513=( BOUNDED_SURFACE ( )  B_SPLINE_SURFACE ( 3, 1, ( 
 ( #4474, #3570 ),
 ( #6038, #10223 ),
 ( #25616, #10486 ),
 ( #23031, #1138 ) ),
 .UNSPECIFIED., .F., .F., .F. ) 
 B_SPLINE_SURFACE_WITH_KNOTS ( ( 4, 4 ),
 ( 2, 2 ),
 ( 0.000000000000000000, 1.000000000000000000 ),
 ( 0.000000000000000000, 1.000000000000000000 ),
 .UNSPECIFIED. ) 
 GEOMETRIC_REPRESENTATION_ITEM ( )  RATIONAL_B_SPLINE_SURFACE ( (
 ( 1.000000000000000000, 1.000000000000000000),
 ( 0.7789835883360578528, 0.9689951854195403280),
 ( 0.7789835883360578528, 0.9689951854195403280),
 ( 1.000000000000000000, 1.000000000000000000) ) ) 
 REPRESENTATION_ITEM ( '' )  SURFACE ( )  );
#1515=CARTESIAN_POINT ( 'NONE',  ( -1.619063947482197729, -25.20140673341401438, -38.92136151114898723 ) ) ;
#1517=CARTESIAN_POINT ( 'NONE',  ( -1.583189561560252701, -46.33203782964464068, -2.490696082059713046 ) ) ;
#1518=CARTESIAN_POINT ( 'NONE',  ( -20.57838717382308502, 25.16001208503106668, -16.28767523336130196 ) ) ;
#1519=ORIENTED_EDGE ( 'NONE', *, *, #10871, .T. ) ;
#1523=VERTEX_POINT ( 'NONE', #15912 ) ;
#1526=ORIENTED_EDGE ( 'NONE', *, *, #25692, .T. ) ;
#1532=AXIS2_PLACEMENT_3D ( 'NONE', #8845, #27889, #10356 ) ;
#1538=FACE_OUTER_BOUND ( 'NONE', #5157, .T. ) ;
#1540=ORIENTED_EDGE ( 'NONE', *, *, #10596, .T. ) ;
#1542=CARTESIAN_POINT ( 'NONE',  ( -22.34422965417122953, 6.759368364654329220, -37.30738373203623581 ) ) ;
#1545=CARTESIAN_POINT ( 'NONE',  ( -20.57838717382308147, -7.715628353033481268, 28.96176188950225949 ) ) ;
#1546=B_SPLINE_CURVE_WITH_KNOTS ( 'NONE', 3,
 ( #19880, #13249, #168, #4623, #4772, #14211 ),
 .UNSPECIFIED., .F., .F.,
 ( 4, 2, 4 ),
 ( 0.000000000000000000, 0.0004335184443140242989, 0.0008670368886280485979 ),
 .UNSPECIFIED. ) ;
#1550=CARTESIAN_POINT ( 'NONE',  ( -25.21435515916025594, 1.749597353048488237E-16, -4.373993382621220594E-17 ) ) ;
#1552=CARTESIAN_POINT ( 'NONE',  ( -18.41936578851709783, 37.37524689996197935, -20.09935324538209045 ) ) ;
#1558=CARTESIAN_POINT ( 'NONE',  ( -6.574463467970655728, 34.08059230520098737, 38.37705091668339463 ) ) ;
#1559=EDGE_LOOP ( 'NONE', ( #15507, #13669, #15161, #23910 ) ) ;
#1560=CARTESIAN_POINT ( 'NONE',  ( -55.25719721206881729, -0.006045473558784038998, 0.009391134844733136505 ) ) ;
#1561=CARTESIAN_POINT ( 'NONE',  ( -23.79248802219731473, -16.82188324679459868, 28.61009539422402881 ) ) ;
#1574=CARTESIAN_POINT ( 'NONE',  ( -28.41354790283022069, -12.60397206714818097, 19.47297445639563307 ) ) ;
#1580=CARTESIAN_POINT ( 'NONE',  ( -1.113427685306995318, 28.52429901637220411, 35.91272432484627330 ) ) ;
#1582=ORIENTED_EDGE ( 'NONE', *, *, #26831, .T. ) ;
#1584=FACE_OUTER_BOUND ( 'NONE', #1559, .T. ) ;
#1598=CARTESIAN_POINT ( 'NONE',  ( -8.259864102781671491, -9.986657004933254811, 52.06232470801721490 ) ) ;
#1600=( BOUNDED_SURFACE ( )  B_SPLINE_SURFACE ( 3, 1, ( 
 ( #22171, #2437 ),
 ( #14978, #6638 ),
 ( #28347, #6225 ),
 ( #1876, #15391 ) ),
 .UNSPECIFIED., .F., .F., .F. ) 
 B_SPLINE_SURFACE_WITH_KNOTS ( ( 4, 4 ),
 ( 2, 2 ),
 ( 0.000000000000000000, 1.000000000000000000 ),
 ( 0.000000000000000000, 1.000000000000000000 ),
 .UNSPECIFIED. ) 
 GEOMETRIC_REPRESENTATION_ITEM ( )  RATIONAL_B_SPLINE_SURFACE ( (
 ( 1.000000000000000000, 1.000000000000000000),
 ( 0.9934239774497838349, 0.8357310067453913582),
 ( 0.9934239774497838349, 0.8357310067453913582),
 ( 1.000000000000000000, 1.000000000000000000) ) ) 
 REPRESENTATION_ITEM ( '' )  SURFACE ( )  );
#1602=EDGE_CURVE ( 'NONE', #11658, #27831, #4011, .T. ) ;
#1606=CARTESIAN_POINT ( 'NONE',  ( -20.20700224038492365, 10.08426345511628597, 27.82980252387807951 ) ) ;
#1612=CARTESIAN_POINT ( 'NONE',  ( -1.323439229708139875, 46.01398008004444762, -2.317790194799894010 ) ) ;
#1613=CARTESIAN_POINT ( 'NONE',  ( -16.86833981943423311, 19.19877306373907189, 39.83928801320569590 ) ) ;
#1617=CARTESIAN_POINT ( 'NONE',  ( -55.24390624410018802, -0.007503127514277506058, -0.007245494385991484328 ) ) ;
#1626=CARTESIAN_POINT ( 'NONE',  ( -6.574463467970653952, -51.07975593197902953, 5.014313797967556496 ) ) ;
#1627=CARTESIAN_POINT ( 'NONE',  ( -1.045287976400365970, 45.76855895860943235, -1.530335034934267258 ) ) ;
#1628=ORIENTED_EDGE ( 'NONE', *, *, #24073, .T. ) ;
#1639=VERTEX_POINT ( 'NONE', #25837 ) ;
#1649=CARTESIAN_POINT ( 'NONE',  ( -20.20700224038492721, -27.82980252387812570, 10.08426345511618649 ) ) ;
#1650=CARTESIAN_POINT ( 'NONE',  ( -55.24271866751342941, -0.001425019990778747699, -0.009388511352200236415 ) ) ;
#1666=( BOUNDED_SURFACE ( )  B_SPLINE_SURFACE ( 3, 1, ( 
 ( #19392, #8329 ),
 ( #22120, #26565 ),
 ( #239, #24289 ),
 ( #26021, #19806 ) ),
 .UNSPECIFIED., .F., .F., .F. ) 
 B_SPLINE_SURFACE_WITH_KNOTS ( ( 4, 4 ),
 ( 2, 2 ),
 ( 0.000000000000000000, 1.000000000000000000 ),
 ( 0.000000000000000000, 1.000000000000000000 ),
 .UNSPECIFIED. ) 
 GEOMETRIC_REPRESENTATION_ITEM ( )  RATIONAL_B_SPLINE_SURFACE ( (
 ( 1.000000000000000000, 1.000000000000000000),
 ( 0.7789835883360576307, 0.9689951854195403280),
 ( 0.7789835883360576307, 0.9689951854195403280),
 ( 1.000000000000000000, 1.000000000000000000) ) ) 
 REPRESENTATION_ITEM ( '' )  SURFACE ( )  );
#1672=VERTEX_POINT ( 'NONE', #1507 ) ;
#1683=CARTESIAN_POINT ( 'NONE',  ( -25.21435515916043713, 4.655591116594827383, 34.29329011225949841 ) ) ;
#1685=PLANE ( 'NONE',  #21136 ) ;
#1689=EDGE_CURVE ( 'NONE', #21619, #8934, #6086, .T. ) ;
#1690=VERTEX_POINT ( 'NONE', #8148 ) ;
#1694=ADVANCED_FACE ( 'NONE', ( #5984 ), #18525, .F. ) ;
#1697=ORIENTED_EDGE ( 'NONE', *, *, #12105, .T. ) ;
#1710=CARTESIAN_POINT ( 'NONE',  ( -1.539760825549688850, 29.16712717142812039, 35.94320866319458219 ) ) ;
#1729=ORIENTED_EDGE ( 'NONE', *, *, #10485, .F. ) ;
#1731=EDGE_CURVE ( 'NONE', #11830, #18479, #26633, .T. ) ;
#1742=CARTESIAN_POINT ( 'NONE',  ( -55.24390624410018802, -0.01027195578987978239, -0.001811362924362686826 ) ) ;
#1743=FACE_OUTER_BOUND ( 'NONE', #27486, .T. ) ;
#1745=EDGE_CURVE ( 'NONE', #15398, #12444, #11416, .T. ) ;
#1750=ADVANCED_FACE ( 'NONE', ( #11138 ), #7711, .F. ) ;
#1751=CARTESIAN_POINT ( 'NONE',  ( -1.045287976400362417, 25.66401692419989899, -37.92705037016767733 ) ) ;
#1754=ORIENTED_EDGE ( 'NONE', *, *, #19850, .T. ) ;
#1756=ORIENTED_EDGE ( 'NONE', *, *, #11864, .T. ) ;
#1765=B_SPLINE_CURVE_WITH_KNOTS ( 'NONE', 3,
 ( #5159, #18243, #9625, #18388, #1135, #5597 ),
 .UNSPECIFIED., .F., .F.,
 ( 4, 2, 4 ),
 ( 3.469446951953613804E-18, 0.0004335184443139973023, 0.0008670368886279911352 ),
 .UNSPECIFIED. ) ;
#1776=ORIENTED_EDGE ( 'NONE', *, *, #14718, .T. ) ;
#1779=CARTESIAN_POINT ( 'NONE',  ( -55.24728320129491266, 0.009072670231978626973, -0.01137345571547102377 ) ) ;
#1784=B_SPLINE_CURVE_WITH_KNOTS ( 'NONE', 3,
 ( #16588, #756, #5660, #14423, #23232, #3483, #21035 ),
 .UNSPECIFIED., .F., .F.,
 ( 4, 3, 4 ),
 ( 0.000000000000000000, 0.006568092053401769319, 0.02506242213020846987 ),
 .UNSPECIFIED. ) ;
#1785=CARTESIAN_POINT ( 'NONE',  ( -25.21435515916043713, 6.169479169075932745, 34.05351380035326514 ) ) ;
#1790=ORIENTED_EDGE ( 'NONE', *, *, #15453, .F. ) ;
#1798=CARTESIAN_POINT ( 'NONE',  ( -1.583189561560255143, 46.33203782964461936, 2.490696082060026573 ) ) ;
#1803=CARTESIAN_POINT ( 'NONE',  ( -20.20700224038492010, 8.199606986804733211, 28.44216453106527709 ) ) ;
#1804=CARTESIAN_POINT ( 'NONE',  ( -20.24399999263416561, 24.70869149526203401, -16.36687688782867411 ) ) ;
#1813=CARTESIAN_POINT ( 'NONE',  ( -1.045287976400383290, -44.00138577190632816, 12.68782741917368106 ) ) ;
#1816=EDGE_CURVE ( 'NONE', #6924, #23596, #26389, .T. ) ;
#1819=CARTESIAN_POINT ( 'NONE',  ( -1.019300379054419947, -38.21680004809145714, 25.26451264419685572 ) ) ;
#1826=CIRCLE ( 'NONE', #4605, 53.53553390275978785 ) ;
#1835=CARTESIAN_POINT ( 'NONE',  ( -1.050229599974481065, 36.90196321294333615, 27.12684363859215608 ) ) ;
#1838=DIRECTION ( 'NONE',  ( 0.000000000000000000, 5.223019709707975211E-21, -1.000000000000000000 ) ) ;
#1840=EDGE_CURVE ( 'NONE', #7314, #2342, #25244, .T. ) ;
#1842=CARTESIAN_POINT ( 'NONE',  ( -8.786685647604890903, -25.35688121747466184, 47.14957014837381166 ) ) ;
#1844=CARTESIAN_POINT ( 'NONE',  ( -20.20700224038492721, -10.08426345511609235, -27.82980252387815767 ) ) ;
#1845=ORIENTED_EDGE ( 'NONE', *, *, #19157, .F. ) ;
#1847=AXIS2_PLACEMENT_3D ( 'NONE', #23932, #8656, #24077 ) ;
#1850=CARTESIAN_POINT ( 'NONE',  ( -1.044556982611267948, -43.01635920718339179, 15.70482750345280820 ) ) ;
#1853=AXIS2_PLACEMENT_3D ( 'NONE', #18213, #7302, #16351 ) ;
#1857=CARTESIAN_POINT ( 'NONE',  ( -55.24390624410018802, 0.004572280736702236288, 0.009374879212970765180 ) ) ;
#1861=VECTOR ( 'NONE', #11403, 1000.000000000000114 ) ;
#1865=ORIENTED_EDGE ( 'NONE', *, *, #6707, .F. ) ;
#1869=B_SPLINE_CURVE_WITH_KNOTS ( 'NONE', 3,
 ( #1021, #1168, #27201, #9816, #18582, #21013, #25510, #16562 ),
 .UNSPECIFIED., .F., .F.,
 ( 4, 2, 2, 4 ),
 ( 2.223105199230524488E-16, 0.002761568181852866802, 0.005523136363705516763, 0.01104627272741080628 ),
 .UNSPECIFIED. ) ;
#1876=CARTESIAN_POINT ( 'NONE',  ( -55.24390624410018802, -0.01032895241566962087, 0.001451500391950532459 ) ) ;
#1878=AXIS2_PLACEMENT_3D ( 'NONE', #6192, #15353, #12916 ) ;
#1888=CARTESIAN_POINT ( 'NONE',  ( -20.57838717382308147, -29.92853265176830746, 1.611677988432673070 ) ) ;
#1891=CARTESIAN_POINT ( 'NONE',  ( -1.619063947482197729, -16.67502769180532596, 43.26576862488450104 ) ) ;
#1898=VERTEX_POINT ( 'NONE', #7548 ) ;
#1900=CARTESIAN_POINT ( 'NONE',  ( -1.050230346682680560, 45.79907861045643358, 0.0006945978177289460027 ) ) ;
#1901=VERTEX_POINT ( 'NONE', #27383 ) ;
#1903=EDGE_LOOP ( 'NONE', ( #25085, #10046, #18799, #3743 ) ) ;
#1907=CARTESIAN_POINT ( 'NONE',  ( -55.24300891470650754, 0.009439835024159288004, 0.002702093572893217704 ) ) ;
#1916=ORIENTED_EDGE ( 'NONE', *, *, #4191, .T. ) ;
#1925=CARTESIAN_POINT ( 'NONE',  ( -1.046935749539995353, -36.28605774377782467, -27.93995161054682441 ) ) ;
#1930=CARTESIAN_POINT ( 'NONE',  ( -1.058197053496165108, -15.81317659443655721, 42.99116279335168400 ) ) ;
#1931=AXIS2_PLACEMENT_3D ( 'NONE', #3378, #6929, #18534 ) ;
#1935=ORIENTED_EDGE ( 'NONE', *, *, #21425, .T. ) ;
#1938=ADVANCED_FACE ( 'NONE', ( #11076 ), #8605, .F. ) ;
#1958=CARTESIAN_POINT ( 'NONE',  ( -1.050229599974472627, -43.63650726458052986, 13.90955673306172002 ) ) ;
#1963=CARTESIAN_POINT ( 'NONE',  ( -1.239374126674604337, -2.406737988130801309, 45.98822239537608425 ) ) ;
#1970=ADVANCED_FACE ( 'NONE', ( #13091 ), #18705, .F. ) ;
#1973=ORIENTED_EDGE ( 'NONE', *, *, #8707, .T. ) ;
#1977=ORIENTED_EDGE ( 'NONE', *, *, #10816, .T. ) ;
#1987=CARTESIAN_POINT ( 'NONE',  ( -7.733045908741336127, 5.980865481988145937, -52.15131830128824220 ) ) ;
#1994=ORIENTED_EDGE ( 'NONE', *, *, #23288, .F. ) ;
#2003=FACE_OUTER_BOUND ( 'NONE', #18739, .T. ) ;
#2013=( BOUNDED_SURFACE ( )  B_SPLINE_SURFACE ( 3, 1, ( 
 ( #14369, #27608 ),
 ( #12766, #23187 ),
 ( #20986, #23749 ),
 ( #1560, #25748 ) ),
 .UNSPECIFIED., .F., .F., .F. ) 
 B_SPLINE_SURFACE_WITH_KNOTS ( ( 4, 4 ),
 ( 2, 2 ),
 ( 0.000000000000000000, 1.000000000000000000 ),
 ( 0.000000000000000000, 1.000000000000000000 ),
 .UNSPECIFIED. ) 
 GEOMETRIC_REPRESENTATION_ITEM ( )  RATIONAL_B_SPLINE_SURFACE ( (
 ( 1.000000000000000000, 1.000000000000000000),
 ( 0.7789835883360576307, 0.9689951854195403280),
 ( 0.7789835883360576307, 0.9689951854195403280),
 ( 1.000000000000000000, 1.000000000000000000) ) ) 
 REPRESENTATION_ITEM ( '' )  SURFACE ( )  );
#2015=ORIENTED_EDGE ( 'NONE', *, *, #25109, .T. ) ;
#2020=B_SPLINE_CURVE_WITH_KNOTS ( 'NONE', 3,
 ( #28244, #4074, #15136, #6124, #14876, #25697, #14730 ),
 .UNSPECIFIED., .F., .F.,
 ( 4, 3, 4 ),
 ( 0.000000000000000000, 0.006568092053401771921, 0.02506242213020852885 ),
 .UNSPECIFIED. ) ;
#2024=CARTESIAN_POINT ( 'NONE',  ( -25.21435515916043713, 34.05351380035342146, 6.169479169075106739 ) ) ;
#2026=DIRECTION ( 'NONE',  ( 1.000000000000000000, -6.938893903907226837E-18, 1.734723475976806709E-18 ) ) ;
#2028=CARTESIAN_POINT ( 'NONE',  ( -1.044556982611269058, -36.05793013899078403, 28.22896456560707534 ) ) ;
#2029=CARTESIAN_POINT ( 'NONE',  ( -1.050230346682680560, -26.92058491724839797, 37.05182464822011923 ) ) ;
#2031=CARTESIAN_POINT ( 'NONE',  ( -25.21435515916043713, -6.169479169075696490, -34.05351380035330777 ) ) ;
#2036=CARTESIAN_POINT ( 'NONE',  ( -25.21435515916043713, -31.17620025257598471, -15.02493970636134613 ) ) ;
#2038=EDGE_CURVE ( 'NONE', #20677, #20045, #958, .T. ) ;
#2054=ORIENTED_EDGE ( 'NONE', *, *, #18217, .F. ) ;
#2057=CARTESIAN_POINT ( 'NONE',  ( -4.473127245936434626, 31.51789735524247504, 37.94261489385684882 ) ) ;
#2061=ORIENTED_EDGE ( 'NONE', *, *, #18923, .T. ) ;
#2063=CARTESIAN_POINT ( 'NONE',  ( -1.048172774974284405, -27.73787987941035027, -36.44231470008705998 ) ) ;
#2066=ADVANCED_FACE ( 'NONE', ( #15817 ), #21690, .F. ) ;
#2067=CARTESIAN_POINT ( 'NONE',  ( -7.733045908741340568, -10.42750254442575120, -51.44704017882771296 ) ) ;
#2081=B_SPLINE_CURVE_WITH_KNOTS ( 'NONE', 3,
 ( #27281, #7593, #7739, #10033 ),
 .UNSPECIFIED., .F., .F.,
 ( 4, 4 ),
 ( 1.977889076651310254E-16, 0.001982023823822932906 ),
 .UNSPECIFIED. ) ;
#2082=CARTESIAN_POINT ( 'NONE',  ( -20.37983603106074426, 7.753708011498974706, 28.74620395171554321 ) ) ;
#2083=PRODUCT ( 'pinion 3', 'pinion 3', '', ( #5724 ) ) ;
#2085=CARTESIAN_POINT ( 'NONE',  ( -21.41427618760446450, -30.75468365310881325, -1.815001260755733536 ) ) ;
#2091=CARTESIAN_POINT ( 'NONE',  ( -55.24271866751342941, -0.008433070970613520956, 0.004365563123935277227 ) ) ;
#2096=EDGE_LOOP ( 'NONE', ( #28233, #26782, #28214, #17757 ) ) ;
#2097=CARTESIAN_POINT ( 'NONE',  ( -55.24300891470648622, -0.005486913146696059326, -0.008142823778062177609 ) ) ;
#2101=CARTESIAN_POINT ( 'NONE',  ( -2.911734481061400537, 30.23325065583413718, 36.84482841982617884 ) ) ;
#2105=ORIENTED_EDGE ( 'NONE', *, *, #20102, .F. ) ;
#2108=ORIENTED_EDGE ( 'NONE', *, *, #24654, .T. ) ;
#2109=CARTESIAN_POINT ( 'NONE',  ( -23.79223135445719706, -22.01133905265668034, 24.83942264280426926 ) ) ;
#2110=CARTESIAN_POINT ( 'NONE',  ( -55.24300891470650754, -0.006048736206179085827, -0.007734635432136639961 ) ) ;
#2111=DIRECTION ( 'NONE',  ( 0.000000000000000000, 5.223019709707975211E-21, -1.000000000000000000 ) ) ;
#2114=CARTESIAN_POINT ( 'NONE',  ( -25.21435515916025594, 1.749597353048488237E-16, -4.373993382621220594E-17 ) ) ;
#2119=CARTESIAN_POINT ( 'NONE',  ( -1.056502255334265339, -43.72121397317214786, 13.66916755949895546 ) ) ;
#2123=CARTESIAN_POINT ( 'NONE',  ( -25.21435515916025594, 34.29329011225976842, -4.655591116594504086 ) ) ;
#2124=CARTESIAN_POINT ( 'NONE',  ( -20.47566262905009893, -28.85746289809572218, 7.708089517695493775 ) ) ;
#2133=CARTESIAN_POINT ( 'NONE',  ( -55.24271866751342941, 0.004256484107795918508, -0.008488649505343059953 ) ) ;
#2136=B_SPLINE_CURVE_WITH_KNOTS ( 'NONE', 3,
 ( #3890, #13081, #25914, #19691, #24044, #6617, #19421 ),
 .UNSPECIFIED., .F., .F.,
 ( 4, 3, 4 ),
 ( 0.000000000000000000, 0.006568092053401751972, 0.02506242213020840742 ),
 .UNSPECIFIED. ) ;
#2137=CARTESIAN_POINT ( 'NONE',  ( -2.911734481061404090, 40.13920818157116344, 25.69892591260225245 ) ) ;
#2144=CARTESIAN_POINT ( 'NONE',  ( -24.53237795827032031, -16.68575684089471878, 29.54731592868582979 ) ) ;
#2145=FACE_OUTER_BOUND ( 'NONE', #853, .T. ) ;
#2149=CARTESIAN_POINT ( 'NONE',  ( -6.588769196390773963, 47.06982923582537381, 20.50531526814514294 ) ) ;
#2162=EDGE_CURVE ( 'NONE', #10634, #24113, #8232, .T. ) ;
#2166=ORIENTED_EDGE ( 'NONE', *, *, #1305, .F. ) ;
#2168=CARTESIAN_POINT ( 'NONE',  ( -1.539760825549679080, 38.84664866728813593, 25.17088484262099612 ) ) ;
#2177=CARTESIAN_POINT ( 'NONE',  ( -1.259920593601975058, -45.95412615877143026, -2.243284667987618608 ) ) ;
#2185=CARTESIAN_POINT ( 'NONE',  ( -20.20700224038492721, -23.35150625415671755, -18.19058640100215385 ) ) ;
#2188=ORIENTED_EDGE ( 'NONE', *, *, #8930, .T. ) ;
#2192=CARTESIAN_POINT ( 'NONE',  ( -1.259920593601978833, -28.82601305773628297, 35.85909937955954518 ) ) ;
#2193=CARTESIAN_POINT ( 'NONE',  ( -55.24198130335446422, 0.009170435128245573234, 0.001516807524708093389 ) ) ;
#2194=CARTESIAN_POINT ( 'NONE',  ( -1.583189561560252701, 36.01941156322829585, 29.24830400313125978 ) ) ;
#2199=CARTESIAN_POINT ( 'NONE',  ( -1.045287976400365970, -37.92705037016778391, -25.66401692419976399 ) ) ;
#2211=CARTESIAN_POINT ( 'NONE',  ( -1.155001620486251213, 2.068551059060327546, -45.85729774065935516 ) ) ;
#2225=CARTESIAN_POINT ( 'NONE',  ( -1.056502255334264895, 45.80535052436397336, -0.5104472526221494055 ) ) ;
#2226=CARTESIAN_POINT ( 'NONE',  ( -8.259864102781506290, -46.42816643551554989, -25.58601832199090609 ) ) ;
#2227=ADVANCED_FACE ( 'NONE', ( #14791 ), #1685, .F. ) ;
#2228=DIRECTION ( 'NONE',  ( 1.000000000000000000, -6.938893903907226837E-18, 1.734723475976806709E-18 ) ) ;
#2239=CARTESIAN_POINT ( 'NONE',  ( -1.045287976400362417, -12.68782741917263657, 44.00138577190661948 ) ) ;
#2246=CARTESIAN_POINT ( 'NONE',  ( -55.24728320129491266, -0.003868537197316542463, 0.01402509393918130107 ) ) ;
#2249=CARTESIAN_POINT ( 'NONE',  ( -16.86833981943425087, -31.95666732167541113, 30.57013526701953054 ) ) ;
#2250=CARTESIAN_POINT ( 'NONE',  ( -1.583189561560255143, -43.29471907393753582, -16.68617981233685299 ) ) ;
#2251=DIRECTION ( 'NONE',  ( 0.000000000000000000, 5.223019709708233256E-21, -1.000000000000000000 ) ) ;
#2253=EDGE_CURVE ( 'NONE', #26396, #17575, #1382, .T. ) ;
#2258=CARTESIAN_POINT ( 'NONE',  ( -21.81686047589425925, 34.70276904128910189, 16.72402253294277230 ) ) ;
#2260=ORIENTED_EDGE ( 'NONE', *, *, #2387, .F. ) ;
#2268=CARTESIAN_POINT ( 'NONE',  ( -55.24271866751342941, 0.006671293903668402275, 0.006757859501010043089 ) ) ;
#2275=CARTESIAN_POINT ( 'NONE',  ( -1.031422197589716205, -15.60268798220668174, -43.06660437151303711 ) ) ;
#2277=B_SPLINE_CURVE_WITH_KNOTS ( 'NONE', 3,
 ( #12442, #16917, #18936, #10320 ),
 .UNSPECIFIED., .F., .F.,
 ( 4, 4 ),
 ( 1.892757412642747523E-16, 0.001982023823822945917 ),
 .UNSPECIFIED. ) ;
#2279=ORIENTED_EDGE ( 'NONE', *, *, #28227, .F. ) ;
#2287=ORIENTED_EDGE ( 'NONE', *, *, #21230, .F. ) ;
#2288=CARTESIAN_POINT ( 'NONE',  ( -19.53423201713129842, 1.355459634611817431E-16, -3.388649086529543578E-17 ) ) ;
#2291=CARTESIAN_POINT ( 'NONE',  ( -1.619063947482201282, -11.94059994246191359, -44.80407745103779860 ) ) ;
#2294=ORIENTED_EDGE ( 'NONE', *, *, #14119, .T. ) ;
#2296=CARTESIAN_POINT ( 'NONE',  ( -1.155031165708881202, -12.20332162035433576, 44.25214473648924951 ) ) ;
#2302=CARTESIAN_POINT ( 'NONE',  ( -20.20700224038492010, -18.19058640100240254, -23.35150625415651859 ) ) ;
#2303=CARTESIAN_POINT ( 'NONE',  ( -20.57838717382308502, 27.96569011373086866, -10.78122205917010135 ) ) ;
#2313=EDGE_LOOP ( 'NONE', ( #14788, #4286, #662, #16977 ) ) ;
#2318=EDGE_CURVE ( 'NONE', #26396, #15398, #7863, .T. ) ;
#2319=EDGE_CURVE ( 'NONE', #13547, #14642, #10272, .T. ) ;
#2325=CARTESIAN_POINT ( 'NONE',  ( -16.86833981943422600, -7.884812276281804699, 43.51541671545733436 ) ) ;
#2335=ORIENTED_EDGE ( 'NONE', *, *, #27227, .F. ) ;
#2338=CARTESIAN_POINT ( 'NONE',  ( -20.20997486282891131, -0.3303599360441825672, -29.60348406988234871 ) ) ;
#2342=VERTEX_POINT ( 'NONE', #10819 ) ;
#2347=CARTESIAN_POINT ( 'NONE',  ( -1.056502255334265339, 14.64009593116102614, -43.40574022158779144 ) ) ;
#2362=CARTESIAN_POINT ( 'NONE',  ( -55.24390624410018802, 0.001451500391951047672, 0.01032895241566990016 ) ) ;
#2375=VECTOR ( 'NONE', #3215, 1000.000000000000114 ) ;
#2387=EDGE_CURVE ( 'NONE', #15661, #7846, #15779, .T. ) ;
#2390=ORIENTED_EDGE ( 'NONE', *, *, #13514, .T. ) ;
#2394=CARTESIAN_POINT ( 'NONE',  ( -55.25719721206881729, -0.007063345920776780730, 0.008651607285660046359 ) ) ;
#2398=CARTESIAN_POINT ( 'NONE',  ( -7.711401346138398338, -6.030154970217270538, -52.11446537925909439 ) ) ;
#2401=CARTESIAN_POINT ( 'NONE',  ( -22.34422965417126150, -17.95715691811022552, 33.39267070835840912 ) ) ;
#2407=ORIENTED_EDGE ( 'NONE', *, *, #12847, .T. ) ;
#2411=CARTESIAN_POINT ( 'NONE',  ( -20.57838717382308147, 27.96569011373101077, 10.78122205916971055 ) ) ;
#2419=FACE_OUTER_BOUND ( 'NONE', #7849, .T. ) ;
#2429=CARTESIAN_POINT ( 'NONE',  ( -1.619063947482197729, -11.94059994246129008, 44.80407745103795492 ) ) ;
#2432=B_SPLINE_CURVE_WITH_KNOTS ( 'NONE', 3,
 ( #21925, #44, #11553, #22508, #16009, #13418, #2773, #20330 ),
 .UNSPECIFIED., .F., .F.,
 ( 4, 2, 2, 4 ),
 ( 0.000000000000000000, 0.002761524886576654115, 0.005523049773153308230, 0.01104609954630660952 ),
 .UNSPECIFIED. ) ;
#2433=ORIENTED_EDGE ( 'NONE', *, *, #24449, .F. ) ;
#2437=CARTESIAN_POINT ( 'NONE',  ( -1.031422197589711987, 25.67058493451442658, -37.93675465142480618 ) ) ;
#2446=CARTESIAN_POINT ( 'NONE',  ( -1.583189561560253589, 38.94740041318330981, 25.21827308671188561 ) ) ;
#2449=DIRECTION ( 'NONE',  ( 0.000000000000000000, 5.223019709708233256E-21, -1.000000000000000000 ) ) ;
#2450=CARTESIAN_POINT ( 'NONE',  ( -1.619063947482197729, -11.94059994246129008, 44.80407745103795492 ) ) ;
#2453=CARTESIAN_POINT ( 'NONE',  ( -1.619063947482197729, 43.26576862488456499, 16.67502769180516964 ) ) ;
#2454=CARTESIAN_POINT ( 'NONE',  ( -1.113427685307003534, -35.91272432484637278, 28.52429901637207266 ) ) ;
#2460=ORIENTED_EDGE ( 'NONE', *, *, #16287, .F. ) ;
#2462=EDGE_CURVE ( 'NONE', #7846, #5380, #13233, .T. ) ;
#2467=ORIENTED_EDGE ( 'NONE', *, *, #15714, .F. ) ;
#2472=ORIENTED_EDGE ( 'NONE', *, *, #11972, .F. ) ;
#2484=ORIENTED_EDGE ( 'NONE', *, *, #17025, .T. ) ;
#2493=VERTEX_POINT ( 'NONE', #2239 ) ;
#2496=ORIENTED_EDGE ( 'NONE', *, *, #14089, .T. ) ;
#2497=ORIENTED_EDGE ( 'NONE', *, *, #11941, .F. ) ;
#2501=ORIENTED_EDGE ( 'NONE', *, *, #23556, .F. ) ;
#2503=ORIENTED_EDGE ( 'NONE', *, *, #23561, .F. ) ;
#2504=( BOUNDED_SURFACE ( )  B_SPLINE_SURFACE ( 3, 1, ( 
 ( #10194, #1798 ),
 ( #25454, #19368 ),
 ( #28141, #17208 ),
 ( #6287, #221 ) ),
 .UNSPECIFIED., .F., .F., .F. ) 
 B_SPLINE_SURFACE_WITH_KNOTS ( ( 4, 4 ),
 ( 2, 2 ),
 ( 0.000000000000000000, 1.000000000000000000 ),
 ( 0.000000000000000000, 1.000000000000000000 ),
 .UNSPECIFIED. ) 
 GEOMETRIC_REPRESENTATION_ITEM ( )  RATIONAL_B_SPLINE_SURFACE ( (
 ( 1.000000000000000000, 1.000000000000000000),
 ( 0.9934239774497837239, 0.8357310067453919133),
 ( 0.9934239774497837239, 0.8357310067453919133),
 ( 1.000000000000000000, 1.000000000000000000) ) ) 
 REPRESENTATION_ITEM ( '' )  SURFACE ( )  );
#2510=CARTESIAN_POINT ( 'NONE',  ( -55.24271866751342941, 0.001425019990782615698, -0.009388511352197861579 ) ) ;
#2513=CARTESIAN_POINT ( 'NONE',  ( -55.24271866751342941, 0.006757859501006707216, 0.006671293903669109175 ) ) ;
#2520=CARTESIAN_POINT ( 'NONE',  ( -8.786685647604720373, -47.14957014837338534, -25.35688121747513435 ) ) ;
#2525=ORIENTED_EDGE ( 'NONE', *, *, #9725, .F. ) ;
#2527=ADVANCED_FACE ( 'NONE', ( #811 ), #10629, .F. ) ;
#2531=EDGE_LOOP ( 'NONE', ( #19992, #26224, #27993, #15738 ) ) ;
#2541=CARTESIAN_POINT ( 'NONE',  ( -9.156249394959706578, 53.90509764945129945, 8.027840202794124025 ) ) ;
#2551=ORIENTED_EDGE ( 'NONE', *, *, #25140, .F. ) ;
#2552=ORIENTED_EDGE ( 'NONE', *, *, #10951, .F. ) ;
#2558=CARTESIAN_POINT ( 'NONE',  ( -1.058197053496161555, -38.06270006878834522, 25.48582931365511328 ) ) ;
#2561=CARTESIAN_POINT ( 'NONE',  ( -20.21097721712959583, -8.835581498567664838, -28.26295595852182529 ) ) ;
#2574=CARTESIAN_POINT ( 'NONE',  ( -8.786685647604887350, 53.04920435127183254, 7.199674155859139724 ) ) ;
#2578=B_SPLINE_CURVE_WITH_KNOTS ( 'NONE', 3,
 ( #789, #5102, #13880, #2958, #16184, #6851 ),
 .UNSPECIFIED., .F., .F.,
 ( 4, 2, 4 ),
 ( 3.689388176052398149E-16, 0.003576372551511164399, 0.007152745103021965374 ),
 .UNSPECIFIED. ) ;
#2579=ORIENTED_EDGE ( 'NONE', *, *, #10709, .T. ) ;
#2580=VERTEX_POINT ( 'NONE', #325 ) ;
#2581=CARTESIAN_POINT ( 'NONE',  ( -20.20700224038492721, -18.19058640100206503, 23.35150625415678860 ) ) ;
#2583=CARTESIAN_POINT ( 'NONE',  ( -20.47566338032525124, 16.24827550219824701, -25.06314818626695740 ) ) ;
#2585=B_SPLINE_CURVE_WITH_KNOTS ( 'NONE', 3,
 ( #22186, #17425, #11, #28362, #12972, #4338, #2454, #6508, #2028, #4471 ),
 .UNSPECIFIED., .F., .F.,
 ( 4, 2, 2, 2, 4 ),
 ( 0.000000000000000000, 0.0003346267210630928380, 0.0006692534421261856761, 0.001003880163189278460, 0.001338506884252371352 ),
 .UNSPECIFIED. ) ;
#2587=ORIENTED_EDGE ( 'NONE', *, *, #7537, .F. ) ;
#2592=CARTESIAN_POINT ( 'NONE',  ( -55.25719721206881729, 0.01041086141212550775, -0.004044147484878501606 ) ) ;
#2593=CARTESIAN_POINT ( 'NONE',  ( -1.049817751779871688, -37.35030165458155693, 26.50542916749608580 ) ) ;
#2598=( BOUNDED_SURFACE ( )  B_SPLINE_SURFACE ( 3, 1, ( 
 ( #26107, #12720 ),
 ( #10860, #19345 ),
 ( #25839, #25975 ),
 ( #26244, #21933 ) ),
 .UNSPECIFIED., .F., .F., .F. ) 
 B_SPLINE_SURFACE_WITH_KNOTS ( ( 4, 4 ),
 ( 2, 2 ),
 ( 0.000000000000000000, 1.000000000000000000 ),
 ( 0.000000000000000000, 1.000000000000000000 ),
 .UNSPECIFIED. ) 
 GEOMETRIC_REPRESENTATION_ITEM ( )  RATIONAL_B_SPLINE_SURFACE ( (
 ( 1.000000000000000000, 1.000000000000000000),
 ( 0.9593753223639863714, 0.9995975284513187731),
 ( 0.9593753223639863714, 0.9995975284513187731),
 ( 1.000000000000000000, 1.000000000000000000) ) ) 
 REPRESENTATION_ITEM ( '' )  SURFACE ( )  );
#2602=EDGE_CURVE ( 'NONE', #23301, #11627, #22915, .T. ) ;
#2608=ORIENTED_EDGE ( 'NONE', *, *, #27061, .F. ) ;
#2615=CARTESIAN_POINT ( 'NONE',  ( -1.044556982611269502, 25.56989963842203650, -37.98985389331818396 ) ) ;
#2620=CARTESIAN_POINT ( 'NONE',  ( -55.24340739397742794, -0.009842732675348539115, -0.002421372372456522849 ) ) ;
#2623=B_SPLINE_CURVE_WITH_KNOTS ( 'NONE', 3,
 ( #2989, #11905, #9603, #18364, #15317, #6418, #23856, #13451, #19782, #6564 ),
 .UNSPECIFIED., .F., .F.,
 ( 4, 2, 2, 2, 4 ),
 ( 8.420559318810145779E-18, 0.0003346267210630978796, 0.0006692534421261874108, 0.001003880163189276942, 0.001338506884252366365 ),
 .UNSPECIFIED. ) ;
#2625=CARTESIAN_POINT ( 'NONE',  ( -21.41427618760447871, 29.81030852927067443, -7.777551129310157130 ) ) ;
#2634=CARTESIAN_POINT ( 'NONE',  ( -9.156249394959713683, 53.74753343182715781, 9.022661520477214481 ) ) ;
#2635=CARTESIAN_POINT ( 'NONE',  ( -9.156249394959706578, 48.32878616081010392, -25.18996226954632078 ) ) ;
#2639=CARTESIAN_POINT ( 'NONE',  ( -1.619063947482197729, -29.22875152547781852, -35.99532424477369830 ) ) ;
#2641=CARTESIAN_POINT ( 'NONE',  ( -20.20700224038492010, -0.9908225410476447781, 29.58392382092673500 ) ) ;
#2648=EDGE_LOOP ( 'NONE', ( #21089, #21586, #19739, #6640 ) ) ;
#2652=ADVANCED_FACE ( 'NONE', ( #18612 ), #18798, .T. ) ;
#2653=CARTESIAN_POINT ( 'NONE',  ( -1.048172774974294175, 37.64158596421250991, 26.08722459372745206 ) ) ;
#2660=CARTESIAN_POINT ( 'NONE',  ( -20.57838717382308502, 27.96569011373086866, -10.78122205917010135 ) ) ;
#2661=B_SPLINE_CURVE_WITH_KNOTS ( 'NONE', 3,
 ( #6330, #2700, #258, #26584 ),
 .UNSPECIFIED., .F., .F.,
 ( 4, 4 ),
 ( 1.904175111373004964E-16, 0.001982023823822943748 ),
 .UNSPECIFIED. ) ;
#2668=CARTESIAN_POINT ( 'NONE',  ( -1.619063947482201282, 43.26576862488434472, -16.67502769180576649 ) ) ;
#2672=CARTESIAN_POINT ( 'NONE',  ( -4.473127245936431073, 45.82513704981569447, 18.25038884639822712 ) ) ;
#2673=ORIENTED_EDGE ( 'NONE', *, *, #375, .F. ) ;
#2675=ORIENTED_EDGE ( 'NONE', *, *, #7491, .F. ) ;
#2676=CARTESIAN_POINT ( 'NONE',  ( -1.539760825549692402, -16.63252404870386059, -43.19716078875433851 ) ) ;
#2680=CARTESIAN_POINT ( 'NONE',  ( -1.463510566862831430, 46.14841196428341163, 2.430838777910348192 ) ) ;
#2687=EDGE_CURVE ( 'NONE', #11364, #12467, #10510, .T. ) ;
#2695=CARTESIAN_POINT ( 'NONE',  ( -1.044557008772713180, 15.70482370518816495, -43.01636061108991527 ) ) ;
#2700=CARTESIAN_POINT ( 'NONE',  ( -20.21097721712958872, 29.61001327235739566, 0.3305963429843793433 ) ) ;
#2704=ORIENTED_EDGE ( 'NONE', *, *, #5469, .F. ) ;
#2706=CARTESIAN_POINT ( 'NONE',  ( -1.619063947482201282, 44.80407745103784123, -11.94059994246174838 ) ) ;
#2709=CARTESIAN_POINT ( 'NONE',  ( -1.619063947482197729, 46.30105812165548684, 2.489035965910320503 ) ) ;
#2724=CARTESIAN_POINT ( 'NONE',  ( -25.21435515916025594, 34.29329011225976842, -4.655591116594504086 ) ) ;
#2725=VERTEX_POINT ( 'NONE', #11708 ) ;
#2729=CARTESIAN_POINT ( 'NONE',  ( -55.24728320129491266, -0.009072670231977940022, 0.01137345571547076703 ) ) ;
#2734=VERTEX_POINT ( 'NONE', #20480 ) ;
#2736=CARTESIAN_POINT ( 'NONE',  ( -1.045287976400362417, 43.05558670614268379, 15.59869763335023229 ) ) ;
#2737=CARTESIAN_POINT ( 'NONE',  ( -1.050229599974474404, -0.2556477501656316820, 45.79907399707867199 ) ) ;
#2740=CARTESIAN_POINT ( 'NONE',  ( -55.25297051322618813, -0.01466904165775103838, -0.002853887643042541354 ) ) ;
#2741=CARTESIAN_POINT ( 'NONE',  ( -1.045287976400365970, -36.12803364096568259, 28.14015102489869591 ) ) ;
#2743=ADVANCED_BREP_SHAPE_REPRESENTATION ( '', ( #17192, #27263 ), #2919 ) ;
#2747=CARTESIAN_POINT ( 'NONE',  ( -1.239374126674604337, 42.99367564261279995, -16.50008610789313934 ) ) ;
#2749=CARTESIAN_POINT ( 'NONE',  ( -20.20700224038492010, -10.08426345511570332, 27.82980252387829623 ) ) ;
#2750=CARTESIAN_POINT ( 'NONE',  ( -1.113548883309562587, 44.18588492042589166, -12.28732181966532622 ) ) ;
#2753=CARTESIAN_POINT ( 'NONE',  ( -1.044556982611280604, 44.03203163107544071, 12.57890920527730394 ) ) ;
#2761=B_SPLINE_CURVE_WITH_KNOTS ( 'NONE', 3,
 ( #18895, #25531, #21187, #1612, #25235, #27815, #14568, #23373, #10413, #16447 ),
 .UNSPECIFIED., .F., .F.,
 ( 4, 2, 2, 2, 4 ),
 ( 1.371419323662773916E-18, 0.0003346267210630953859, 0.0006692534421261894708, 0.001003880163189283447, 0.001338506884252376773 ),
 .UNSPECIFIED. ) ;
#2772=DIRECTION ( 'NONE',  ( -0.7637818620346800147, 0.3617919495470713898, -0.5345501402766312804 ) ) ;
#2773=CARTESIAN_POINT ( 'NONE',  ( -2.911734481061399205, -44.38410240830292963, 17.36785190846027049 ) ) ;
#2775=CARTESIAN_POINT ( 'NONE',  ( -20.37983603106073716, -23.16947629293375854, -18.69865230096518616 ) ) ;
#2777=CONICAL_SURFACE ( 'NONE', #24386, 34.60786435723138510, 0.8559913436420825139 ) ;
#2782=CARTESIAN_POINT ( 'NONE',  ( -20.20700224038492721, 23.35150625415659320, -18.19058640100232438 ) ) ;
#2783=CARTESIAN_POINT ( 'NONE',  ( -1.155031165708876317, 16.13806347973058664, 42.97366960678581194 ) ) ;
#2789=CARTESIAN_POINT ( 'NONE',  ( -8.786685647604885574, 6.096987947571466530E-17, -1.524246986892866633E-17 ) ) ;
#2798=B_SPLINE_CURVE_WITH_KNOTS ( 'NONE', 3,
 ( #20190, #13148, #10863, #479, #9271, #26111 ),
 .UNSPECIFIED., .F., .F.,
 ( 4, 2, 4 ),
 ( 3.681866292528241208E-16, 0.003576372551511175675, 0.007152745103021982721 ),
 .UNSPECIFIED. ) ;
#2802=VECTOR ( 'NONE', #11675, 1000.000000000000114 ) ;
#2805=CARTESIAN_POINT ( 'NONE',  ( -9.156249394959713683, 38.89149400288408032, -38.17928057392006025 ) ) ;
#2809=CARTESIAN_POINT ( 'NONE',  ( 180.4657679828686980, -20.00000000000000000, 3.130582043300658722E-16 ) ) ;
#2813=B_SPLINE_CURVE_WITH_KNOTS ( 'NONE', 3,
 ( #8241, #17003, #22026, #11096, #15530, #26481, #19720, #11234, #6786, #2291 ),
 .UNSPECIFIED., .F., .F.,
 ( 4, 2, 2, 2, 4 ),
 ( 2.863532086325413454E-16, 0.0003346187017559052986, 0.0006692374035115242594, 0.001003856105267143329, 0.001338474807022762289 ),
 .UNSPECIFIED. ) ;
#2819=CARTESIAN_POINT ( 'NONE',  ( -4.178947244162622532, 45.38689110596718734, -18.28784278438465805 ) ) ;
#2825=CARTESIAN_POINT ( 'NONE',  ( -55.25297051322618813, -0.002853887643042011396, 0.01466904165775133329 ) ) ;
#2833=ADVANCED_FACE ( 'NONE', ( #17157 ), #10809, .F. ) ;
#2843=EDGE_LOOP ( 'NONE', ( #4922, #18678, #26819, #7289, #15528, #27664, #11564, #7666, #21942, #22075, #9126, #24896, #21469, #13925, #1072, #22571, #19319, #18253, #23211, #27188, #17300, #120, #25770, #2407, #24343, #12123, #17271, #3644, #14897, #27958, #20488, #1000, #26399, #27934, #1162, #26185, #15819, #13439, #18311, #17751, #10530, #5949, #913, #20168, #16926, #18795, #22005, #16529, #6294, #24219, #22346, #27571, #25549, #14558, #2497, #27032, #306, #1973, #9674, #12306, #2552, #11223, #4104, #9613 ) ) ;
#2846=CARTESIAN_POINT ( 'NONE',  ( -1.031422197589716205, 28.14735071801744581, -36.13727897780137965 ) ) ;
#2856=CARTESIAN_POINT ( 'NONE',  ( -1.050229599974473293, 0.2556477501659514262, -45.79907399707867199 ) ) ;
#2865=EDGE_CURVE ( 'NONE', #9063, #4666, #20788, .T. ) ;
#2866=CARTESIAN_POINT ( 'NONE',  ( -1.031422197589716205, -37.93675465142491277, -25.67058493451430934 ) ) ;
#2870=EDGE_LOOP ( 'NONE', ( #10453, #1098, #9974, #27720 ) ) ;
#2874=EDGE_CURVE ( 'NONE', #11368, #3864, #2585, .T. ) ;
#2876=ORIENTED_EDGE ( 'NONE', *, *, #6707, .T. ) ;
#2877=CIRCLE ( 'NONE', #1931, 20.00000000000000000 ) ;
#2879=EDGE_LOOP ( 'NONE', ( #22242, #6218, #11057, #6869 ) ) ;
#2881=CARTESIAN_POINT ( 'NONE',  ( -1.583189561560253589, -29.24830400313191348, -36.01941156322777005 ) ) ;
#2889=ORIENTED_EDGE ( 'NONE', *, *, #13729, .F. ) ;
#2899=DIRECTION ( 'NONE',  ( 0.000000000000000000, -5.223019709708116647E-21, 1.000000000000000000 ) ) ;
#2919=( GEOMETRIC_REPRESENTATION_CONTEXT ( 3 ) GLOBAL_UNCERTAINTY_ASSIGNED_CONTEXT ( ( #3341 ) ) GLOBAL_UNIT_ASSIGNED_CONTEXT ( ( #24443, #17931, #13762 ) ) REPRESENTATION_CONTEXT ( 'NONE', 'WORKASPACE' ) );
#2924=DIRECTION ( 'NONE',  ( 1.000000000000000000, -6.938893903907226837E-18, 1.734723475976806709E-18 ) ) ;
#2926=CARTESIAN_POINT ( 'NONE',  ( -55.24390624410018802, -0.007245494385991098352, -0.007503127514281985981 ) ) ;
#2931=CARTESIAN_POINT ( 'NONE',  ( -23.79223135445719350, -3.207301057648115350, 33.03345552685149755 ) ) ;
#2956=CARTESIAN_POINT ( 'NONE',  ( -1.619063947482197729, -2.489035965910479486, -46.30105812165547974 ) ) ;
#2958=CARTESIAN_POINT ( 'NONE',  ( -22.23342874802667879, -30.68433055777675733, 7.677086057585283285 ) ) ;
#2960=CARTESIAN_POINT ( 'NONE',  ( -1.045287976400365970, 15.59869763335068171, -43.05558670614252037 ) ) ;
#2961=CARTESIAN_POINT ( 'NONE',  ( -55.24300891470648622, 0.009225237711098475957, 0.003362556190414738716 ) ) ;
#2969=ADVANCED_FACE ( 'NONE', ( #27354 ), #22574, .F. ) ;
#2970=CARTESIAN_POINT ( 'NONE',  ( -1.619063947482197729, -46.30105812165550105, -2.489035965909997206 ) ) ;
#2989=CARTESIAN_POINT ( 'NONE',  ( -1.619063947482197729, -38.92136151114925724, -25.20140673341360227 ) ) ;
#2990=DIRECTION ( 'NONE',  ( -1.000000000000000000, 6.938893903907226837E-18, -1.734723475976806709E-18 ) ) ;
#2993=EDGE_CURVE ( 'NONE', #194, #11495, #27523, .T. ) ;
#2995=CARTESIAN_POINT ( 'NONE',  ( -1.619063947482197729, -29.22875152547781852, -35.99532424477369830 ) ) ;
#2997=VERTEX_POINT ( 'NONE', #24792 ) ;
#3003=CARTESIAN_POINT ( 'NONE',  ( -20.90916690077964191, -39.20864005633521998, 5.322316104228396405 ) ) ;
#3004=DIRECTION ( 'NONE',  ( 1.000000000000000000, -6.938893903907226837E-18, 1.734723475976806709E-18 ) ) ;
#3018=CARTESIAN_POINT ( 'NONE',  ( -55.24300891470650754, 0.0003472257464218577502, 0.009812809446892801005 ) ) ;
#3024=ORIENTED_EDGE ( 'NONE', *, *, #6512, .F. ) ;
#3028=CARTESIAN_POINT ( 'NONE',  ( -1.239374126674604337, -44.48112152129355934, -11.92219841463812280 ) ) ;
#3033=CARTESIAN_POINT ( 'NONE',  ( -21.81686047589425215, 16.72402253294313823, -34.70276904128894557 ) ) ;
#3050=CARTESIAN_POINT ( 'NONE',  ( -1.619063947482201282, 44.80407745103784123, -11.94059994246174838 ) ) ;
#3053=ORIENTED_EDGE ( 'NONE', *, *, #21230, .T. ) ;
#3055=ORIENTED_EDGE ( 'NONE', *, *, #15974, .T. ) ;
#3058=CARTESIAN_POINT ( 'NONE',  ( -1.050230346682668126, 43.55729751025884156, 14.15335421912537583 ) ) ;
#3063=CARTESIAN_POINT ( 'NONE',  ( -8.786685647604894456, -23.24040270374358030, 48.22796981442792230 ) ) ;
#3065=CARTESIAN_POINT ( 'NONE',  ( -1.155031165708882757, 2.068616213631583545, 45.85732438018710866 ) ) ;
#3068=CARTESIAN_POINT ( 'NONE',  ( -55.24271866751342941, -0.008433070970613520956, -0.004365563123939561994 ) ) ;
#3075=CARTESIAN_POINT ( 'NONE',  ( -1.583189561560253589, 44.83405390829688741, 11.94859433442854701 ) ) ;
#3085=VERTEX_POINT ( 'NONE', #19288 ) ;
#3087=VERTEX_POINT ( 'NONE', #14546 ) ;
#3095=CARTESIAN_POINT ( 'NONE',  ( -25.21435515916043713, -34.29329011225952684, 4.655591116594705703 ) ) ;
#3120=ORIENTED_EDGE ( 'NONE', *, *, #25561, .F. ) ;
#3123=EDGE_CURVE ( 'NONE', #21594, #15548, #18760, .T. ) ;
#3126=FACE_OUTER_BOUND ( 'NONE', #15413, .T. ) ;
#3132=ORIENTED_EDGE ( 'NONE', *, *, #21352, .F. ) ;
#3133=CARTESIAN_POINT ( 'NONE',  ( -1.048994561756802169, -14.87838255483227101, 43.31369460697990803 ) ) ;
#3134=CARTESIAN_POINT ( 'NONE',  ( -1.155031165708884311, -25.28071330859858534, 38.31525684316168423 ) ) ;
#3135=CARTESIAN_POINT ( 'NONE',  ( -55.25297051322618813, -0.01019003092403448357, -0.01093108995494832154 ) ) ;
#3145=CARTESIAN_POINT ( 'NONE',  ( -55.24271866751342941, 0.001425019990779444407, 0.009388511352200054269 ) ) ;
#3156=EDGE_CURVE ( 'NONE', #5981, #3564, #21091, .T. ) ;
#3160=ADVANCED_FACE ( 'NONE', ( #2003 ), #11722, .F. ) ;
#3165=CARTESIAN_POINT ( 'NONE',  ( -12.94347594948497537, -42.93165645342824632, 23.08810053288727104 ) ) ;
#3166=DIRECTION ( 'NONE',  ( -0.7563875759206388771, -0.4122509917856824191, -0.5078650950445610102 ) ) ;
#3175=CARTESIAN_POINT ( 'NONE',  ( -1.583189561560255143, -46.33203782964464068, -2.490696082059702832 ) ) ;
#3185=CARTESIAN_POINT ( 'NONE',  ( -55.24271866751342941, 0.004365563123939758886, -0.008433070970614048312 ) ) ;
#3188=EDGE_CURVE ( 'NONE', #13254, #25142, #13354, .T. ) ;
#3200=CARTESIAN_POINT ( 'NONE',  ( -25.21435515916043713, -25.00736669481004526, 23.92354251275963861 ) ) ;
#3215=DIRECTION ( 'NONE',  ( 0.7563875759206387661, 0.5490129373055256945, -0.3556158456312918936 ) ) ;
#3225=VERTEX_POINT ( 'NONE', #8926 ) ;
#3226=CARTESIAN_POINT ( 'NONE',  ( -55.24390624410018802, -0.009374879212970498032, 0.004572280736701721943 ) ) ;
#3229=( BOUNDED_SURFACE ( )  B_SPLINE_SURFACE ( 3, 1, ( 
 ( #5124, #11890 ),
 ( #20946, #11754 ),
 ( #14323, #20521 ),
 ( #808, #9590 ) ),
 .UNSPECIFIED., .F., .F., .F. ) 
 B_SPLINE_SURFACE_WITH_KNOTS ( ( 4, 4 ),
 ( 2, 2 ),
 ( 0.000000000000000000, 1.000000000000000000 ),
 ( 0.000000000000000000, 1.000000000000000000 ),
 .UNSPECIFIED. ) 
 GEOMETRIC_REPRESENTATION_ITEM ( )  RATIONAL_B_SPLINE_SURFACE ( (
 ( 1.000000000000000000, 1.000000000000000000),
 ( 0.7789835883360578528, 0.9689951854195403280),
 ( 0.7789835883360578528, 0.9689951854195403280),
 ( 1.000000000000000000, 1.000000000000000000) ) ) 
 REPRESENTATION_ITEM ( '' )  SURFACE ( )  );
#3234=VECTOR ( 'NONE', #6793, 1000.000000000000000 ) ;
#3237=AXIS2_PLACEMENT_3D ( 'NONE', #24708, #27251, #22825 ) ;
#3243=ORIENTED_EDGE ( 'NONE', *, *, #140, .F. ) ;
#3250=ORIENTED_EDGE ( 'NONE', *, *, #14119, .F. ) ;
#3251=EDGE_LOOP ( 'NONE', ( #2472, #2061, #24855, #27914 ) ) ;
#3256=CARTESIAN_POINT ( 'NONE',  ( -22.23342874802667168, -7.677086057585177592, -30.68433055777678931 ) ) ;
#3258=B_SPLINE_CURVE_WITH_KNOTS ( 'NONE', 3,
 ( #12331, #14346, #10345, #25463, #16940, #5875, #27585, #21397, #6165, #6019 ),
 .UNSPECIFIED., .F., .F.,
 ( 4, 2, 2, 2, 4 ),
 ( 2.976962515321448001E-16, 0.0003346187017559152190, 0.0006692374035115327162, 0.001003856105267150267, 0.001338474807022767710 ),
 .UNSPECIFIED. ) ;
#3260=EDGE_CURVE ( 'NONE', #9397, #13041, #12536, .T. ) ;
#3261=CIRCLE ( 'NONE', #25343, 34.60786435723138510 ) ;
#3267=VERTEX_POINT ( 'NONE', #20694 ) ;
#3268=CARTESIAN_POINT ( 'NONE',  ( -20.57838717382308147, 25.16001208503129760, 16.28767523336092893 ) ) ;
#3275=ORIENTED_EDGE ( 'NONE', *, *, #23416, .T. ) ;
#3278=CARTESIAN_POINT ( 'NONE',  ( -55.24728320129491266, -0.005114031043466088153, -0.01362040845703062046 ) ) ;
#3279=CARTESIAN_POINT ( 'NONE',  ( -16.86833981943424376, -30.57013526701942041, -31.95666732167553548 ) ) ;
#3283=DIRECTION ( 'NONE',  ( 1.000000000000000000, -6.938893903907226837E-18, 1.734723475976806709E-18 ) ) ;
#3292=ORIENTED_EDGE ( 'NONE', *, *, #15708, .F. ) ;
#3306=ORIENTED_EDGE ( 'NONE', *, *, #11705, .F. ) ;
#3315=CARTESIAN_POINT ( 'NONE',  ( -55.24300891470648622, -0.009439835024157194193, 0.002702093572889528381 ) ) ;
#3320=CARTESIAN_POINT ( 'NONE',  ( -1.113427685307007087, 42.96952363574832390, -16.03057832159165486 ) ) ;
#3325=CARTESIAN_POINT ( 'NONE',  ( -1.046935749539990468, -45.77872888003169294, -1.275486069320314497 ) ) ;
#3330=EDGE_CURVE ( 'NONE', #7007, #23103, #22855, .T. ) ;
#3341=UNCERTAINTY_MEASURE_WITH_UNIT (LENGTH_MEASURE( 1.000000000000000082E-05 ), #24443, 'distance_accuracy_value', 'NONE');
#3363=CIRCLE ( 'NONE', #13024, 53.53553390275978785 ) ;
#3367=CARTESIAN_POINT ( 'NONE',  ( -1.049817751779889008, 26.50542916749622080, 37.35030165458145746 ) ) ;
#3378=CARTESIAN_POINT ( 'NONE',  ( 180.4657679828686980, -1.252232817320263489E-15, 3.130582043300658722E-16 ) ) ;
#3389=CARTESIAN_POINT ( 'NONE',  ( -1.259920593601967287, 25.19630221849107343, 38.49623866863322519 ) ) ;
#3391=B_SPLINE_CURVE_WITH_KNOTS ( 'NONE', 3,
 ( #9110, #16446, #16005, #5503 ),
 .UNSPECIFIED., .F., .F.,
 ( 4, 4 ),
 ( 1.895855152355442610E-16, 0.001982023823822949386 ),
 .UNSPECIFIED. ) ;
#3400=CARTESIAN_POINT ( 'NONE',  ( -7.078251931573406708, 11.16394717458676311, -50.86685171665416050 ) ) ;
#3405=ORIENTED_EDGE ( 'NONE', *, *, #1306, .F. ) ;
#3411=FACE_OUTER_BOUND ( 'NONE', #23043, .T. ) ;
#3417=CARTESIAN_POINT ( 'NONE',  ( -1.046935749539995131, -15.35946454248365711, 43.14401153755482454 ) ) ;
#3422=EDGE_CURVE ( 'NONE', #4347, #9246, #27623, .T. ) ;
#3423=ORIENTED_EDGE ( 'NONE', *, *, #27690, .T. ) ;
#3428=DIRECTION ( 'NONE',  ( 0.000000000000000000, 1.000000000000000000, 0.000000000000000000 ) ) ;
#3430=CARTESIAN_POINT ( 'NONE',  ( -25.21435515916043713, -30.48034229288627017, 16.39063784838775462 ) ) ;
#3431=ORIENTED_EDGE ( 'NONE', *, *, #21749, .T. ) ;
#3436=CARTESIAN_POINT ( 'NONE',  ( -1.045287976400362417, -43.05558670614257721, -15.59869763335051651 ) ) ;
#3437=CARTESIAN_POINT ( 'NONE',  ( -23.77929240705207192, 4.877832571065432887, 35.93174012244165283 ) ) ;
#3442=VERTEX_POINT ( 'NONE', #1406 ) ;
#3447=DIRECTION ( 'NONE',  ( -0.7637818620346801257, -0.02150485345385289709, -0.6451161201712178883 ) ) ;
#3460=CARTESIAN_POINT ( 'NONE',  ( -1.058473599757830730, 42.99101666105228503, -15.81436910992533029 ) ) ;
#3465=CARTESIAN_POINT ( 'NONE',  ( -8.786685647604887350, 53.04920435127183254, -7.199674155859138835 ) ) ;
#3481=CARTESIAN_POINT ( 'NONE',  ( -8.786685647604896232, 25.35688121747570278, 47.14957014837326454 ) ) ;
#3482=CARTESIAN_POINT ( 'NONE',  ( -20.57838717382308147, -1.611677988432151709, 29.92853265176832878 ) ) ;
#3483=CARTESIAN_POINT ( 'NONE',  ( -12.82751273423876803, -48.09651489336695107, -8.715310691360061313 ) ) ;
#3484=EDGE_CURVE ( 'NONE', #19144, #10778, #13905, .T. ) ;
#3488=CARTESIAN_POINT ( 'NONE',  ( -20.90916690077963125, 18.74041620980169043, -34.84883504600955462 ) ) ;
#3492=CARTESIAN_POINT ( 'NONE',  ( -55.24390624410018802, -0.004572280736702649152, 0.009374879212966917563 ) ) ;
#3500=CARTESIAN_POINT ( 'NONE',  ( -1.031422197589711764, -15.60268798220608488, 43.06660437151322895 ) ) ;
#3507=CARTESIAN_POINT ( 'NONE',  ( -1.239374126674604337, 16.50008610789360119, 42.99367564261261521 ) ) ;
#3508=CARTESIAN_POINT ( 'NONE',  ( -55.24390624410018802, 0.009209468562452933355, 0.004896917417131438528 ) ) ;
#3512=CARTESIAN_POINT ( 'NONE',  ( -20.57838717382308147, 29.92853265176831812, -1.611677988432464126 ) ) ;
#3513=CARTESIAN_POINT ( 'NONE',  ( -20.20700224038492365, 10.08426345511628597, 27.82980252387807951 ) ) ;
#3521=CARTESIAN_POINT ( 'NONE',  ( -20.37983603106074426, -7.753708011498764208, -28.74620395171560006 ) ) ;
#3527=DIRECTION ( 'NONE',  ( 0.000000000000000000, -1.000000000000000000, 0.000000000000000000 ) ) ;
#3534=ORIENTED_EDGE ( 'NONE', *, *, #25339, .F. ) ;
#3537=EDGE_CURVE ( 'NONE', #20148, #5123, #12135, .T. ) ;
#3544=FACE_OUTER_BOUND ( 'NONE', #2531, .T. ) ;
#3546=ORIENTED_EDGE ( 'NONE', *, *, #4636, .F. ) ;
#3548=LINE ( 'NONE', #8174, #23112 ) ;
#3549=CARTESIAN_POINT ( 'NONE',  ( -1.113427685307001314, -45.82016658690749722, 1.967672929087657785 ) ) ;
#3550=FACE_OUTER_BOUND ( 'NONE', #21894, .T. ) ;
#3557=CARTESIAN_POINT ( 'NONE',  ( -8.786685647604890903, -52.67761315067279781, 9.545808661481174795 ) ) ;
#3559=CARTESIAN_POINT ( 'NONE',  ( -25.21435515916043357, 31.17620025257608418, 15.02493970636113474 ) ) ;
#3560=CARTESIAN_POINT ( 'NONE',  ( -10.86508079875781618, 35.35100740321776414, -36.95527278096538737 ) ) ;
#3564=VERTEX_POINT ( 'NONE', #2031 ) ;
#3567=( BOUNDED_SURFACE ( )  B_SPLINE_SURFACE ( 3, 1, ( 
 ( #23878, #4132 ),
 ( #2825, #20519 ),
 ( #17913, #2672 ),
 ( #11603, #22851 ) ),
 .UNSPECIFIED., .F., .F., .F. ) 
 B_SPLINE_SURFACE_WITH_KNOTS ( ( 4, 4 ),
 ( 2, 2 ),
 ( 0.000000000000000000, 1.000000000000000000 ),
 ( 0.000000000000000000, 1.000000000000000000 ),
 .UNSPECIFIED. ) 
 GEOMETRIC_REPRESENTATION_ITEM ( )  RATIONAL_B_SPLINE_SURFACE ( (
 ( 1.000000000000000000, 1.000000000000000000),
 ( 0.7789835883360578528, 0.9689951854195403280),
 ( 0.7789835883360578528, 0.9689951854195403280),
 ( 1.000000000000000000, 1.000000000000000000) ) ) 
 REPRESENTATION_ITEM ( '' )  SURFACE ( )  );
#3570=CARTESIAN_POINT ( 'NONE',  ( -9.156249394959706578, -53.74753343182696597, 9.022661520478342467 ) ) ;
#3584=ADVANCED_FACE ( 'NONE', ( #27956 ), #1102, .F. ) ;
#3595=CARTESIAN_POINT ( 'NONE',  ( -1.323439229708139431, -43.04565903621273293, 16.42345129173381935 ) ) ;
#3597=CARTESIAN_POINT ( 'NONE',  ( -1.048171036023497704, 13.17819047681665090, 43.86077206077055735 ) ) ;
#3600=VERTEX_POINT ( 'NONE', #24217 ) ;
#3616=EDGE_LOOP ( 'NONE', ( #3250, #1865, #667, #27436 ) ) ;
#3619=CARTESIAN_POINT ( 'NONE',  ( -55.25719721206881729, 0.004044147484875269816, -0.01041086141212288138 ) ) ;
#3623=CARTESIAN_POINT ( 'NONE',  ( -55.24271866751342941, -0.006757859501005985571, -0.006671293903669251422 ) ) ;
#3633=CARTESIAN_POINT ( 'NONE',  ( -22.23342874802668234, -16.78332232459660389, -26.81018246605532340 ) ) ;
#3639=ORIENTED_EDGE ( 'NONE', *, *, #26965, .T. ) ;
#3644=ORIENTED_EDGE ( 'NONE', *, *, #15097, .T. ) ;
#3645=EDGE_CURVE ( 'NONE', #27689, #17580, #3363, .T. ) ;
#3650=CARTESIAN_POINT ( 'NONE',  ( -55.24198130335446422, 0.004163123460806185221, -0.008310594958150844397 ) ) ;
#3652=DIRECTION ( 'NONE',  ( 1.000000000000000000, -6.938893903907226837E-18, 1.734723475976806709E-18 ) ) ;
#3654=EDGE_CURVE ( 'NONE', #13961, #14330, #15210, .T. ) ;
#3672=ORIENTED_EDGE ( 'NONE', *, *, #27552, .F. ) ;
#3677=CARTESIAN_POINT ( 'NONE',  ( -1.619063947482197729, 38.92136151114943488, 25.20140673341330739 ) ) ;
#3687=B_SPLINE_CURVE_WITH_KNOTS ( 'NONE', 3,
 ( #1627, #27962, #8259, #6375, #4061, #12834, #1900, #10700, #17297, #602, #15551, #20167, #24223 ),
 .UNSPECIFIED., .F., .F.,
 ( 4, 3, 3, 3, 4 ),
 ( 1.084202172485504434E-17, 0.0007657099931970561164, 0.001531419946797918721, 0.002296279302920154267, 0.003061450627205758099 ),
 .UNSPECIFIED. ) ;
#3688=CARTESIAN_POINT ( 'NONE',  ( -28.41354790283022069, -14.62505768302787779, 18.00456980371915705 ) ) ;
#3690=CARTESIAN_POINT ( 'NONE',  ( -55.25297051322618813, 0.007247191603132027878, 0.01306918787467585205 ) ) ;
#3697=CARTESIAN_POINT ( 'NONE',  ( -20.20612092514784308, -1.137292630518264680, -29.57813644637189299 ) ) ;
#3701=CARTESIAN_POINT ( 'NONE',  ( -23.79248802219730052, -30.42578156345377849, 13.25839849636389367 ) ) ;
#3707=CARTESIAN_POINT ( 'NONE',  ( -20.20997486282892552, 3.551351076220724598E-15, -29.60348406988233450 ) ) ;
#3709=VERTEX_POINT ( 'NONE', #13829 ) ;
#3711=FACE_OUTER_BOUND ( 'NONE', #5895, .T. ) ;
#3715=AXIS2_PLACEMENT_3D ( 'NONE', #25509, #5783, #23633 ) ;
#3728=CIRCLE ( 'NONE', #9706, 34.60786435723138510 ) ;
#3731=CARTESIAN_POINT ( 'NONE',  ( -15.02187109954798316, -40.82269973458204504, 21.95370994985608704 ) ) ;
#3734=CARTESIAN_POINT ( 'NONE',  ( -24.53237795827028123, -14.09663893005605395, -30.86653739599992363 ) ) ;
#3737=CARTESIAN_POINT ( 'NONE',  ( -8.259864102781673267, 38.68084189741949785, -36.24929574824924572 ) ) ;
#3740=ORIENTED_EDGE ( 'NONE', *, *, #25673, .T. ) ;
#3743=ORIENTED_EDGE ( 'NONE', *, *, #1731, .F. ) ;
#3744=CARTESIAN_POINT ( 'NONE',  ( -1.464342487929857661, -43.13914623307948659, 16.57334911911557285 ) ) ;
#3745=CARTESIAN_POINT ( 'NONE',  ( -28.13707043255157103, 22.88591869784691113, -0.7675454997507807908 ) ) ;
#3747=CARTESIAN_POINT ( 'NONE',  ( -1.050230346682689664, 14.15203301556493010, 43.55772679531834513 ) ) ;
#3751=ORIENTED_EDGE ( 'NONE', *, *, #10476, .F. ) ;
#3754=CARTESIAN_POINT ( 'NONE',  ( -1.045287976400386842, 37.92705037016744285, -25.66401692420027203 ) ) ;
#3756=B_SPLINE_CURVE_WITH_KNOTS ( 'NONE', 3,
 ( #19588, #10826, #28356, #26205, #4333, #21897, #20444, #18266, #24924, #726, #11953, #16556, #7510 ),
 .UNSPECIFIED., .F., .F.,
 ( 4, 3, 3, 3, 4 ),
 ( 8.673617379884035472E-18, 0.0007657099931970579596, 0.001531419946797923492, 0.002296279302920159471, 0.003061450627205763737 ),
 .UNSPECIFIED. ) ;
#3774=CARTESIAN_POINT ( 'NONE',  ( -20.57838717382308147, 10.78122205917039977, 27.96569011373074076 ) ) ;
#3779=CARTESIAN_POINT ( 'NONE',  ( -22.34422965417122597, 16.46028608106157876, 34.15536449444073241 ) ) ;
#3784=CARTESIAN_POINT ( 'NONE',  ( -9.156249394959706578, 53.74753343182702991, -9.022661520477960551 ) ) ;
#3794=ORIENTED_EDGE ( 'NONE', *, *, #28165, .F. ) ;
#3809=CARTESIAN_POINT ( 'NONE',  ( -1.048994561756789734, -27.53485040342867407, 36.59609844253159139 ) ) ;
#3811=CARTESIAN_POINT ( 'NONE',  ( -55.24198130335446422, 0.004276389980780370345, -0.008252882783649044540 ) ) ;
#3817=ORIENTED_EDGE ( 'NONE', *, *, #15974, .F. ) ;
#3821=CARTESIAN_POINT ( 'NONE',  ( -7.711401346138400115, -25.75361633141456608, 45.70592430511747040 ) ) ;
#3822=CARTESIAN_POINT ( 'NONE',  ( -55.24340739397742794, 0.0007387096945709508214, 0.01010924026184075245 ) ) ;
#3824=ORIENTED_EDGE ( 'NONE', *, *, #18702, .F. ) ;
#3826=CARTESIAN_POINT ( 'NONE',  ( -8.259864102781671491, -52.06232470801718648, -9.986657004933428894 ) ) ;
#3843=CARTESIAN_POINT ( 'NONE',  ( -20.20612091757424622, 8.058516044219587116, 28.48192249925577357 ) ) ;
#3846=CARTESIAN_POINT ( 'NONE',  ( -28.41354790283022069, -23.16239616762929998, 1.249099604787319295 ) ) ;
#3858=CARTESIAN_POINT ( 'NONE',  ( -55.24340739397742794, 0.006539691034608862037, 0.007744344507854531226 ) ) ;
#3860=DIRECTION ( 'NONE',  ( -6.938893903907226837E-18, -1.000000000000000000, 0.000000000000000000 ) ) ;
#3864=VERTEX_POINT ( 'NONE', #19020 ) ;
#3867=( BOUNDED_SURFACE ( )  B_SPLINE_SURFACE ( 3, 1, ( 
 ( #25907, #19414 ),
 ( #8485, #17248 ),
 ( #21572, #17526 ),
 ( #26447, #24306 ) ),
 .UNSPECIFIED., .F., .F., .F. ) 
 B_SPLINE_SURFACE_WITH_KNOTS ( ( 4, 4 ),
 ( 2, 2 ),
 ( 0.000000000000000000, 1.000000000000000000 ),
 ( 0.000000000000000000, 1.000000000000000000 ),
 .UNSPECIFIED. ) 
 GEOMETRIC_REPRESENTATION_ITEM ( )  RATIONAL_B_SPLINE_SURFACE ( (
 ( 1.000000000000000000, 1.000000000000000000),
 ( 0.7789835883360578528, 0.9689951854195403280),
 ( 0.7789835883360578528, 0.9689951854195403280),
 ( 1.000000000000000000, 1.000000000000000000) ) ) 
 REPRESENTATION_ITEM ( '' )  SURFACE ( )  );
#3876=CARTESIAN_POINT ( 'NONE',  ( -1.048996300304502194, 37.49570739463922564, 26.29666317565261124 ) ) ;
#3883=CARTESIAN_POINT ( 'NONE',  ( -5.986830583229481917, 38.20088153919500229, -33.39046620690925238 ) ) ;
#3890=CARTESIAN_POINT ( 'NONE',  ( -25.21435515916043002, 31.17620025257588523, -15.02493970636157705 ) ) ;
#3891=CARTESIAN_POINT ( 'NONE',  ( -1.050229599974486616, 13.90955673306187990, 43.63650726458048013 ) ) ;
#3894=CARTESIAN_POINT ( 'NONE',  ( -20.20700224038492365, -8.199606986804534259, -28.44216453106533748 ) ) ;
#3895=ORIENTED_EDGE ( 'NONE', *, *, #15644, .F. ) ;
#3896=CARTESIAN_POINT ( 'NONE',  ( -10.86508079875782684, -9.118642906269649018, -50.32133009257454859 ) ) ;
#3904=ORIENTED_EDGE ( 'NONE', *, *, #1189, .T. ) ;
#3907=EDGE_CURVE ( 'NONE', #15665, #14553, #8438, .T. ) ;
#3908=CARTESIAN_POINT ( 'NONE',  ( -55.24390624410018802, 0.004896917417131886954, -0.009209468562452662738 ) ) ;
#3912=EDGE_CURVE ( 'NONE', #21594, #21998, #21022, .T. ) ;
#3913=B_SPLINE_CURVE_WITH_KNOTS ( 'NONE', 3,
 ( #21704, #10779, #21849, #10495, #19264, #28033, #19672, #28443, #4001, #17100 ),
 .UNSPECIFIED., .F., .F.,
 ( 4, 2, 2, 2, 4 ),
 ( 2.947001115474787729E-16, 0.0003346187017559134843, 0.0006692374035115322825, 0.001003856105267151135, 0.001338474807022769879 ),
 .UNSPECIFIED. ) ;
#3918=CARTESIAN_POINT ( 'NONE',  ( -55.24340739397742084, -0.01010924026184288269, -0.0007387096945739216438 ) ) ;
#3921=CARTESIAN_POINT ( 'NONE',  ( -1.050230347699842692, 5.964912479342754695E-15, -45.79907861674080749 ) ) ;
#3929=CARTESIAN_POINT ( 'NONE',  ( -1.044556982611269280, 37.98985389331847529, 25.56989963842161728 ) ) ;
#3934=EDGE_CURVE ( 'NONE', #3864, #6911, #17131, .T. ) ;
#3939=EDGE_CURVE ( 'NONE', #24113, #4452, #19024, .T. ) ;
#3941=CARTESIAN_POINT ( 'NONE',  ( -20.20700224038492721, 0.9908225410482660589, 29.58392382092671724 ) ) ;
#3950=CARTESIAN_POINT ( 'NONE',  ( -10.86508079875780730, -35.35100740321749413, 36.95527278096565027 ) ) ;
#3957=B_SPLINE_CURVE_WITH_KNOTS ( 'NONE', 3,
 ( #12208, #12070, #5882, #12480, #1259, #7767 ),
 .UNSPECIFIED., .F., .F.,
 ( 4, 2, 4 ),
 ( 0.000000000000000000, 0.0004335184443140232147, 0.0008670368886280464295 ),
 .UNSPECIFIED. ) ;
#3958=CARTESIAN_POINT ( 'NONE',  ( -20.38016308990358638, 23.16952666206584155, -18.69911008768343663 ) ) ;
#3972=FACE_OUTER_BOUND ( 'NONE', #25658, .T. ) ;
#3984=CARTESIAN_POINT ( 'NONE',  ( 14.74894986621300141, -1.023413983156985299E-16, 2.558534957892463246E-17 ) ) ;
#3987=ORIENTED_EDGE ( 'NONE', *, *, #3537, .T. ) ;
#3990=CARTESIAN_POINT ( 'NONE',  ( -55.24340739397742794, 0.002421372372456844640, -0.009842732675349010960 ) ) ;
#3993=ORIENTED_EDGE ( 'NONE', *, *, #26831, .F. ) ;
#3998=ORIENTED_EDGE ( 'NONE', *, *, #20899, .T. ) ;
#4001=CARTESIAN_POINT ( 'NONE',  ( -1.539763995773692828, -35.94321074656915016, -29.16712963492449973 ) ) ;
#4004=CARTESIAN_POINT ( 'NONE',  ( -8.786685647604887350, -25.35688121747534751, -47.14957014837345639 ) ) ;
#4005=LINE ( 'NONE', #21710, #16607 ) ;
#4011=B_SPLINE_CURVE_WITH_KNOTS ( 'NONE', 3,
 ( #7728, #12029, #23131, #14166, #7873, #3389, #5256, #22700, #16632, #20937 ),
 .UNSPECIFIED., .F., .F.,
 ( 4, 2, 2, 2, 4 ),
 ( 2.799181570144685938E-16, 0.0003346187017559026423, 0.0006692374035115253436, 0.001003856105267148099, 0.001338474807022770746 ),
 .UNSPECIFIED. ) ;
#4013=CARTESIAN_POINT ( 'NONE',  ( -28.41354790283022069, -1.249099604787238249, -23.16239616762930353 ) ) ;
#4015=CARTESIAN_POINT ( 'NONE',  ( -28.13707043255157103, 12.83104814250481596, 18.96624908365832596 ) ) ;
#4016=CARTESIAN_POINT ( 'NONE',  ( -1.323439229708139875, 28.92147054731892908, 35.86372896917441722 ) ) ;
#4018=VERTEX_POINT ( 'NONE', #11357 ) ;
#4021=CARTESIAN_POINT ( 'NONE',  ( -20.24399999263414784, 28.55700515887720670, -7.930419334766287243 ) ) ;
#4035=ORIENTED_EDGE ( 'NONE', *, *, #26734, .T. ) ;
#4042=ORIENTED_EDGE ( 'NONE', *, *, #1496, .F. ) ;
#4046=DIRECTION ( 'NONE',  ( 0.000000000000000000, -5.223019709708116647E-21, 1.000000000000000000 ) ) ;
#4049=CARTESIAN_POINT ( 'NONE',  ( -1.583189561560255143, 11.94859433442965546, 44.83405390829658188 ) ) ;
#4050=DIRECTION ( 'NONE',  ( 0.7637818620346800147, 0.6068965246771059752, 0.2198041754873819864 ) ) ;
#4051=CARTESIAN_POINT ( 'NONE',  ( -1.048996300304498419, -0.7649764263854993418, -45.79145529752469201 ) ) ;
#4059=ORIENTED_EDGE ( 'NONE', *, *, #14405, .F. ) ;
#4060=CARTESIAN_POINT ( 'NONE',  ( -7.711401346138401003, -52.11446537925908018, 6.030154970217441956 ) ) ;
#4061=CARTESIAN_POINT ( 'NONE',  ( -1.049819825607581691, 45.79654196517400777, -0.5097917909110309953 ) ) ;
#4063=B_SPLINE_CURVE_WITH_KNOTS ( 'NONE', 3,
 ( #19305, #12018, #18491, #1081, #9869, #18638, #16474, #16541, #2615, #15705 ),
 .UNSPECIFIED., .F., .F.,
 ( 4, 2, 2, 2, 4 ),
 ( 2.602085213965210642E-18, 0.0003346267210630942475, 0.0006692534421261858929, 0.001003880163189277593, 0.001338506884252369184 ),
 .UNSPECIFIED. ) ;
#4070=CARTESIAN_POINT ( 'NONE',  ( -55.24271866751342941, 0.009369360294296125852, 0.001545935011630558513 ) ) ;
#4074=CARTESIAN_POINT ( 'NONE',  ( -23.77929240705206482, -4.877832571065186862, -35.93174012244169546 ) ) ;
#4076=B_SPLINE_CURVE_WITH_KNOTS ( 'NONE', 3,
 ( #13503, #2561, #15228, #19984 ),
 .UNSPECIFIED., .F., .F.,
 ( 4, 4 ),
 ( 1.920770561445796063E-16, 0.001982023823822942447 ),
 .UNSPECIFIED. ) ;
#4079=CARTESIAN_POINT ( 'NONE',  ( -8.786685647604894456, -23.24040270374358030, 48.22796981442792230 ) ) ;
#4087=CARTESIAN_POINT ( 'NONE',  ( -10.86508079875786414, -50.32133009257452727, 9.118642906269784021 ) ) ;
#4088=CARTESIAN_POINT ( 'NONE',  ( -1.056502255334265339, -45.80535052436398757, -0.5104472526218417627 ) ) ;
#4092=CARTESIAN_POINT ( 'NONE',  ( -4.162674018437150458, -3.424137510344606117, 48.79210541969628423 ) ) ;
#4101=LINE ( 'NONE', #12866, #18918 ) ;
#4104=ORIENTED_EDGE ( 'NONE', *, *, #24256, .T. ) ;
#4105=CARTESIAN_POINT ( 'NONE',  ( -1.259920593601971950, 2.243284667987781589, -45.95412615877140894 ) ) ;
#4109=CARTESIAN_POINT ( 'NONE',  ( -1.048171036023517688, 15.11933492062827966, -43.23005599774305807 ) ) ;
#4112=B_SPLINE_CURVE_WITH_KNOTS ( 'NONE', 3,
 ( #23666, #21334, #3779, #19178, #1613, #10414, #21475 ),
 .UNSPECIFIED., .F., .F.,
 ( 4, 3, 4 ),
 ( 0.000000000000000000, 0.006568092053401836973, 0.02506242213020846987 ),
 .UNSPECIFIED. ) ;
#4115=DIRECTION ( 'NONE',  ( -0.7637818620346801257, 0.02150485345384840416, 0.6451161201712179993 ) ) ;
#4117=ADVANCED_FACE ( 'NONE', ( #1142 ), #4954, .F. ) ;
#4120=CARTESIAN_POINT ( 'NONE',  ( -20.57838717382308147, 7.715628353034087894, 28.96176188950209962 ) ) ;
#4123=CARTESIAN_POINT ( 'NONE',  ( -25.21435515916025594, 1.749597353048488237E-16, -4.373993382621220594E-17 ) ) ;
#4124=CARTESIAN_POINT ( 'NONE',  ( 14.74894986621300141, 20.00000000000000000, 2.618615375249201539E-15 ) ) ;
#4128=ORIENTED_EDGE ( 'NONE', *, *, #10366, .T. ) ;
#4129=CARTESIAN_POINT ( 'NONE',  ( -1.583189561560255143, -2.490696082059541627, 46.33203782964464068 ) ) ;
#4131=CARTESIAN_POINT ( 'NONE',  ( -5.986830583229376224, -38.20088153919473939, 33.39046620690945844 ) ) ;
#4132=CARTESIAN_POINT ( 'NONE',  ( -9.156249394959706578, 48.78605533024773422, 24.29252099376439489 ) ) ;
#4141=CARTESIAN_POINT ( 'NONE',  ( -22.23342874802668589, -20.31166691703108285, 24.24669006619395617 ) ) ;
#4149=CARTESIAN_POINT ( 'NONE',  ( -8.786685647604890903, -25.35688121747466184, 47.14957014837381166 ) ) ;
#4150=CARTESIAN_POINT ( 'NONE',  ( -20.20700224038492721, -23.35150625415671755, -18.19058640100215385 ) ) ;
#4151=DIRECTION ( 'NONE',  ( -0.7637818620346801257, -0.3965875333584914508, -0.5092696688508597802 ) ) ;
#4165=CARTESIAN_POINT ( 'NONE',  ( -21.41430102051751305, -23.81424706376350287, 19.54553566814611898 ) ) ;
#4166=DIRECTION ( 'NONE',  ( 0.000000000000000000, -1.000000000000000000, 0.000000000000000000 ) ) ;
#4170=ADVANCED_FACE ( 'NONE', ( #12355 ), #2013, .F. ) ;
#4175=ORIENTED_EDGE ( 'NONE', *, *, #18823, .F. ) ;
#4177=B_SPLINE_CURVE_WITH_KNOTS ( 'NONE', 3,
 ( #15732, #24545, #4808, #24112, #13574, #22376, #19763, #2639 ),
 .UNSPECIFIED., .F., .F.,
 ( 4, 2, 2, 4 ),
 ( 0.000000000000000000, 0.002761524886576656283, 0.005523049773153312567, 0.01104609954630661126 ),
 .UNSPECIFIED. ) ;
#4184=AXIS2_PLACEMENT_3D ( 'NONE', #27737, #25725, #16659 ) ;
#4189=CARTESIAN_POINT ( 'NONE',  ( -55.24300891470648622, -0.007734635432132420246, -0.006048736206180634067 ) ) ;
#4190=CARTESIAN_POINT ( 'NONE',  ( -25.21435515916043713, 23.92354251275973809, 25.00736669480994934 ) ) ;
#4191=EDGE_CURVE ( 'NONE', #8983, #14341, #17904, .T. ) ;
#4192=CARTESIAN_POINT ( 'NONE',  ( -25.21435515916043002, 4.655591116594353984, -34.29329011225956947 ) ) ;
#4205=ORIENTED_EDGE ( 'NONE', *, *, #28000, .T. ) ;
#4206=APPLICATION_CONTEXT ( 'automotive_design' ) ;
#4208=ORIENTED_EDGE ( 'NONE', *, *, #10241, .T. ) ;
#4211=CARTESIAN_POINT ( 'NONE',  ( -1.539763995773683503, 2.469814354917492238, -46.22267697748602444 ) ) ;
#4215=ADVANCED_FACE ( 'NONE', ( #19258 ), #1666, .F. ) ;
#4225=FACE_OUTER_BOUND ( 'NONE', #9612, .T. ) ;
#4236=CARTESIAN_POINT ( 'NONE',  ( -4.780792508754325709, -11.68149851467495637, -48.13366140756553335 ) ) ;
#4237=AXIS2_PLACEMENT_3D ( 'NONE', #21930, #26242, #8985 ) ;
#4250=CARTESIAN_POINT ( 'NONE',  ( -1.045287976400351981, 12.68782741917293855, -44.00138577190654132 ) ) ;
#4253=AXIS2_PLACEMENT_3D ( 'NONE', #22795, #5351, #13691 ) ;
#4254=ADVANCED_FACE ( 'NONE', ( #10906 ), #18591, .F. ) ;
#4266=VERTEX_POINT ( 'NONE', #17234 ) ;
#4286=ORIENTED_EDGE ( 'NONE', *, *, #20495, .F. ) ;
#4293=CARTESIAN_POINT ( 'NONE',  ( -8.786685647604890903, 7.199674155858966529, -53.04920435127184675 ) ) ;
#4300=CARTESIAN_POINT ( 'NONE',  ( -8.786685647604898008, 48.22796981442802178, 23.24040270374343464 ) ) ;
#4301=ORIENTED_EDGE ( 'NONE', *, *, #15886, .F. ) ;
#4303=ORIENTED_EDGE ( 'NONE', *, *, #27041, .T. ) ;
#4304=CARTESIAN_POINT ( 'NONE',  ( -20.90916690077944295, 39.20864005633548999, -5.322316104228152156 ) ) ;
#4311=CARTESIAN_POINT ( 'NONE',  ( -18.41936578851711204, -7.566034416291083531, -41.75701384111729197 ) ) ;
#4318=CARTESIAN_POINT ( 'NONE',  ( -1.031422197589716205, -12.69107518035533211, -44.01264471863842687 ) ) ;
#4324=CARTESIAN_POINT ( 'NONE',  ( -22.23342874802668589, 11.82490389046315116, -29.33662284748865900 ) ) ;
#4326=CARTESIAN_POINT ( 'NONE',  ( -7.733045908741340568, 21.80378472388487054, -47.75066202881800592 ) ) ;
#4330=CARTESIAN_POINT ( 'NONE',  ( -6.588769196390752647, 34.04709086065316370, -38.42957692275855663 ) ) ;
#4332=VERTEX_POINT ( 'NONE', #9456 ) ;
#4333=CARTESIAN_POINT ( 'NONE',  ( -1.049819825607587909, -43.71263398674761191, -13.66706894614421408 ) ) ;
#4338=CARTESIAN_POINT ( 'NONE',  ( -1.155031165708885199, -35.88345263711027400, 28.62780465193348789 ) ) ;
#4347=VERTEX_POINT ( 'NONE', #15923 ) ;
#4354=EDGE_CURVE ( 'NONE', #7314, #24805, #6270, .T. ) ;
#4358=CARTESIAN_POINT ( 'NONE',  ( -1.323830074806773283, -46.01435746200692023, -2.318057800980537930 ) ) ;
#4373=CARTESIAN_POINT ( 'NONE',  ( -4.162674018437136247, 11.82104147411627970, 47.46216648493545165 ) ) ;
#4374=CARTESIAN_POINT ( 'NONE',  ( -1.259972190295306715, 35.85909728507050431, -28.82609802125271514 ) ) ;
#4376=CARTESIAN_POINT ( 'NONE',  ( -6.588769196390775740, -4.956336548259307584, 51.10255870850478033 ) ) ;
#4377=CARTESIAN_POINT ( 'NONE',  ( -6.574463467970654840, -25.96726214983158698, 44.27173031830760408 ) ) ;
#4379=CARTESIAN_POINT ( 'NONE',  ( -1.048994561756786625, -36.59609844253148481, -27.53485040342882328 ) ) ;
#4380=EDGE_LOOP ( 'NONE', ( #18765, #21029, #17766, #19437 ) ) ;
#4383=EDGE_CURVE ( 'NONE', #5017, #2997, #28219, .T. ) ;
#4391=CARTESIAN_POINT ( 'NONE',  ( -1.045287976400365970, 1.530335034933814731, -45.76855895860946788 ) ) ;
#4392=CARTESIAN_POINT ( 'NONE',  ( -20.57838717382308147, 18.89542499756500149, -23.26537097894111383 ) ) ;
#4397=DIRECTION ( 'NONE',  ( 0.7563875759206388771, 0.2351350468682867345, -0.6104009704506935252 ) ) ;
#4401=CARTESIAN_POINT ( 'NONE',  ( -7.711401346138398338, 21.83927363365101115, 47.70038152767067885 ) ) ;
#4411=ORIENTED_EDGE ( 'NONE', *, *, #16647, .F. ) ;
#4417=ORIENTED_EDGE ( 'NONE', *, *, #14095, .F. ) ;
#4421=CARTESIAN_POINT ( 'NONE',  ( -7.078251931573400491, 51.82710018979476274, 5.101176922830847893 ) ) ;
#4430=CARTESIAN_POINT ( 'NONE',  ( -15.02187109954782507, 41.75590530176335591, 20.12219089991046772 ) ) ;
#4435=LINE ( 'NONE', #27919, #15562 ) ;
#4449=ORIENTED_EDGE ( 'NONE', *, *, #16387, .T. ) ;
#4452=VERTEX_POINT ( 'NONE', #3677 ) ;
#4456=CARTESIAN_POINT ( 'NONE',  ( -23.79223135445720061, 13.25822371132295352, -30.42557260166815780 ) ) ;
#4458=CARTESIAN_POINT ( 'NONE',  ( -1.619063947482201282, 16.67502769180561728, -43.26576862488438735 ) ) ;
#4461=CARTESIAN_POINT ( 'NONE',  ( -20.20612091757422490, -1.137293889216157705, 29.57813639663779171 ) ) ;
#4462=CARTESIAN_POINT ( 'NONE',  ( -20.57838717382308147, -25.16001208503117326, -16.28767523336112433 ) ) ;
#4463=VERTEX_POINT ( 'NONE', #6146 ) ;
#4466=FACE_OUTER_BOUND ( 'NONE', #10979, .T. ) ;
#4471=CARTESIAN_POINT ( 'NONE',  ( -1.045287976400365970, -36.12803364096568259, 28.14015102489869591 ) ) ;
#4472=CARTESIAN_POINT ( 'NONE',  ( -20.37983603106074426, -24.94323704205426040, 16.25728007463434110 ) ) ;
#4474=CARTESIAN_POINT ( 'NONE',  ( -55.25719721206881729, -0.008651607285659737578, -0.007063345920777289004 ) ) ;
#4479=ORIENTED_EDGE ( 'NONE', *, *, #22480, .F. ) ;
#4481=ADVANCED_FACE ( 'NONE', ( #8030 ), #14756, .T. ) ;
#4485=ORIENTED_EDGE ( 'NONE', *, *, #19473, .T. ) ;
#4491=CARTESIAN_POINT ( 'NONE',  ( -1.031422197589711764, 25.67058493451497725, 37.93675465142443670 ) ) ;
#4492=CARTESIAN_POINT ( 'NONE',  ( -20.90916690077962414, -7.054312691028722604, 38.93431874629081335 ) ) ;
#4493=CARTESIAN_POINT ( 'NONE',  ( -1.046936909428682005, 1.275306677858881743, 45.77873603877004882 ) ) ;
#4501=CARTESIAN_POINT ( 'NONE',  ( -4.473127245936431073, 41.70021447285055416, -26.34600523034553277 ) ) ;
#4502=EDGE_CURVE ( 'NONE', #21576, #22983, #13798, .T. ) ;
#4504=CARTESIAN_POINT ( 'NONE',  ( -1.155001620486265645, 38.31519699443499150, -25.28075036143234300 ) ) ;
#4505=CARTESIAN_POINT ( 'NONE',  ( -20.57838717382308147, 10.78122205917000365, -27.96569011373090063 ) ) ;
#4511=EDGE_CURVE ( 'NONE', #16646, #11340, #16569, .T. ) ;
#4516=CARTESIAN_POINT ( 'NONE',  ( -55.24271866751342941, -0.006757859501009782881, 0.006671293903667897471 ) ) ;
#4519=B_SPLINE_CURVE_WITH_KNOTS ( 'NONE', 3,
 ( #1353, #27264, #10158, #14022, #14596, #9572 ),
 .UNSPECIFIED., .F., .F.,
 ( 4, 2, 4 ),
 ( 0.000000000000000000, 0.003570751334075647834, 0.007141502668151295669 ),
 .UNSPECIFIED. ) ;
#4521=( BOUNDED_SURFACE ( )  B_SPLINE_SURFACE ( 3, 1, ( 
 ( #26616, #20433 ),
 ( #16108, #15969 ),
 ( #22764, #3028 ),
 ( #11806, #15672 ) ),
 .UNSPECIFIED., .F., .F., .F. ) 
 B_SPLINE_SURFACE_WITH_KNOTS ( ( 4, 4 ),
 ( 2, 2 ),
 ( 0.000000000000000000, 1.000000000000000000 ),
 ( 0.000000000000000000, 1.000000000000000000 ),
 .UNSPECIFIED. ) 
 GEOMETRIC_REPRESENTATION_ITEM ( )  RATIONAL_B_SPLINE_SURFACE ( (
 ( 1.000000000000000000, 1.000000000000000000),
 ( 0.9934239774497838349, 0.8357310067453913582),
 ( 0.9934239774497838349, 0.8357310067453913582),
 ( 1.000000000000000000, 1.000000000000000000) ) ) 
 REPRESENTATION_ITEM ( '' )  SURFACE ( )  );
#4528=CARTESIAN_POINT ( 'NONE',  ( 14.74894986621300319, -1.023413983156987147E-16, 2.558534957892467869E-17 ) ) ;
#4531=CARTESIAN_POINT ( 'NONE',  ( -55.24340739397742794, -0.0007387096945702591004, -0.01010924026184094153 ) ) ;
#4533=CARTESIAN_POINT ( 'NONE',  ( -25.21435515916043357, -25.00736669481038987, -23.92354251275926558 ) ) ;
#4537=B_SPLINE_CURVE_WITH_KNOTS ( 'NONE', 3,
 ( #11701, #27073, #24813, #10122, #1325, #3065, #18891, #27663, #13848, #25232 ),
 .UNSPECIFIED., .F., .F.,
 ( 4, 2, 2, 2, 4 ),
 ( 3.104682540412587095E-18, 0.0003346267210630946812, 0.0006692534421261863266, 0.001003880163189277809, 0.001338506884252369401 ),
 .UNSPECIFIED. ) ;
#4545=ADVANCED_FACE ( 'NONE', ( #21657 ), #21517, .F. ) ;
#4550=VERTEX_POINT ( 'NONE', #21516 ) ;
#4557=VERTEX_POINT ( 'NONE', #6407 ) ;
#4564=CARTESIAN_POINT ( 'NONE',  ( -4.178947244162636743, -3.367451375481460563, -48.81675275154075422 ) ) ;
#4568=EDGE_CURVE ( 'NONE', #26336, #5981, #8652, .T. ) ;
#4573=EDGE_CURVE ( 'NONE', #5967, #565, #19632, .T. ) ;
#4578=CARTESIAN_POINT ( 'NONE',  ( -1.323830074806762402, -38.58891736138512840, 25.17121255494518550 ) ) ;
#4591=CARTESIAN_POINT ( 'NONE',  ( -8.786685647604890903, 23.24040270374391426, -48.22796981442777309 ) ) ;
#4593=CARTESIAN_POINT ( 'NONE',  ( -4.473127245936434626, 26.34600523034538355, -41.70021447285062521 ) ) ;
#4599=CARTESIAN_POINT ( 'NONE',  ( -2.265401668238149036, 17.02144111536879123, -43.82493763960390254 ) ) ;
#4601=AXIS2_PLACEMENT_3D ( 'NONE', #15131, #6880, #2111 ) ;
#4605=AXIS2_PLACEMENT_3D ( 'NONE', #8744, #17513, #26297 ) ;
#4609=CARTESIAN_POINT ( 'NONE',  ( -1.619063947482197729, -25.20140673341345305, 38.92136151114934961 ) ) ;
#4614=B_SPLINE_CURVE_WITH_KNOTS ( 'NONE', 3,
 ( #10312, #27844, #16908, #10159, #18493, #25699, #5978, #5394, #7865, #14306 ),
 .UNSPECIFIED., .F., .F.,
 ( 4, 2, 2, 2, 4 ),
 ( 7.961322465290408245E-18, 0.0003346267210630986927, 0.0006692534421261893624, 0.001003880163189280195, 0.001338506884252370919 ),
 .UNSPECIFIED. ) ;
#4623=CARTESIAN_POINT ( 'NONE',  ( -20.38016308990358638, -24.94368798801364662, -16.25718651464972098 ) ) ;
#4629=CARTESIAN_POINT ( 'NONE',  ( -55.25719721206881729, 0.004044147484878754875, 0.01041086141212503938 ) ) ;
#4631=VECTOR ( 'NONE', #2772, 1000.000000000000114 ) ;
#4632=ORIENTED_EDGE ( 'NONE', *, *, #6742, .T. ) ;
#4636=EDGE_CURVE ( 'NONE', #3085, #27654, #14410, .T. ) ;
#4639=CARTESIAN_POINT ( 'NONE',  ( -1.323830074806772616, -25.17121255494502563, -38.58891736138520656 ) ) ;
#4643=AXIS2_PLACEMENT_3D ( 'NONE', #18762, #16313, #9852 ) ;
#4644=CARTESIAN_POINT ( 'NONE',  ( -20.57838717382308502, 28.96176188950218844, -7.715628353033780584 ) ) ;
#4645=CIRCLE ( 'NONE', #20258, 53.53553390275978785 ) ;
#4648=EDGE_CURVE ( 'NONE', #17203, #11340, #13582, .T. ) ;
#4657=CARTESIAN_POINT ( 'NONE',  ( -1.058197053496162887, 36.00048521498994347, 28.32422455455037991 ) ) ;
#4666=VERTEX_POINT ( 'NONE', #23076 ) ;
#4668=CARTESIAN_POINT ( 'NONE',  ( -1.155001620486246550, -16.13799328198394178, 42.97366440495927975 ) ) ;
#4673=CONICAL_SURFACE ( 'NONE', #18457, 28.92774122539760384, 0.7853981625000054922 ) ;
#4676=EDGE_CURVE ( 'NONE', #15665, #11364, #22049, .T. ) ;
#4677=CARTESIAN_POINT ( 'NONE',  ( -10.86508079875779842, -24.22249093393332231, -45.04061326950863275 ) ) ;
#4687=CARTESIAN_POINT ( 'NONE',  ( -1.048996300304493978, 26.29666317565303046, -37.49570739463894142 ) ) ;
#4698=CARTESIAN_POINT ( 'NONE',  ( -21.81686047589424859, -38.17230180719262478, -5.181745222995322919 ) ) ;
#4711=CARTESIAN_POINT ( 'NONE',  ( -4.473127245936431073, 12.17046501147583548, 47.80062405537787384 ) ) ;
#4716=CARTESIAN_POINT ( 'NONE',  ( -18.41936578851709072, 7.566034416291376630, 41.75701384111728487 ) ) ;
#4721=CARTESIAN_POINT ( 'NONE',  ( -12.94347594948480484, 43.91326021875542551, 21.16159467081307710 ) ) ;
#4729=CARTESIAN_POINT ( 'NONE',  ( -25.21435515916043713, -15.02493970636168896, -31.17620025257581062 ) ) ;
#4730=DIRECTION ( 'NONE',  ( -0.7563875759206388771, 0.5490129373055280260, 0.3556158456312881189 ) ) ;
#4734=FACE_OUTER_BOUND ( 'NONE', #3251, .T. ) ;
#4744=ORIENTED_EDGE ( 'NONE', *, *, #261, .T. ) ;
#4757=CONICAL_SURFACE ( 'NONE', #14403, 34.60786435723138510, 0.8559913436420825139 ) ;
#4761=ORIENTED_EDGE ( 'NONE', *, *, #17089, .T. ) ;
#4763=CARTESIAN_POINT ( 'NONE',  ( -1.155031165708874985, 42.97366960678603931, -16.13806347973012834 ) ) ;
#4766=B_SPLINE_CURVE_WITH_KNOTS ( 'NONE', 3,
 ( #17593, #26376, #13561, #6680, #2625, #4644 ),
 .UNSPECIFIED., .F., .F.,
 ( 4, 2, 4 ),
 ( 1.072867218403649326E-17, 0.003576372551510812684, 0.007152745103021620164 ),
 .UNSPECIFIED. ) ;
#4767=CARTESIAN_POINT ( 'NONE',  ( -1.044556982611271279, -12.57890920527746381, 44.03203163107538387 ) ) ;
#4769=FACE_OUTER_BOUND ( 'NONE', #10038, .T. ) ;
#4772=CARTESIAN_POINT ( 'NONE',  ( -20.47566338032522992, -25.06314818626703200, -16.24827550219816885 ) ) ;
#4773=CARTESIAN_POINT ( 'NONE',  ( -1.539763995773683503, 44.72359274866481371, -11.93465967526309868 ) ) ;
#4775=CARTESIAN_POINT ( 'NONE',  ( -1.056502255334265339, 43.40574022158794065, 14.64009593116057317 ) ) ;
#4776=ORIENTED_EDGE ( 'NONE', *, *, #28032, .T. ) ;
#4787=EDGE_CURVE ( 'NONE', #15548, #2734, #14968, .T. ) ;
#4788=B_SPLINE_CURVE_WITH_KNOTS ( 'NONE', 3,
 ( #17381, #10787, #10919, #19411, #21716, #6326, #1987, #4293 ),
 .UNSPECIFIED., .F., .F.,
 ( 4, 2, 2, 4 ),
 ( 2.251264292202123005E-16, 0.002761568181852863766, 0.005523136363705502885, 0.01104627272741079413 ),
 .UNSPECIFIED. ) ;
#4808=CARTESIAN_POINT ( 'NONE',  ( -7.711401346138395674, -35.51061203065555816, -38.61705198405353912 ) ) ;
#4811=EDGE_CURVE ( 'NONE', #14553, #12735, #19814, .T. ) ;
#4820=ORIENTED_EDGE ( 'NONE', *, *, #4568, .F. ) ;
#4821=ADVANCED_FACE ( 'NONE', ( #26470 ), #26302, .F. ) ;
#4823=ADVANCED_FACE ( 'NONE', ( #6491 ), #20596, .F. ) ;
#4828=CARTESIAN_POINT ( 'NONE',  ( -55.24300891470648622, 0.0003472257464250210184, -0.009812809446890590967 ) ) ;
#4829=CARTESIAN_POINT ( 'NONE',  ( -23.79223135445720771, 22.01133905265687929, -24.83942264280410228 ) ) ;
#4830=CARTESIAN_POINT ( 'NONE',  ( -1.048172774974286847, 26.08722459372787128, -37.64158596421222569 ) ) ;
#4832=ORIENTED_EDGE ( 'NONE', *, *, #23459, .T. ) ;
#4835=CARTESIAN_POINT ( 'NONE',  ( -8.259864102781676820, 22.52209142945002895, 47.98931516265572128 ) ) ;
#4848=CARTESIAN_POINT ( 'NONE',  ( -20.38016308990358638, -28.74660391518349911, -7.753479680700832155 ) ) ;
#4857=CARTESIAN_POINT ( 'NONE',  ( -21.81686047589426991, -34.70276904128901663, -16.72402253294301744 ) ) ;
#4864=VERTEX_POINT ( 'NONE', #2724 ) ;
#4867=CARTESIAN_POINT ( 'NONE',  ( -12.82751273423879113, -21.21958768041828947, -44.03362901247000138 ) ) ;
#4869=CARTESIAN_POINT ( 'NONE',  ( -1.046935749539996907, 1.275486069320473481, -45.77872888003166452 ) ) ;
#4897=CARTESIAN_POINT ( 'NONE',  ( -1.583189561560256253, 29.24830400313217282, 36.01941156322756399 ) ) ;
#4902=CARTESIAN_POINT ( 'NONE',  ( -1.323439229708146536, -25.17120723334064891, 38.58845475799796532 ) ) ;
#4907=CARTESIAN_POINT ( 'NONE',  ( -20.47566262905010603, 27.87687924095562408, 10.72601569609867944 ) ) ;
#4908=CARTESIAN_POINT ( 'NONE',  ( -22.23342874802667879, 31.55488258420089664, 2.180636882146622657 ) ) ;
#4909=ADVANCED_FACE ( 'NONE', ( #18250 ), #17145, .T. ) ;
#4913=EDGE_CURVE ( 'NONE', #27654, #8132, #22234, .T. ) ;
#4914=CARTESIAN_POINT ( 'NONE',  ( -1.045287976400365970, 15.59869763335068171, -43.05558670614252037 ) ) ;
#4918=ORIENTED_EDGE ( 'NONE', *, *, #14850, .F. ) ;
#4922=ORIENTED_EDGE ( 'NONE', *, *, #14661, .F. ) ;
#4929=CARTESIAN_POINT ( 'NONE',  ( -20.57838717382308147, -16.28767523336139078, -25.16001208503099917 ) ) ;
#4931=CARTESIAN_POINT ( 'NONE',  ( -12.82751273423878047, -8.715310691359913875, 48.09651489336692975 ) ) ;
#4934=CARTESIAN_POINT ( 'NONE',  ( -6.588769196390761529, -47.06982923582523171, -20.50531526814544847 ) ) ;
#4938=CARTESIAN_POINT ( 'NONE',  ( -28.13707043255157103, -14.07296284901319439, 18.06394523322468615 ) ) ;
#4942=CARTESIAN_POINT ( 'NONE',  ( -1.323439229708132547, 16.42345129173398632, 43.04565903621268319 ) ) ;
#4947=ORIENTED_EDGE ( 'NONE', *, *, #16320, .T. ) ;
#4948=CARTESIAN_POINT ( 'NONE',  ( -12.94347594948482794, -6.555928820868979656, 48.30328466416770539 ) ) ;
#4954=( BOUNDED_SURFACE ( )  B_SPLINE_SURFACE ( 3, 1, ( 
 ( #27470, #13940 ),
 ( #3018, #10364 ),
 ( #17094, #25329 ),
 ( #6042, #25620 ) ),
 .UNSPECIFIED., .F., .F., .F. ) 
 B_SPLINE_SURFACE_WITH_KNOTS ( ( 4, 4 ),
 ( 2, 2 ),
 ( 0.000000000000000000, 1.000000000000000000 ),
 ( 0.000000000000000000, 1.000000000000000000 ),
 .UNSPECIFIED. ) 
 GEOMETRIC_REPRESENTATION_ITEM ( )  RATIONAL_B_SPLINE_SURFACE ( (
 ( 1.000000000000000000, 1.000000000000000000),
 ( 0.9934239774497838349, 0.8357310067453913582),
 ( 0.9934239774497838349, 0.8357310067453913582),
 ( 1.000000000000000000, 1.000000000000000000) ) ) 
 REPRESENTATION_ITEM ( '' )  SURFACE ( )  );
#4956=CYLINDRICAL_SURFACE ( 'NONE', #22091, 37.50000000000001421 ) ;
#4966=ORIENTED_EDGE ( 'NONE', *, *, #7172, .T. ) ;
#4969=CARTESIAN_POINT ( 'NONE',  ( -4.178947244162533714, -41.47292084251643729, -25.96944194166775333 ) ) ;
#4988=ORIENTED_EDGE ( 'NONE', *, *, #22535, .F. ) ;
#4990=EDGE_CURVE ( 'NONE', #2580, #13961, #21418, .T. ) ;
#4997=CARTESIAN_POINT ( 'NONE',  ( -28.13707043255157103, 18.96624908365847162, -12.83104814250460990 ) ) ;
#4998=ORIENTED_EDGE ( 'NONE', *, *, #7972, .T. ) ;
#5001=ORIENTED_EDGE ( 'NONE', *, *, #10476, .T. ) ;
#5003=LINE ( 'NONE', #124, #7520 ) ;
#5004=CARTESIAN_POINT ( 'NONE',  ( -1.113548883309548376, -38.22628252420791739, 25.34012683631596374 ) ) ;
#5005=CARTESIAN_POINT ( 'NONE',  ( -6.588769196390758864, 51.10255870850473769, 4.956336548259831609 ) ) ;
#5013=CARTESIAN_POINT ( 'NONE',  ( -20.57838717382308147, 10.78122205917039977, 27.96569011373074076 ) ) ;
#5014=CARTESIAN_POINT ( 'NONE',  ( -1.619063947482197729, -35.99532424477357750, 29.22875152547795707 ) ) ;
#5017=VERTEX_POINT ( 'NONE', #16959 ) ;
#5028=FACE_OUTER_BOUND ( 'NONE', #8473, .T. ) ;
#5037=LINE ( 'NONE', #9956, #5619 ) ;
#5055=ORIENTED_EDGE ( 'NONE', *, *, #9735, .F. ) ;
#5060=CARTESIAN_POINT ( 'NONE',  ( -7.078251931573406708, -47.71415099571790108, 20.86696228105274997 ) ) ;
#5061=UNCERTAINTY_MEASURE_WITH_UNIT (LENGTH_MEASURE( 1.000000000000000082E-05 ), #10377, 'distance_accuracy_value', 'NONE');
#5062=CARTESIAN_POINT ( 'NONE',  ( -6.588769196390754423, -20.50531526814530636, 47.06982923582530276 ) ) ;
#5070=CARTESIAN_POINT ( 'NONE',  ( -22.34422965417124374, 17.95715691811047776, -33.39267070835825990 ) ) ;
#5073=AXIS2_PLACEMENT_3D ( 'NONE', #10961, #2026, #2449 ) ;
#5080=CARTESIAN_POINT ( 'NONE',  ( -1.031422197589716205, 1.530725436377464499, -45.78027046666444733 ) ) ;
#5081=CARTESIAN_POINT ( 'NONE',  ( -1.045287976400351981, 36.12803364096590997, -28.14015102489844011 ) ) ;
#5094=CIRCLE ( 'NONE', #23516, 34.60786435723138510 ) ;
#5095=CONICAL_SURFACE ( 'NONE', #13367, 34.60786435723138510, 0.8559913436420825139 ) ;
#5102=CARTESIAN_POINT ( 'NONE',  ( -24.53239521893648245, -33.25736993155760501, 6.738460611583118265 ) ) ;
#5104=CARTESIAN_POINT ( 'NONE',  ( -1.239374126674604337, -28.97829083655411964, 35.79060836339844087 ) ) ;
#5105=DIRECTION ( 'NONE',  ( 0.000000000000000000, 5.223019709707975211E-21, -1.000000000000000000 ) ) ;
#5109=EDGE_LOOP ( 'NONE', ( #7373, #24980, #15638, #17759 ) ) ;
#5116=CARTESIAN_POINT ( 'NONE',  ( -2.911734481061406754, 44.38410240830302911, -17.36785190845994720 ) ) ;
#5117=EDGE_LOOP ( 'NONE', ( #3998, #2460, #4128, #10975 ) ) ;
#5121=CARTESIAN_POINT ( 'NONE',  ( -25.21435515916043357, -34.29329011225959079, -4.655591116594231416 ) ) ;
#5123=VERTEX_POINT ( 'NONE', #26080 ) ;
#5124=CARTESIAN_POINT ( 'NONE',  ( -55.25719721206881729, -0.002847566758683717138, -0.01079965405819494247 ) ) ;
#5144=FACE_OUTER_BOUND ( 'NONE', #23949, .T. ) ;
#5148=ORIENTED_EDGE ( 'NONE', *, *, #21292, .F. ) ;
#5152=CARTESIAN_POINT ( 'NONE',  ( -22.34422965417125795, -37.57019010019543970, 5.100074259622997097 ) ) ;
#5154=CARTESIAN_POINT ( 'NONE',  ( -4.780792508754322157, 49.38761389561003767, 3.764354093953751423 ) ) ;
#5156=CARTESIAN_POINT ( 'NONE',  ( -1.044557008772710516, -28.22896138707343994, 36.05793264791374497 ) ) ;
#5157=EDGE_LOOP ( 'NONE', ( #10733, #24610, #5148, #26275 ) ) ;
#5159=CARTESIAN_POINT ( 'NONE',  ( -20.20700224038492721, -23.35150625415645820, 18.19058640100249491 ) ) ;
#5181=CARTESIAN_POINT ( 'NONE',  ( -10.86508079875781974, 22.20099862734820562, -46.07061504567093380 ) ) ;
#5187=CARTESIAN_POINT ( 'NONE',  ( -1.048172774974294619, -36.44231470008696760, 27.73787987941047817 ) ) ;
#5193=CARTESIAN_POINT ( 'NONE',  ( -55.24300891470650754, -0.009439835024158502175, -0.002702093572893477045 ) ) ;
#5194=DIRECTION ( 'NONE',  ( 0.000000000000000000, 5.223019709707975211E-21, -1.000000000000000000 ) ) ;
#5195=B_SPLINE_CURVE_WITH_KNOTS ( 'NONE', 3,
 ( #358, #650, #4829, #9145, #17900, #9439 ),
 .UNSPECIFIED., .F., .F.,
 ( 4, 2, 4 ),
 ( 3.208066105977133993E-16, 0.003576372551511132307, 0.007152745103021943690 ),
 .UNSPECIFIED. ) ;
#5196=CARTESIAN_POINT ( 'NONE',  ( -1.463510566862827655, 44.64091840826493041, -11.94877850058517765 ) ) ;
#5198=FACE_OUTER_BOUND ( 'NONE', #1036, .T. ) ;
#5208=VECTOR ( 'NONE', #17213, 1000.000000000000114 ) ;
#5210=CARTESIAN_POINT ( 'NONE',  ( -55.24390624410018802, 0.009209468562452933355, 0.004896917417131438528 ) ) ;
#5211=AXIS2_PLACEMENT_3D ( 'NONE', #6830, #12145, #23242 ) ;
#5217=ADVANCED_FACE ( 'NONE', ( #5198 ), #14551, .F. ) ;
#5232=CARTESIAN_POINT ( 'NONE',  ( -20.20700224038492365, 23.35150625415685255, 18.19058640100197977 ) ) ;
#5236=ORIENTED_EDGE ( 'NONE', *, *, #1183, .T. ) ;
#5237=ORIENTED_EDGE ( 'NONE', *, *, #8172, .F. ) ;
#5241=CARTESIAN_POINT ( 'NONE',  ( -1.019300379054419725, 12.21833869579464604, -44.15350047934403221 ) ) ;
#5242=( BOUNDED_SURFACE ( )  B_SPLINE_SURFACE ( 3, 1, ( 
 ( #13901, #10177 ),
 ( #14470, #1371 ),
 ( #7443, #3400 ),
 ( #5715, #22710 ) ),
 .UNSPECIFIED., .F., .F., .F. ) 
 B_SPLINE_SURFACE_WITH_KNOTS ( ( 4, 4 ),
 ( 2, 2 ),
 ( 0.000000000000000000, 1.000000000000000000 ),
 ( 0.000000000000000000, 1.000000000000000000 ),
 .UNSPECIFIED. ) 
 GEOMETRIC_REPRESENTATION_ITEM ( )  RATIONAL_B_SPLINE_SURFACE ( (
 ( 1.000000000000000000, 1.000000000000000000),
 ( 0.7789835883360576307, 0.9689951854195403280),
 ( 0.7789835883360576307, 0.9689951854195403280),
 ( 1.000000000000000000, 1.000000000000000000) ) ) 
 REPRESENTATION_ITEM ( '' )  SURFACE ( )  );
#5244=FACE_OUTER_BOUND ( 'NONE', #22142, .T. ) ;
#5246=FACE_OUTER_BOUND ( 'NONE', #5937, .T. ) ;
#5250=CARTESIAN_POINT ( 'NONE',  ( -1.619063947482194177, 29.22875152547808852, 35.99532424477347092 ) ) ;
#5253=ORIENTED_EDGE ( 'NONE', *, *, #17089, .F. ) ;
#5256=CARTESIAN_POINT ( 'NONE',  ( -1.323830074806759960, 25.17121255494532406, 38.58891736138504314 ) ) ;
#5287=CARTESIAN_POINT ( 'NONE',  ( -1.048996300304511298, 43.31387123529979277, -14.87787369922182990 ) ) ;
#5294=FACE_OUTER_BOUND ( 'NONE', #25868, .T. ) ;
#5302=CARTESIAN_POINT ( 'NONE',  ( -1.619063947482197729, -29.22875152547730337, 35.99532424477411041 ) ) ;
#5306=DIRECTION ( 'NONE',  ( 0.000000000000000000, 5.223019709707975211E-21, -1.000000000000000000 ) ) ;
#5307=FACE_OUTER_BOUND ( 'NONE', #18548, .T. ) ;
#5311=CARTESIAN_POINT ( 'NONE',  ( -1.045287976400383290, 12.68782741917383738, 44.00138577190627842 ) ) ;
#5327=FACE_OUTER_BOUND ( 'NONE', #24869, .T. ) ;
#5328=EDGE_CURVE ( 'NONE', #8855, #17826, #9821, .T. ) ;
#5331=CARTESIAN_POINT ( 'NONE',  ( -8.786685647604889127, 9.545808661480615243, -52.67761315067287597 ) ) ;
#5332=CARTESIAN_POINT ( 'NONE',  ( -8.259864102781676820, 6.590267880897663133, 52.60025989855196116 ) ) ;
#5333=CARTESIAN_POINT ( 'NONE',  ( -1.049819825607609225, -45.79654196517396514, 0.5097917909113501844 ) ) ;
#5348=B_SPLINE_CURVE_WITH_KNOTS ( 'NONE', 3,
 ( #4300, #17670, #4721, #4430, #13077, #2258, #13203 ),
 .UNSPECIFIED., .F., .F.,
 ( 4, 3, 4 ),
 ( 0.000000000000000000, 0.009512539173626427882, 0.02506242213020844906 ),
 .UNSPECIFIED. ) ;
#5349=ORIENTED_EDGE ( 'NONE', *, *, #12105, .F. ) ;
#5350=EDGE_LOOP ( 'NONE', ( #5684, #27566, #15298, #10978 ) ) ;
#5351=DIRECTION ( 'NONE',  ( 1.000000000000000000, -6.938893903907226837E-18, 1.734723475976806709E-18 ) ) ;
#5354=CARTESIAN_POINT ( 'NONE',  ( -1.048996300304498419, 43.78665266739856321, 13.42280206896931638 ) ) ;
#5358=CARTESIAN_POINT ( 'NONE',  ( -25.21435515916043713, 25.00736669481056751, 23.92354251275909505 ) ) ;
#5369=B_SPLINE_CURVE_WITH_KNOTS ( 'NONE', 3,
 ( #14910, #13169, #19233, #1804, #10604, #26001 ),
 .UNSPECIFIED., .F., .F.,
 ( 4, 2, 4 ),
 ( 0.000000000000000000, 0.0004335151646191511953, 0.0008670303292383023906 ),
 .UNSPECIFIED. ) ;
#5374=ORIENTED_EDGE ( 'NONE', *, *, #10638, .F. ) ;
#5375=CARTESIAN_POINT ( 'NONE',  ( -55.24340739397742794, -0.003826481709799693914, -0.009386184976285299672 ) ) ;
#5380=VERTEX_POINT ( 'NONE', #1304 ) ;
#5381=VERTEX_POINT ( 'NONE', #3754 ) ;
#5387=CARTESIAN_POINT ( 'NONE',  ( -5.986830583229487246, 49.46736940480273859, 11.27873876172089851 ) ) ;
#5394=CARTESIAN_POINT ( 'NONE',  ( -1.058473599757822292, -44.07591602137166831, -12.47539220917846237 ) ) ;
#5395=CARTESIAN_POINT ( 'NONE',  ( -1.046936909428682894, -15.35929614323696413, -43.14407378092988665 ) ) ;
#5408=CARTESIAN_POINT ( 'NONE',  ( -12.82751273423880711, 35.32125660155448088, -33.78816682541299343 ) ) ;
#5411=ORIENTED_EDGE ( 'NONE', *, *, #11379, .F. ) ;
#5417=EDGE_LOOP ( 'NONE', ( #24930, #14170, #8406, #17374 ) ) ;
#5428=ORIENTED_EDGE ( 'NONE', *, *, #4354, .T. ) ;
#5430=CARTESIAN_POINT ( 'NONE',  ( -55.24300891470648622, -0.003362556190414485880, 0.009225237711097986765 ) ) ;
#5431=CARTESIAN_POINT ( 'NONE',  ( -1.045287976400365970, -45.76855895860942525, 1.530335034934587002 ) ) ;
#5435=EDGE_LOOP ( 'NONE', ( #27746, #3405, #4411, #4175 ) ) ;
#5441=CARTESIAN_POINT ( 'NONE',  ( -8.786685647604890903, 37.00619870957935120, -38.68584556812312059 ) ) ;
#5443=CARTESIAN_POINT ( 'NONE',  ( -1.239374126674604337, -35.79060836339793639, 28.97829083655478399 ) ) ;
#5452=CARTESIAN_POINT ( 'NONE',  ( -1.045287976400365970, -25.66401692419961833, 37.92705037016786918 ) ) ;
#5457=CARTESIAN_POINT ( 'NONE',  ( -1.044557008772713624, 12.57891310333411106, 44.03203053429556491 ) ) ;
#5459=ORIENTED_EDGE ( 'NONE', *, *, #8113, .T. ) ;
#5469=EDGE_CURVE ( 'NONE', #25788, #1690, #25325, .T. ) ;
#5476=CARTESIAN_POINT ( 'NONE',  ( -55.24728320129491266, -0.01214321324516726489, -0.008013189884950557701 ) ) ;
#5480=CARTESIAN_POINT ( 'NONE',  ( -5.986830583229484581, 4.559539818181838733, 50.53158596890435916 ) ) ;
#5484=CARTESIAN_POINT ( 'NONE',  ( -25.21435515916025594, 1.749597353048488237E-16, -4.373993382621220594E-17 ) ) ;
#5491=ORIENTED_EDGE ( 'NONE', *, *, #6775, .T. ) ;
#5494=CARTESIAN_POINT ( 'NONE',  ( -4.473127245936434626, 18.25038884639934977, 45.82513704981523972 ) ) ;
#5503=CARTESIAN_POINT ( 'NONE',  ( -20.20700224038492721, 23.35150625415659320, -18.19058640100232438 ) ) ;
#5512=CARTESIAN_POINT ( 'NONE',  ( -1.539763995773681504, 35.94321074656937753, 29.16712963492422617 ) ) ;
#5519=CARTESIAN_POINT ( 'NONE',  ( -1.019300379054419947, -16.06793277091962935, 42.90269154183443590 ) ) ;
#5520=ORIENTED_EDGE ( 'NONE', *, *, #14428, .T. ) ;
#5521=VECTOR ( 'NONE', #13446, 1000.000000000000114 ) ;
#5529=CARTESIAN_POINT ( 'NONE',  ( -18.41936578851711204, 41.75701384111740566, -7.566034416290932541 ) ) ;
#5530=ADVANCED_FACE ( 'NONE', ( #11214, #2419 ), #11793, .T. ) ;
#5531=FACE_OUTER_BOUND ( 'NONE', #11258, .T. ) ;
#5532=CARTESIAN_POINT ( 'NONE',  ( -12.94347594948481195, -43.91326021875530472, -21.16159467081338263 ) ) ;
#5541=AXIS2_PLACEMENT_3D ( 'NONE', #10677, #19446, #28215 ) ;
#5543=VERTEX_POINT ( 'NONE', #6907 ) ;
#5557=CARTESIAN_POINT ( 'NONE',  ( -1.323439229708138987, -28.92147054731866263, -35.86372896917463038 ) ) ;
#5564=ORIENTED_EDGE ( 'NONE', *, *, #15708, .T. ) ;
#5571=CARTESIAN_POINT ( 'NONE',  ( -1.019300379054419725, 38.21680004809200426, 25.26451264419602438 ) ) ;
#5576=CARTESIAN_POINT ( 'NONE',  ( -1.050231094221201644, -13.91061116148162391, 43.63617436699752261 ) ) ;
#5578=CARTESIAN_POINT ( 'NONE',  ( -1.050230346682676785, 43.55772679531850855, -14.15203301556446647 ) ) ;
#5583=EDGE_LOOP ( 'NONE', ( #2105, #17997, #7562, #2166 ) ) ;
#5597=CARTESIAN_POINT ( 'NONE',  ( -20.57838717382308147, -23.26537097894090778, 18.89542499756525729 ) ) ;
#5602=CARTESIAN_POINT ( 'NONE',  ( -8.786685647604896232, 52.67761315067299677, 9.545808661480061019 ) ) ;
#5619=VECTOR ( 'NONE', #866, 1000.000000000000114 ) ;
#5637=B_SPLINE_CURVE_WITH_KNOTS ( 'NONE', 3,
 ( #15422, #11129, #19901, #186, #8975, #22212, #9109 ),
 .UNSPECIFIED., .F., .F.,
 ( 4, 3, 4 ),
 ( 0.000000000000000000, 0.006568092053401801411, 0.02506242213020845253 ),
 .UNSPECIFIED. ) ;
#5648=EDGE_CURVE ( 'NONE', #26826, #13127, #11765, .T. ) ;
#5657=CARTESIAN_POINT ( 'NONE',  ( -20.20700224038492721, -24.51628800869035274, 16.58740185276737122 ) ) ;
#5660=CARTESIAN_POINT ( 'NONE',  ( -22.34422965417124729, -37.30738373203622871, -6.759368364654178230 ) ) ;
#5670=DIRECTION ( 'NONE',  ( -0.7637818620346801257, 0.6451161201712179993, -0.02150485345385064542 ) ) ;
#5677=DIRECTION ( 'NONE',  ( 1.000000000000000000, -6.938893903907226837E-18, 1.734723475976806709E-18 ) ) ;
#5680=AXIS2_PLACEMENT_3D ( 'NONE', #24713, #22543, #5105 ) ;
#5684=ORIENTED_EDGE ( 'NONE', *, *, #4636, .T. ) ;
#5686=CARTESIAN_POINT ( 'NONE',  ( -1.045287976400351981, 43.05558670614237116, -15.59869763335110449 ) ) ;
#5693=CARTESIAN_POINT ( 'NONE',  ( -20.20700224038492010, 8.199606986804733211, 28.44216453106527709 ) ) ;
#5710=CARTESIAN_POINT ( 'NONE',  ( -55.24728320129491266, 0.003868537197317211632, -0.01402509393918151964 ) ) ;
#5711=B_SPLINE_CURVE_WITH_KNOTS ( 'NONE', 3,
 ( #2709, #20119, #9484, #9054, #5154, #5005, #22590, #27012 ),
 .UNSPECIFIED., .F., .F.,
 ( 4, 2, 2, 4 ),
 ( 2.324173423859648542E-16, 0.002761568181852869838, 0.005523136363705506355, 0.01104627272741078026 ),
 .UNSPECIFIED. ) ;
#5713=ORIENTED_EDGE ( 'NONE', *, *, #10070, .T. ) ;
#5715=CARTESIAN_POINT ( 'NONE',  ( -55.25719721206881729, -0.007063345920780820901, -0.008651607285661404648 ) ) ;
#5716=CARTESIAN_POINT ( 'NONE',  ( -5.986830583229487246, -49.46736940480267464, -11.27873876172122181 ) ) ;
#5717=EDGE_CURVE ( 'NONE', #8132, #23403, #26536, .T. ) ;
#5722=ORIENTED_EDGE ( 'NONE', *, *, #18217, .T. ) ;
#5724=PRODUCT_CONTEXT ( 'NONE', #16352, 'mechanical' ) ;
#5725=DIRECTION ( 'NONE',  ( 0.7563875759206388771, -0.4122509917856713724, 0.5078650950445698919 ) ) ;
#5734=CARTESIAN_POINT ( 'NONE',  ( -55.24340739397742794, -0.002421372372456151618, 0.009842732675348802793 ) ) ;
#5735=CARTESIAN_POINT ( 'NONE',  ( -1.539760825549685519, -46.22267384399379608, 2.469813586483570855 ) ) ;
#5736=LINE ( 'NONE', #10201, #19803 ) ;
#5744=CARTESIAN_POINT ( 'NONE',  ( -24.53239521893653929, 30.86654523348686041, 14.09666242510765954 ) ) ;
#5750=CARTESIAN_POINT ( 'NONE',  ( -8.786685647604890903, 47.14957014837354876, -25.35688121747519119 ) ) ;
#5768=CARTESIAN_POINT ( 'NONE',  ( -2.904412668506679118, 46.12477647685274462, -11.97478724945526629 ) ) ;
#5781=EDGE_CURVE ( 'NONE', #14642, #10702, #16254, .T. ) ;
#5783=DIRECTION ( 'NONE',  ( 1.000000000000000000, -6.938893903907226837E-18, 1.734723475976806709E-18 ) ) ;
#5787=ORIENTED_EDGE ( 'NONE', *, *, #6742, .F. ) ;
#5791=ADVANCED_FACE ( 'NONE', ( #20050 ), #16746, .F. ) ;
#5796=ORIENTED_EDGE ( 'NONE', *, *, #22369, .T. ) ;
#5799=B_SPLINE_CURVE_WITH_KNOTS ( 'NONE', 3,
 ( #11681, #22785, #9524, #13828, #20452, #26920, #18275, #26779 ),
 .UNSPECIFIED., .F., .F.,
 ( 4, 2, 2, 4 ),
 ( 2.189053321159284187E-16, 0.002761568181852863766, 0.005523136363705508090, 0.01104627272741077852 ),
 .UNSPECIFIED. ) ;
#5804=CARTESIAN_POINT ( 'NONE',  ( -20.57838717382308147, 10.78122205917039977, 27.96569011373074076 ) ) ;
#5822=( BOUNDED_SURFACE ( )  B_SPLINE_SURFACE ( 3, 1, ( 
 ( #6783, #26340 ),
 ( #15527, #15106 ),
 ( #8792, #284 ),
 ( #10821, #23925 ) ),
 .UNSPECIFIED., .F., .F., .F. ) 
 B_SPLINE_SURFACE_WITH_KNOTS ( ( 4, 4 ),
 ( 2, 2 ),
 ( 0.000000000000000000, 1.000000000000000000 ),
 ( 0.000000000000000000, 1.000000000000000000 ),
 .UNSPECIFIED. ) 
 GEOMETRIC_REPRESENTATION_ITEM ( )  RATIONAL_B_SPLINE_SURFACE ( (
 ( 1.000000000000000000, 1.000000000000000000),
 ( 0.9934239774497837239, 0.8357310067453919133),
 ( 0.9934239774497837239, 0.8357310067453919133),
 ( 1.000000000000000000, 1.000000000000000000) ) ) 
 REPRESENTATION_ITEM ( '' )  SURFACE ( )  );
#5826=CARTESIAN_POINT ( 'NONE',  ( -1.048994561756802391, 26.29622118251734619, 37.49601524795380669 ) ) ;
#5831=ADVANCED_FACE ( 'NONE', ( #15882 ), #25576, .F. ) ;
#5838=DIRECTION ( 'NONE',  ( 1.000000000000000000, -6.938893903907226837E-18, 1.734723475976806709E-18 ) ) ;
#5839=ORIENTED_EDGE ( 'NONE', *, *, #20303, .T. ) ;
#5844=DIRECTION ( 'NONE',  ( 1.000000000000000000, -6.938893903907226837E-18, 1.734723475976806709E-18 ) ) ;
#5846=ORIENTED_EDGE ( 'NONE', *, *, #19326, .T. ) ;
#5856=VECTOR ( 'NONE', #27005, 999.9999999999998863 ) ;
#5864=CARTESIAN_POINT ( 'NONE',  ( -25.21435515916025594, 34.29329011225976132, 4.655591116594488099 ) ) ;
#5866=CARTESIAN_POINT ( 'NONE',  ( -4.473127245936434626, -37.94261489385694830, 31.51789735524234004 ) ) ;
#5872=CARTESIAN_POINT ( 'NONE',  ( -1.046936909428679563, -12.93351869073243243, 43.93225665392628088 ) ) ;
#5874=CARTESIAN_POINT ( 'NONE',  ( -1.049819825607605672, 43.39756533277881800, -14.63675055554395321 ) ) ;
#5875=CARTESIAN_POINT ( 'NONE',  ( -1.259920593601976169, 28.82601305773653877, -35.85909937955931071 ) ) ;
#5877=ORIENTED_EDGE ( 'NONE', *, *, #13220, .T. ) ;
#5882=CARTESIAN_POINT ( 'NONE',  ( -20.24419206586954090, 27.76448493191444200, -10.37009329716774708 ) ) ;
#5886=CARTESIAN_POINT ( 'NONE',  ( -1.463510566862834539, 38.76366072687779507, -25.15876608740827436 ) ) ;
#5888=CARTESIAN_POINT ( 'NONE',  ( -25.21435515916043002, 30.48034229288640162, -16.39063784838753790 ) ) ;
#5891=DIRECTION ( 'NONE',  ( 0.000000000000000000, 5.223019709708233256E-21, -1.000000000000000000 ) ) ;
#5893=CARTESIAN_POINT ( 'NONE',  ( -4.780792508754322157, 42.16805077400959334, -25.98388465890095489 ) ) ;
#5895=EDGE_LOOP ( 'NONE', ( #10327, #26498, #10115, #5966 ) ) ;
#5901=B_SPLINE_CURVE_WITH_KNOTS ( 'NONE', 3,
 ( #23455, #28162, #12903, #1558, #26292, #17504, #2101, #14650 ),
 .UNSPECIFIED., .F., .F.,
 ( 4, 2, 2, 4 ),
 ( 0.000000000000000000, 0.002761524886576655416, 0.005523049773153310832, 0.01104609954630661646 ),
 .UNSPECIFIED. ) ;
#5911=CARTESIAN_POINT ( 'NONE',  ( -8.786685647604890903, 52.67761315067286176, -9.545808661480789326 ) ) ;
#5918=ORIENTED_EDGE ( 'NONE', *, *, #16381, .F. ) ;
#5923=CARTESIAN_POINT ( 'NONE',  ( -1.619063947482197729, 11.94059994246222622, 44.80407745103770623 ) ) ;
#5925=FACE_OUTER_BOUND ( 'NONE', #2870, .T. ) ;
#5937=EDGE_LOOP ( 'NONE', ( #21485, #14636, #20600, #20711 ) ) ;
#5946=EDGE_CURVE ( 'NONE', #710, #23103, #14279, .T. ) ;
#5949=ORIENTED_EDGE ( 'NONE', *, *, #3654, .T. ) ;
#5962=CARTESIAN_POINT ( 'NONE',  ( -1.464342487929850778, 38.76467504336618219, 25.15873223207648834 ) ) ;
#5966=ORIENTED_EDGE ( 'NONE', *, *, #24256, .F. ) ;
#5967=VERTEX_POINT ( 'NONE', #23523 ) ;
#5976=( BOUNDED_SURFACE ( )  B_SPLINE_SURFACE ( 3, 1, ( 
 ( #20233, #22125 ),
 ( #17924, #7021 ),
 ( #15482, #244 ),
 ( #17791, #9029 ) ),
 .UNSPECIFIED., .F., .F., .F. ) 
 B_SPLINE_SURFACE_WITH_KNOTS ( ( 4, 4 ),
 ( 2, 2 ),
 ( 0.000000000000000000, 1.000000000000000000 ),
 ( 0.000000000000000000, 1.000000000000000000 ),
 .UNSPECIFIED. ) 
 GEOMETRIC_REPRESENTATION_ITEM ( )  RATIONAL_B_SPLINE_SURFACE ( (
 ( 1.000000000000000000, 1.000000000000000000),
 ( 0.7789835883360576307, 0.9689951854195403280),
 ( 0.7789835883360576307, 0.9689951854195403280),
 ( 1.000000000000000000, 1.000000000000000000) ) ) 
 REPRESENTATION_ITEM ( '' )  SURFACE ( )  );
#5978=CARTESIAN_POINT ( 'NONE',  ( -1.113427685306998649, -44.18561238466747199, -12.28784199929917875 ) ) ;
#5981=VERTEX_POINT ( 'NONE', #10137 ) ;
#5984=FACE_OUTER_BOUND ( 'NONE', #8722, .T. ) ;
#5991=B_SPLINE_CURVE_WITH_KNOTS ( 'NONE', 3,
 ( #2956, #7570, #14301, #16326, #16624, #25121, #14156, #18773, #18924, #22978 ),
 .UNSPECIFIED., .F., .F.,
 ( 4, 2, 2, 2, 4 ),
 ( 1.563658610346375379E-18, 0.0003346267210630954943, 0.0006692534421261893624, 0.001003880163189283230, 0.001338506884252377207 ),
 .UNSPECIFIED. ) ;
#6008=CIRCLE ( 'NONE', #3237, 53.53553390275978785 ) ;
#6017=CARTESIAN_POINT ( 'NONE',  ( -20.20700224038492010, -16.58740185276728241, -24.51628800869040958 ) ) ;
#6019=CARTESIAN_POINT ( 'NONE',  ( -1.619063947482197729, 29.22875152547757338, -35.99532424477389725 ) ) ;
#6020=( BOUNDED_SURFACE ( )  B_SPLINE_SURFACE ( 3, 1, ( 
 ( #1227, #20515 ),
 ( #801, #944 ),
 ( #10026, #18788 ),
 ( #9583, #7586 ) ),
 .UNSPECIFIED., .F., .F., .F. ) 
 B_SPLINE_SURFACE_WITH_KNOTS ( ( 4, 4 ),
 ( 2, 2 ),
 ( 0.000000000000000000, 1.000000000000000000 ),
 ( 0.000000000000000000, 1.000000000000000000 ),
 .UNSPECIFIED. ) 
 GEOMETRIC_REPRESENTATION_ITEM ( )  RATIONAL_B_SPLINE_SURFACE ( (
 ( 1.000000000000000000, 1.000000000000000000),
 ( 0.7789835883360578528, 0.9689951854195403280),
 ( 0.7789835883360578528, 0.9689951854195403280),
 ( 1.000000000000000000, 1.000000000000000000) ) ) 
 REPRESENTATION_ITEM ( '' )  SURFACE ( )  );
#6025=CARTESIAN_POINT ( 'NONE',  ( -2.265401668238153032, -45.46007138824032978, 11.98901689611089516 ) ) ;
#6032=FACE_OUTER_BOUND ( 'NONE', #5350, .T. ) ;
#6035=DIRECTION ( 'NONE',  ( -1.000000000000000000, 6.938893903907226837E-18, -1.734723475976806709E-18 ) ) ;
#6036=VECTOR ( 'NONE', #21582, 1000.000000000000000 ) ;
#6038=CARTESIAN_POINT ( 'NONE',  ( -55.25297051322618813, -0.006313402748431807057, -0.01354497706059512932 ) ) ;
#6041=ORIENTED_EDGE ( 'NONE', *, *, #19615, .T. ) ;
#6042=CARTESIAN_POINT ( 'NONE',  ( -55.24390624410018802, -0.001811362924362171613, 0.01027195578988007209 ) ) ;
#6043=EDGE_CURVE ( 'NONE', #15548, #21594, #12255, .T. ) ;
#6057=B_SPLINE_CURVE_WITH_KNOTS ( 'NONE', 3,
 ( #25324, #1271, #16836, #1412, #5893, #12492, #13318, #21694 ),
 .UNSPECIFIED., .F., .F.,
 ( 4, 2, 2, 4 ),
 ( 2.211348276820754320E-16, 0.002761568181852864200, 0.005523136363705507222, 0.01104627272741079066 ),
 .UNSPECIFIED. ) ;
#6077=DIRECTION ( 'NONE',  ( 0.000000000000000000, 5.223019709708233256E-21, -1.000000000000000000 ) ) ;
#6083=CARTESIAN_POINT ( 'NONE',  ( -4.178947244162637631, -11.88256963646706410, 47.46809051147732816 ) ) ;
#6086=B_SPLINE_CURVE_WITH_KNOTS ( 'NONE', 3,
 ( #16915, #3950, #13007, #12580, #23970, #25704, #17041 ),
 .UNSPECIFIED., .F., .F.,
 ( 4, 3, 4 ),
 ( 0.000000000000000000, 0.009512539173626361963, 0.02506242213020844212 ),
 .UNSPECIFIED. ) ;
#6116=CIRCLE ( 'NONE', #4253, 37.50000000000001421 ) ;
#6124=CARTESIAN_POINT ( 'NONE',  ( -20.90916690077966322, -5.322316104228261402, -39.20864005633521998 ) ) ;
#6130=ORIENTED_EDGE ( 'NONE', *, *, #19817, .T. ) ;
#6142=CARTESIAN_POINT ( 'NONE',  ( -20.20700224038492721, 23.35150625415659320, -18.19058640100232438 ) ) ;
#6146=CARTESIAN_POINT ( 'NONE',  ( -20.20700224038492721, 0.9908225410482660589, 29.58392382092671724 ) ) ;
#6148=ORIENTED_EDGE ( 'NONE', *, *, #19817, .F. ) ;
#6151=CARTESIAN_POINT ( 'NONE',  ( -1.044557008772713402, 1.643388457097889166, -45.76404748504490527 ) ) ;
#6164=CARTESIAN_POINT ( 'NONE',  ( -25.21435515916043357, -34.29329011225959079, -4.655591116594231416 ) ) ;
#6165=CARTESIAN_POINT ( 'NONE',  ( -1.539763995773680838, 29.16712963492463473, -35.94321074656906490 ) ) ;
#6170=CARTESIAN_POINT ( 'NONE',  ( -28.13707043255157103, -14.07296284901345551, -18.06394523322448009 ) ) ;
#6176=CARTESIAN_POINT ( 'NONE',  ( -1.619063947482201282, 38.92136151114908671, -25.20140673341387227 ) ) ;
#6190=CARTESIAN_POINT ( 'NONE',  ( -15.02187109954783040, -21.95370994985601953, -40.82269973458228662 ) ) ;
#6191=AXIS2_PLACEMENT_3D ( 'NONE', #23562, #17052, #25850 ) ;
#6192=CARTESIAN_POINT ( 'NONE',  ( -25.21435515916025594, 1.749597353048488237E-16, -4.373993382621220594E-17 ) ) ;
#6198=EDGE_CURVE ( 'NONE', #2342, #10460, #25124, .T. ) ;
#6201=CARTESIAN_POINT ( 'NONE',  ( -20.20612092514785019, -10.22177639105880864, -27.77903665678161360 ) ) ;
#6204=EDGE_LOOP ( 'NONE', ( #28020, #4417, #4966, #23605 ) ) ;
#6212=CARTESIAN_POINT ( 'NONE',  ( -9.156249394959713683, -53.74753343182709386, -9.022661520477562647 ) ) ;
#6218=ORIENTED_EDGE ( 'NONE', *, *, #253, .F. ) ;
#6222=ORIENTED_EDGE ( 'NONE', *, *, #16319, .F. ) ;
#6225=CARTESIAN_POINT ( 'NONE',  ( -1.239374126674604337, 25.08410696974242882, -38.61989855450947573 ) ) ;
#6244=CARTESIAN_POINT ( 'NONE',  ( -1.619063947482197729, 44.80407745103800465, 11.94059994246113021 ) ) ;
#6248=CARTESIAN_POINT ( 'NONE',  ( -1.045287976400362417, -15.59869763335038506, 43.05558670614261985 ) ) ;
#6250=CARTESIAN_POINT ( 'NONE',  ( -1.019300379054419725, -42.90269154183418010, 16.06793277092037187 ) ) ;
#6253=CARTESIAN_POINT ( 'NONE',  ( -20.20997486282892552, 1.395963739018065216E-16, 29.60348406988233450 ) ) ;
#6259=LINE ( 'NONE', #19338, #23520 ) ;
#6264=B_SPLINE_CURVE_WITH_KNOTS ( 'NONE', 3,
 ( #21063, #15932, #20927, #1351, #24743, #10011 ),
 .UNSPECIFIED., .F., .F.,
 ( 4, 2, 4 ),
 ( 4.653458371169123007E-16, 0.003576372551511270217, 0.007152745103022075529 ),
 .UNSPECIFIED. ) ;
#6265=CARTESIAN_POINT ( 'NONE',  ( -15.02187109954788191, -45.60876405941872491, 8.264310930412850809 ) ) ;
#6269=CARTESIAN_POINT ( 'NONE',  ( -2.911734481061396540, 12.03743348210780439, -46.11606034418766598 ) ) ;
#6270=B_SPLINE_CURVE_WITH_KNOTS ( 'NONE', 3,
 ( #7444, #2676, #22560, #20226, #25144, #27135, #20383, #524, #9318, #16062 ),
 .UNSPECIFIED., .F., .F.,
 ( 4, 2, 2, 2, 4 ),
 ( 4.210279659405072890E-18, 0.0003346267210630970664, 0.0006692534421261899045, 0.001003880163189282580, 0.001338506884252375472 ),
 .UNSPECIFIED. ) ;
#6271=CARTESIAN_POINT ( 'NONE',  ( -5.986830583229487246, -26.01297580803291964, 43.56094206392985058 ) ) ;
#6273=VERTEX_POINT ( 'NONE', #26034 ) ;
#6275=CARTESIAN_POINT ( 'NONE',  ( -1.259920593601966177, -16.33409644610522449, 43.01175804832023886 ) ) ;
#6287=CARTESIAN_POINT ( 'NONE',  ( -55.24271866751342941, -0.008433070970613520956, 0.004365563123935277227 ) ) ;
#6288=CARTESIAN_POINT ( 'NONE',  ( -1.050229599974477734, 14.39582765040461254, -43.47850826583058392 ) ) ;
#6294=ORIENTED_EDGE ( 'NONE', *, *, #10006, .F. ) ;
#6299=CARTESIAN_POINT ( 'NONE',  ( -8.786685647604896232, 25.35688121747570278, 47.14957014837326454 ) ) ;
#6308=ORIENTED_EDGE ( 'NONE', *, *, #6675, .F. ) ;
#6310=B_SPLINE_CURVE_WITH_KNOTS ( 'NONE', 3,
 ( #4929, #9406, #22502, #13133, #15561, #24235 ),
 .UNSPECIFIED., .F., .F.,
 ( 4, 2, 4 ),
 ( 0.000000000000000000, 0.0004335151646191525506, 0.0008670303292383051011 ),
 .UNSPECIFIED. ) ;
#6314=ADVANCED_FACE ( 'NONE', ( #6882 ), #9584, .F. ) ;
#6320=DIRECTION ( 'NONE',  ( 0.7563875759206388771, -0.5078650950445684487, -0.4122509917856733708 ) ) ;
#6322=DIRECTION ( 'NONE',  ( -0.7563875759206388771, 0.6104009704506910827, -0.2351350468682930628 ) ) ;
#6323=CARTESIAN_POINT ( 'NONE',  ( -20.90916690077961704, -28.59207721780126477, 27.35210456531406109 ) ) ;
#6325=CARTESIAN_POINT ( 'NONE',  ( -8.786685647604855376, -7.199674155859337787, -53.04920435127184675 ) ) ;
#6326=CARTESIAN_POINT ( 'NONE',  ( -6.588769196390762417, 4.956336548259653974, -51.10255870850470217 ) ) ;
#6329=CARTESIAN_POINT ( 'NONE',  ( -20.21097721712959938, -23.76068428613694294, -17.67178718142850258 ) ) ;
#6330=CARTESIAN_POINT ( 'NONE',  ( -20.20700224038492721, 29.58392382092673500, 0.9908225410479544193 ) ) ;
#6333=VERTEX_POINT ( 'NONE', #26718 ) ;
#6347=ORIENTED_EDGE ( 'NONE', *, *, #24073, .F. ) ;
#6348=EDGE_CURVE ( 'NONE', #15181, #25910, #21699, .T. ) ;
#6357=ORIENTED_EDGE ( 'NONE', *, *, #17672, .F. ) ;
#6365=CARTESIAN_POINT ( 'NONE',  ( -55.24300891470648622, -0.009812809446890113918, -0.0003472257464246985225 ) ) ;
#6374=CARTESIAN_POINT ( 'NONE',  ( -1.619063947482194177, -46.30105812165547974, 2.489035965910640247 ) ) ;
#6375=CARTESIAN_POINT ( 'NONE',  ( -1.048996300304487095, 45.79145529752471333, -0.7649764263853394697 ) ) ;
#6380=EDGE_CURVE ( 'NONE', #6789, #5543, #6264, .T. ) ;
#6383=CARTESIAN_POINT ( 'NONE',  ( -21.41427618760458529, 25.94789270595506991, -16.60878262545428541 ) ) ;
#6389=B_SPLINE_CURVE_WITH_KNOTS ( 'NONE', 3,
 ( #7149, #9299, #4830, #4687, #11587, #26972, #20363, #22693, #24845, #651, #13595, #13458, #24271 ),
 .UNSPECIFIED., .F., .F.,
 ( 4, 3, 3, 3, 4 ),
 ( 9.813077866773594792E-18, 0.0007657099931970658743, 0.001531419946797928045, 0.002296279302920156435, 0.003061450627205745956 ),
 .UNSPECIFIED. ) ;
#6394=CARTESIAN_POINT ( 'NONE',  ( -1.031422197589716205, -12.69107518035472637, 44.01264471863859740 ) ) ;
#6395=CARTESIAN_POINT ( 'NONE',  ( -18.41936578851712980, -41.75701384111727776, 7.566034416291218534 ) ) ;
#6398=CARTESIAN_POINT ( 'NONE',  ( -1.619063947482201282, 35.99532424477380488, -29.22875152547769062 ) ) ;
#6400=CARTESIAN_POINT ( 'NONE',  ( -4.178947244162631414, 11.88256963646738740, -47.46809051147726422 ) ) ;
#6403=CARTESIAN_POINT ( 'NONE',  ( -20.24419206586951603, 23.20105925399726132, -18.44224248888881590 ) ) ;
#6407=CARTESIAN_POINT ( 'NONE',  ( -20.20700224038492721, 27.82980252387819675, -10.08426345511598932 ) ) ;
#6410=EDGE_CURVE ( 'NONE', #5380, #11657, #8296, .T. ) ;
#6413=DIRECTION ( 'NONE',  ( 0.000000000000000000, 5.223019709708233256E-21, -1.000000000000000000 ) ) ;
#6414=ADVANCED_FACE ( 'NONE', ( #14592 ), #13607, .F. ) ;
#6415=VERTEX_POINT ( 'NONE', #28242 ) ;
#6416=CARTESIAN_POINT ( 'NONE',  ( -1.463510566862832318, 2.430838777910187432, -46.14841196428340453 ) ) ;
#6418=CARTESIAN_POINT ( 'NONE',  ( -1.155031165708884755, -38.31525684316158475, -25.28071330859873100 ) ) ;
#6428=CARTESIAN_POINT ( 'NONE',  ( -1.583189561560255143, -11.94859433442934282, -44.83405390829668136 ) ) ;
#6433=CARTESIAN_POINT ( 'NONE',  ( -55.24271866751342941, -0.008433070970613524425, -0.004365563123939557658 ) ) ;
#6435=CARTESIAN_POINT ( 'NONE',  ( -15.02187109954787303, 21.95370994985631086, 40.82269973458213030 ) ) ;
#6441=CARTESIAN_POINT ( 'NONE',  ( -21.41430102051744200, -30.75470819672111134, 1.815007301162295805 ) ) ;
#6451=ORIENTED_EDGE ( 'NONE', *, *, #16120, .T. ) ;
#6454=CARTESIAN_POINT ( 'NONE',  ( -28.13707043255157103, 12.83104814250454062, -18.96624908365850359 ) ) ;
#6457=CARTESIAN_POINT ( 'NONE',  ( -1.045287976400383290, 36.12803364096649972, 28.14015102489766917 ) ) ;
#6458=CARTESIAN_POINT ( 'NONE',  ( -1.019300379054419725, 44.15350047934416011, 12.21833869579419130 ) ) ;
#6461=CARTESIAN_POINT ( 'NONE',  ( -21.41430102051752016, 16.60879216503635547, -25.94791611261620545 ) ) ;
#6463=CARTESIAN_POINT ( 'NONE',  ( -23.77929240705207192, -17.17389748746940370, 31.93650644494359270 ) ) ;
#6475=CARTESIAN_POINT ( 'NONE',  ( -28.41354790283022069, -19.47297445639558333, -12.60397206714825558 ) ) ;
#6478=VERTEX_POINT ( 'NONE', #17306 ) ;
#6479=CARTESIAN_POINT ( 'NONE',  ( -1.056502255334265339, -43.40574022158784118, -14.64009593116085739 ) ) ;
#6491=FACE_OUTER_BOUND ( 'NONE', #12810, .T. ) ;
#6492=EDGE_LOOP ( 'NONE', ( #13124, #11810, #472, #14123 ) ) ;
#6500=AXIS2_PLACEMENT_3D ( 'NONE', #18540, #3283, #18233 ) ;
#6501=CARTESIAN_POINT ( 'NONE',  ( -1.619063947482197729, 29.22875152547757338, -35.99532424477389725 ) ) ;
#6508=CARTESIAN_POINT ( 'NONE',  ( -1.058473599757826067, -35.99997772736190882, 28.32531354681322711 ) ) ;
#6512=EDGE_CURVE ( 'NONE', #27747, #18251, #12573, .T. ) ;
#6514=CARTESIAN_POINT ( 'NONE',  ( -28.13707043255157103, 7.802116958609309094, 21.52861750560930432 ) ) ;
#6515=CARTESIAN_POINT ( 'NONE',  ( -1.583189561560256253, -38.94740041318311796, -25.21827308671218404 ) ) ;
#6520=CARTESIAN_POINT ( 'NONE',  ( -5.986830583229487246, -50.53158596890438758, 4.559539818181663762 ) ) ;
#6530=CARTESIAN_POINT ( 'NONE',  ( -20.90916690077962770, 27.35210456531415346, 28.59207721780114753 ) ) ;
#6540=CARTESIAN_POINT ( 'NONE',  ( -24.53239521893651087, 6.738460611583212412, 33.25736993155762633 ) ) ;
#6542=CARTESIAN_POINT ( 'NONE',  ( -1.619063947482197729, 11.94059994246222622, 44.80407745103770623 ) ) ;
#6546=CARTESIAN_POINT ( 'NONE',  ( -1.619063947482201282, 11.94059994246159384, -44.80407745103787676 ) ) ;
#6551=CARTESIAN_POINT ( 'NONE',  ( -1.539763995773680172, -16.63252574783015092, 43.19716353142347742 ) ) ;
#6552=VECTOR ( 'NONE', #10338, 999.9999999999998863 ) ;
#6553=ORIENTED_EDGE ( 'NONE', *, *, #27078, .F. ) ;
#6554=CARTESIAN_POINT ( 'NONE',  ( -1.619063947482197729, -11.94059994246129008, 44.80407745103795492 ) ) ;
#6557=( BOUNDED_SURFACE ( )  B_SPLINE_SURFACE ( 3, 1, ( 
 ( #4070, #1350 ),
 ( #1907, #6250 ),
 ( #15003, #27544 ),
 ( #3508, #7855 ) ),
 .UNSPECIFIED., .F., .F., .F. ) 
 B_SPLINE_SURFACE_WITH_KNOTS ( ( 4, 4 ),
 ( 2, 2 ),
 ( 0.000000000000000000, 1.000000000000000000 ),
 ( 0.000000000000000000, 1.000000000000000000 ),
 .UNSPECIFIED. ) 
 GEOMETRIC_REPRESENTATION_ITEM ( )  RATIONAL_B_SPLINE_SURFACE ( (
 ( 1.000000000000000000, 1.000000000000000000),
 ( 0.9934239774497838349, 0.8357310067453913582),
 ( 0.9934239774497838349, 0.8357310067453913582),
 ( 1.000000000000000000, 1.000000000000000000) ) ) 
 REPRESENTATION_ITEM ( '' )  SURFACE ( )  );
#6560=EDGE_LOOP ( 'NONE', ( #25256, #19297, #5796, #3024 ) ) ;
#6564=CARTESIAN_POINT ( 'NONE',  ( -1.045287976400365970, -37.92705037016778391, -25.66401692419976399 ) ) ;
#6571=LINE ( 'NONE', #24136, #18966 ) ;
#6572=CARTESIAN_POINT ( 'NONE',  ( -25.21435515916025594, 1.749597353048488237E-16, -4.373993382621220594E-17 ) ) ;
#6587=CARTESIAN_POINT ( 'NONE',  ( -1.239374126674604337, -38.61989855450920572, 25.08410696974284448 ) ) ;
#6611=CARTESIAN_POINT ( 'NONE',  ( -1.619063947482201282, -16.67502769180592992, -43.26576862488428077 ) ) ;
#6612=ORIENTED_EDGE ( 'NONE', *, *, #6410, .T. ) ;
#6613=ADVANCED_FACE ( 'NONE', ( #17736 ), #17642, .F. ) ;
#6616=LINE ( 'NONE', #26590, #23966 ) ;
#6617=CARTESIAN_POINT ( 'NONE',  ( -12.82751273423882843, 44.03362901247002981, -21.21958768041810117 ) ) ;
#6619=LINE ( 'NONE', #13350, #6036 ) ;
#6622=EDGE_LOOP ( 'NONE', ( #12454, #17141, #8309, #22019 ) ) ;
#6623=DIRECTION ( 'NONE',  ( 0.7637818620346800147, -0.6201872550346642088, 0.1788995134688892708 ) ) ;
#6629=CARTESIAN_POINT ( 'NONE',  ( -7.711401346138435642, 45.70592430511758408, 25.75361633141439199 ) ) ;
#6638=CARTESIAN_POINT ( 'NONE',  ( -1.019300379054419725, 25.26451264419644716, -38.21680004809172004 ) ) ;
#6640=ORIENTED_EDGE ( 'NONE', *, *, #23679, .F. ) ;
#6644=ORIENTED_EDGE ( 'NONE', *, *, #1602, .T. ) ;
#6645=CARTESIAN_POINT ( 'NONE',  ( -1.464342487929864323, -25.15873223207664466, 38.76467504336611114 ) ) ;
#6648=VERTEX_POINT ( 'NONE', #8832 ) ;
#6649=CARTESIAN_POINT ( 'NONE',  ( -4.473127245936434626, 41.70021447285091654, 26.34600523034491815 ) ) ;
#6650=CARTESIAN_POINT ( 'NONE',  ( -55.24300891470650754, -0.005486913146700035313, 0.008142823778062066586 ) ) ;
#6654=CARTESIAN_POINT ( 'NONE',  ( -1.619063947482194177, 25.20140673341374438, -38.92136151114915066 ) ) ;
#6658=CARTESIAN_POINT ( 'NONE',  ( -7.733045908741322805, -45.70676731105703539, 25.81515396910911875 ) ) ;
#6659=FACE_OUTER_BOUND ( 'NONE', #25396, .T. ) ;
#6667=ORIENTED_EDGE ( 'NONE', *, *, #20530, .F. ) ;
#6675=EDGE_CURVE ( 'NONE', #11364, #13776, #3728, .T. ) ;
#6678=CARTESIAN_POINT ( 'NONE',  ( -1.619063947482197729, 29.22875152547757338, -35.99532424477389725 ) ) ;
#6680=CARTESIAN_POINT ( 'NONE',  ( -22.23342874802668234, 30.68433055777684970, -7.677086057585063017 ) ) ;
#6691=CARTESIAN_POINT ( 'NONE',  ( -1.058197053496169548, 38.06270006878853707, -25.48582931365482906 ) ) ;
#6698=CARTESIAN_POINT ( 'NONE',  ( -20.20700224038492721, -29.58392382092672790, 0.9908225410481621420 ) ) ;
#6702=VERTEX_POINT ( 'NONE', #1048 ) ;
#6703=CARTESIAN_POINT ( 'NONE',  ( -16.86833981943424021, -39.83928801320577406, 19.19877306373892978 ) ) ;
#6707=EDGE_CURVE ( 'NONE', #23277, #6842, #4537, .T. ) ;
#6708=ORIENTED_EDGE ( 'NONE', *, *, #28376, .T. ) ;
#6719=CARTESIAN_POINT ( 'NONE',  ( -8.786685647604896232, 23.24040270374459993, 48.22796981442743913 ) ) ;
#6721=DIRECTION ( 'NONE',  ( 0.000000000000000000, 5.223019709708233256E-21, -1.000000000000000000 ) ) ;
#6724=VERTEX_POINT ( 'NONE', #11841 ) ;
#6737=FACE_OUTER_BOUND ( 'NONE', #21262, .T. ) ;
#6738=EDGE_CURVE ( 'NONE', #6333, #9063, #24809, .T. ) ;
#6739=CARTESIAN_POINT ( 'NONE',  ( -1.045287976400362417, -1.530335034934427574, -45.76855895860943235 ) ) ;
#6742=EDGE_CURVE ( 'NONE', #11657, #5017, #1784, .T. ) ;
#6746=CARTESIAN_POINT ( 'NONE',  ( -20.57838717382308147, 16.28767523336121315, -25.16001208503110931 ) ) ;
#6750=CARTESIAN_POINT ( 'NONE',  ( -8.786685647604885574, 6.096987947571466530E-17, -1.524246986892866633E-17 ) ) ;
#6767=CARTESIAN_POINT ( 'NONE',  ( -55.24728320129491266, 0.0006547948648740692726, 0.01453410071985259712 ) ) ;
#6775=EDGE_CURVE ( 'NONE', #21576, #17227, #9680, .T. ) ;
#6783=CARTESIAN_POINT ( 'NONE',  ( -55.24390624410018802, 0.01027195578987812573, -0.001811362924359468263 ) ) ;
#6786=CARTESIAN_POINT ( 'NONE',  ( -1.539763995773685057, -11.93465967526326921, -44.72359274866478529 ) ) ;
#6787=ORIENTED_EDGE ( 'NONE', *, *, #7491, .T. ) ;
#6788=CARTESIAN_POINT ( 'NONE',  ( -1.539760825549689516, -25.17088484262114179, 38.84664866728805066 ) ) ;
#6789=VERTEX_POINT ( 'NONE', #5358 ) ;
#6790=CARTESIAN_POINT ( 'NONE',  ( -23.79248802219722236, 32.40806545715341258, 7.157555990716568672 ) ) ;
#6793=DIRECTION ( 'NONE',  ( -0.7563875759206388771, 0.5078650950445624535, -0.4122509917856805317 ) ) ;
#6797=CARTESIAN_POINT ( 'NONE',  ( -20.24399999263415140, -24.70869149526192032, 16.36687688782885530 ) ) ;
#6806=CARTESIAN_POINT ( 'NONE',  ( -1.583189561560253589, -25.21827308671203127, 38.94740041318322454 ) ) ;
#6810=ORIENTED_EDGE ( 'NONE', *, *, #460, .T. ) ;
#6816=CARTESIAN_POINT ( 'NONE',  ( -1.045287976400383290, 28.14015102489806708, -36.12803364096618708 ) ) ;
#6819=CARTESIAN_POINT ( 'NONE',  ( -25.21435515916025594, 1.749597353048488237E-16, -4.373993382621220594E-17 ) ) ;
#6822=CARTESIAN_POINT ( 'NONE',  ( -2.265401668238147259, -43.82493763960398070, -17.02144111536863136 ) ) ;
#6823=CARTESIAN_POINT ( 'NONE',  ( -25.21435515916043713, -31.17620025257598471, -15.02493970636134613 ) ) ;
#6830=CARTESIAN_POINT ( 'NONE',  ( -25.21435515916025594, 1.749597353048488237E-16, -4.373993382621220594E-17 ) ) ;
#6842=VERTEX_POINT ( 'NONE', #16743 ) ;
#6851=CARTESIAN_POINT ( 'NONE',  ( -20.57838717382308147, -28.96176188950213870, 7.715628353033985753 ) ) ;
#6852=CARTESIAN_POINT ( 'NONE',  ( -55.24728320129491266, -0.005114031043468280843, 0.01362040845703383143 ) ) ;
#6854=CARTESIAN_POINT ( 'NONE',  ( -20.57838717382308147, -23.26537097894118133, -18.89542499756491978 ) ) ;
#6859=CARTESIAN_POINT ( 'NONE',  ( -7.733045908741323693, -52.15131830128827062, -5.980865481987962085 ) ) ;
#6869=ORIENTED_EDGE ( 'NONE', *, *, #8376, .F. ) ;
#6872=EDGE_LOOP ( 'NONE', ( #145, #10101, #13017, #1009 ) ) ;
#6873=CARTESIAN_POINT ( 'NONE',  ( -28.41354790283022069, 22.41474081378008876, 5.969609727607788408 ) ) ;
#6875=CARTESIAN_POINT ( 'NONE',  ( -20.57838717382308147, -23.26537097894090778, 18.89542499756525729 ) ) ;
#6878=CARTESIAN_POINT ( 'NONE',  ( 0.000000000000000000, 0.000000000000000000, 0.000000000000000000 ) ) ;
#6880=DIRECTION ( 'NONE',  ( 1.000000000000000000, -6.938893903907226837E-18, 1.734723475976806709E-18 ) ) ;
#6882=FACE_OUTER_BOUND ( 'NONE', #27682, .T. ) ;
#6885=ORIENTED_EDGE ( 'NONE', *, *, #8610, .F. ) ;
#6897=CARTESIAN_POINT ( 'NONE',  ( -20.20700224038492010, -18.19058640100240254, -23.35150625415651859 ) ) ;
#6898=CARTESIAN_POINT ( 'NONE',  ( -25.21435515916025594, 1.749597353048488237E-16, -4.373993382621220594E-17 ) ) ;
#6903=EDGE_CURVE ( 'NONE', #17826, #26336, #2813, .T. ) ;
#6907=CARTESIAN_POINT ( 'NONE',  ( -20.57838717382308147, 23.26537097894132344, 18.89542499756474569 ) ) ;
#6911=VERTEX_POINT ( 'NONE', #17977 ) ;
#6916=CARTESIAN_POINT ( 'NONE',  ( -55.24198130335446422, 0.004276389980776598189, 0.008252882783650057619 ) ) ;
#6919=ORIENTED_EDGE ( 'NONE', *, *, #9809, .F. ) ;
#6921=LINE ( 'NONE', #9642, #27139 ) ;
#6924=VERTEX_POINT ( 'NONE', #4462 ) ;
#6926=CARTESIAN_POINT ( 'NONE',  ( -4.780792508754329262, 45.80716263181262349, 18.84172549606824987 ) ) ;
#6927=VERTEX_POINT ( 'NONE', #3 ) ;
#6929=DIRECTION ( 'NONE',  ( -1.000000000000000000, 6.938893903907226837E-18, -1.734723475976806709E-18 ) ) ;
#6932=EDGE_CURVE ( 'NONE', #9180, #10634, #27904, .T. ) ;
#6933=CARTESIAN_POINT ( 'NONE',  ( -1.323439229708146536, 43.04565903621286083, -16.42345129173351381 ) ) ;
#6945=CARTESIAN_POINT ( 'NONE',  ( -1.031422197589716205, -1.530725436377144755, 45.78027046666445443 ) ) ;
#6946=DIRECTION ( 'NONE',  ( 0.000000000000000000, 5.223019709708233256E-21, -1.000000000000000000 ) ) ;
#6948=EDGE_CURVE ( 'NONE', #21998, #18571, #16220, .T. ) ;
#6950=ORIENTED_EDGE ( 'NONE', *, *, #24485, .T. ) ;
#6951=CARTESIAN_POINT ( 'NONE',  ( -24.53237795827026346, 24.99972053297905461, -22.94498492516348520 ) ) ;
#6953=CARTESIAN_POINT ( 'NONE',  ( -55.25297051322618813, 0.01093108995495213273, 0.01019003092403696770 ) ) ;
#6955=VECTOR ( 'NONE', #18957, 1000.000000000000114 ) ;
#6959=CARTESIAN_POINT ( 'NONE',  ( -20.20612092514785019, 29.57813644637190365, -1.137292630518160097 ) ) ;
#6970=CARTESIAN_POINT ( 'NONE',  ( -1.539760825549692180, 11.93465943778514315, -44.72358953107736568 ) ) ;
#6984=ORIENTED_EDGE ( 'NONE', *, *, #4913, .F. ) ;
#6997=CARTESIAN_POINT ( 'NONE',  ( -21.81686047589426281, -18.24499610240063419, -33.92779429964196680 ) ) ;
#6999=CARTESIAN_POINT ( 'NONE',  ( -2.911734481061388102, 46.11606034418780098, 12.03743348210733011 ) ) ;
#7000=CARTESIAN_POINT ( 'NONE',  ( -20.57838717382308147, 1.611677988432361097, -29.92853265176831812 ) ) ;
#7001=CARTESIAN_POINT ( 'NONE',  ( -1.031422197589711764, -25.67058493451469303, -37.93675465142463565 ) ) ;
#7007=VERTEX_POINT ( 'NONE', #18132 ) ;
#7011=CARTESIAN_POINT ( 'NONE',  ( -8.786685647604890903, -53.04920435127188938, -7.199674155858766689 ) ) ;
#7012=CARTESIAN_POINT ( 'NONE',  ( -20.20700224038492010, -8.199606986804138131, 28.44216453106544762 ) ) ;
#7021=CARTESIAN_POINT ( 'NONE',  ( -4.473127245936434626, -12.17046501147483895, 47.80062405537812964 ) ) ;
#7023=( BOUNDED_SURFACE ( )  B_SPLINE_SURFACE ( 3, 1, ( 
 ( #770, #27091 ),
 ( #27240, #14004 ),
 ( #14138, #26820 ),
 ( #16021, #20342 ) ),
 .UNSPECIFIED., .F., .F., .F. ) 
 B_SPLINE_SURFACE_WITH_KNOTS ( ( 4, 4 ),
 ( 2, 2 ),
 ( 0.000000000000000000, 1.000000000000000000 ),
 ( 0.000000000000000000, 1.000000000000000000 ),
 .UNSPECIFIED. ) 
 GEOMETRIC_REPRESENTATION_ITEM ( )  RATIONAL_B_SPLINE_SURFACE ( (
 ( 1.000000000000000000, 1.000000000000000000),
 ( 0.9934239774497837239, 0.8357310067453919133),
 ( 0.9934239774497837239, 0.8357310067453919133),
 ( 1.000000000000000000, 1.000000000000000000) ) ) 
 REPRESENTATION_ITEM ( '' )  SURFACE ( )  );
#7032=CARTESIAN_POINT ( 'NONE',  ( -20.20700224038492010, -0.9908225410476447781, 29.58392382092673500 ) ) ;
#7041=CARTESIAN_POINT ( 'NONE',  ( -1.019300379054419947, -44.15350047934390432, 12.21833869579511500 ) ) ;
#7042=CARTESIAN_POINT ( 'NONE',  ( -1.031422197589716205, -44.01264471863839134, 12.69107518035547955 ) ) ;
#7049=DIRECTION ( 'NONE',  ( 0.000000000000000000, 5.223019709707975211E-21, -1.000000000000000000 ) ) ;
#7050=DIRECTION ( 'NONE',  ( 0.7563875759206388771, 0.6104009704506959677, 0.2351350468682803785 ) ) ;
#7058=CARTESIAN_POINT ( 'NONE',  ( -55.24271866751342941, 0.004256484107793641683, 0.008488649505346114801 ) ) ;
#7079=CARTESIAN_POINT ( 'NONE',  ( -1.050230347699842692, 1.897926697972695375E-16, 45.79907861674080749 ) ) ;
#7086=CARTESIAN_POINT ( 'NONE',  ( -1.048996300304495310, 14.87787369922229708, 43.31387123529964356 ) ) ;
#7089=B_SPLINE_CURVE_WITH_KNOTS ( 'NONE', 3,
 ( #18138, #9228, #17986, #7086, #15846, #24653, #3747, #3891, #1167, #16421, #3597, #27493, #12107 ),
 .UNSPECIFIED., .F., .F.,
 ( 4, 3, 3, 3, 4 ),
 ( 1.868354362588067661E-17, 0.0007657099931970537312, 0.001531419946797914168, 0.002296279302920151665, 0.003061450627205758099 ),
 .UNSPECIFIED. ) ;
#7100=ORIENTED_EDGE ( 'NONE', *, *, #25818, .F. ) ;
#7111=( BOUNDED_SURFACE ( )  B_SPLINE_SURFACE ( 3, 1, ( 
 ( #1140, #18985 ),
 ( #18395, #14080 ),
 ( #27764, #8065 ),
 ( #9630, #27175 ) ),
 .UNSPECIFIED., .F., .F., .F. ) 
 B_SPLINE_SURFACE_WITH_KNOTS ( ( 4, 4 ),
 ( 2, 2 ),
 ( 0.000000000000000000, 1.000000000000000000 ),
 ( 0.000000000000000000, 1.000000000000000000 ),
 .UNSPECIFIED. ) 
 GEOMETRIC_REPRESENTATION_ITEM ( )  RATIONAL_B_SPLINE_SURFACE ( (
 ( 1.000000000000000000, 1.000000000000000000),
 ( 0.7789835883360578528, 0.9689951854195403280),
 ( 0.7789835883360578528, 0.9689951854195403280),
 ( 1.000000000000000000, 1.000000000000000000) ) ) 
 REPRESENTATION_ITEM ( '' )  SURFACE ( )  );
#7113=CARTESIAN_POINT ( 'NONE',  ( -22.34422965417123663, -6.759368364654068095, 37.30738373203626423 ) ) ;
#7119=CARTESIAN_POINT ( 'NONE',  ( -55.24728320129491266, -0.01402509393918509838, 0.003868537197316900683 ) ) ;
#7121=ORIENTED_EDGE ( 'NONE', *, *, #17887, .F. ) ;
#7127=EDGE_LOOP ( 'NONE', ( #3740, #2675, #16315, #27134 ) ) ;
#7128=FACE_OUTER_BOUND ( 'NONE', #24340, .T. ) ;
#7130=DIRECTION ( 'NONE',  ( 0.000000000000000000, 5.223019709708233256E-21, -1.000000000000000000 ) ) ;
#7137=EDGE_CURVE ( 'NONE', #27834, #9239, #12238, .T. ) ;
#7147=CARTESIAN_POINT ( 'NONE',  ( -1.019300379054419947, -25.26451264419671361, -38.21680004809154241 ) ) ;
#7148=CARTESIAN_POINT ( 'NONE',  ( -1.045287976400383290, 12.68782741917383738, 44.00138577190627842 ) ) ;
#7149=CARTESIAN_POINT ( 'NONE',  ( -1.045287976400362417, 25.66401692419989899, -37.92705037016767733 ) ) ;
#7151=ORIENTED_EDGE ( 'NONE', *, *, #27690, .F. ) ;
#7155=EDGE_LOOP ( 'NONE', ( #24596, #11197, #5459, #27394 ) ) ;
#7156=CARTESIAN_POINT ( 'NONE',  ( -16.86833981943423311, 31.95666732167563850, -30.57013526701928186 ) ) ;
#7159=ORIENTED_EDGE ( 'NONE', *, *, #8933, .F. ) ;
#7164=CARTESIAN_POINT ( 'NONE',  ( -55.24728320129491266, -0.009072670231974808847, -0.01137345571546840607 ) ) ;
#7165=EDGE_CURVE ( 'NONE', #19774, #2342, #11867, .T. ) ;
#7172=EDGE_CURVE ( 'NONE', #26061, #24558, #16710, .T. ) ;
#7174=B_SPLINE_CURVE_WITH_KNOTS ( 'NONE', 3,
 ( #24650, #8950, #12965, #6790, #21760, #2024 ),
 .UNSPECIFIED., .F., .F.,
 ( 4, 2, 4 ),
 ( 0.000000000000000000, 0.003570751334075638293, 0.007141502668151268780 ),
 .UNSPECIFIED. ) ;
#7178=CARTESIAN_POINT ( 'NONE',  ( -1.259920593601984162, 16.33409644610551581, -43.01175804832013938 ) ) ;
#7195=CARTESIAN_POINT ( 'NONE',  ( -24.53237795827029899, -24.99972053297889119, 22.94498492516371613 ) ) ;
#7203=B_SPLINE_CURVE_WITH_KNOTS ( 'NONE', 3,
 ( #27910, #3737, #1433, #23199, #3883, #12099, #12650, #21296 ),
 .UNSPECIFIED., .F., .F.,
 ( 4, 2, 2, 4 ),
 ( 0.000000000000000000, 0.002761524886576646742, 0.005523049773153293485, 0.01104609954630660605 ),
 .UNSPECIFIED. ) ;
#7208=ORIENTED_EDGE ( 'NONE', *, *, #16415, .F. ) ;
#7212=B_SPLINE_CURVE_WITH_KNOTS ( 'NONE', 3,
 ( #19773, #10874, #17619, #25987, #6703, #15450, #24259 ),
 .UNSPECIFIED., .F., .F.,
 ( 4, 3, 4 ),
 ( 0.000000000000000000, 0.006568092053401781462, 0.02506242213020847681 ),
 .UNSPECIFIED. ) ;
#7213=CARTESIAN_POINT ( 'NONE',  ( -55.25297051322618813, -0.01306918787467559705, 0.007247191603131494450 ) ) ;
#7223=CARTESIAN_POINT ( 'NONE',  ( -8.786685647604887350, -38.68584556812326980, -37.00619870957918778 ) ) ;
#7232=CARTESIAN_POINT ( 'NONE',  ( -1.045287976400379737, 44.00138577190644185, -12.68782741917337198 ) ) ;
#7237=ORIENTED_EDGE ( 'NONE', *, *, #13321, .F. ) ;
#7240=ADVANCED_FACE ( 'NONE', ( #9047 ), #25409, .F. ) ;
#7244=( BOUNDED_SURFACE ( )  B_SPLINE_SURFACE ( 3, 1, ( 
 ( #28361, #27951 ),
 ( #19592, #12971 ),
 ( #19457, #21764 ),
 ( #8659, #23803 ) ),
 .UNSPECIFIED., .F., .F., .F. ) 
 B_SPLINE_SURFACE_WITH_KNOTS ( ( 4, 4 ),
 ( 2, 2 ),
 ( 0.000000000000000000, 1.000000000000000000 ),
 ( 0.000000000000000000, 1.000000000000000000 ),
 .UNSPECIFIED. ) 
 GEOMETRIC_REPRESENTATION_ITEM ( )  RATIONAL_B_SPLINE_SURFACE ( (
 ( 1.000000000000000000, 1.000000000000000000),
 ( 0.9593753223639863714, 0.9995975284513187731),
 ( 0.9593753223639863714, 0.9995975284513187731),
 ( 1.000000000000000000, 1.000000000000000000) ) ) 
 REPRESENTATION_ITEM ( '' )  SURFACE ( )  );
#7248=CARTESIAN_POINT ( 'NONE',  ( -7.733045908741342345, 25.81515396910926086, 45.70676731105690749 ) ) ;
#7251=LINE ( 'NONE', #16850, #16216 ) ;
#7254=CARTESIAN_POINT ( 'NONE',  ( -1.619063947482197729, -43.26576862488445130, -16.67502769180545386 ) ) ;
#7258=CARTESIAN_POINT ( 'NONE',  ( -1.619063947482201282, -11.94059994246191359, -44.80407745103779860 ) ) ;
#7262=ORIENTED_EDGE ( 'NONE', *, *, #3484, .F. ) ;
#7277=CARTESIAN_POINT ( 'NONE',  ( -20.24419206586952313, -16.36655224501349437, 24.70913649113847299 ) ) ;
#7280=EDGE_CURVE ( 'NONE', #10634, #3225, #5348, .T. ) ;
#7282=ORIENTED_EDGE ( 'NONE', *, *, #24125, .F. ) ;
#7283=CARTESIAN_POINT ( 'NONE',  ( -1.045287976400362417, -1.530335034933495653, 45.76855895860946788 ) ) ;
#7289=ORIENTED_EDGE ( 'NONE', *, *, #26954, .T. ) ;
#7291=CARTESIAN_POINT ( 'NONE',  ( -8.786685647604890903, 38.68584556812300690, -37.00619870957947910 ) ) ;
#7295=ORIENTED_EDGE ( 'NONE', *, *, #4990, .T. ) ;
#7300=EDGE_CURVE ( 'NONE', #18479, #8132, #17388, .T. ) ;
#7302=DIRECTION ( 'NONE',  ( 1.000000000000000000, -6.938893903907226837E-18, 1.734723475976806709E-18 ) ) ;
#7307=CARTESIAN_POINT ( 'NONE',  ( -1.031422197589711987, -15.60268798220668707, -43.06660437151302290 ) ) ;
#7308=ORIENTED_EDGE ( 'NONE', *, *, #15984, .T. ) ;
#7309=B_SPLINE_CURVE_WITH_KNOTS ( 'NONE', 3,
 ( #12792, #2124, #15084, #23773, #28460, #22000 ),
 .UNSPECIFIED., .F., .F.,
 ( 4, 2, 4 ),
 ( 4.982613841084487634E-18, 0.0004335151646191490811, 0.0008670303292382946928 ),
 .UNSPECIFIED. ) ;
#7312=CARTESIAN_POINT ( 'NONE',  ( -28.41354790283022069, 12.60397206714832663, -19.47297445639553715 ) ) ;
#7314=VERTEX_POINT ( 'NONE', #6611 ) ;
#7316=FACE_OUTER_BOUND ( 'NONE', #22815, .T. ) ;
#7317=CARTESIAN_POINT ( 'NONE',  ( -20.90916690077961704, -27.35210456531395451, -28.59207721780137135 ) ) ;
#7318=ORIENTED_EDGE ( 'NONE', *, *, #4676, .T. ) ;
#7322=DIRECTION ( 'NONE',  ( -0.7637818620346801257, 0.1788995134688785849, -0.6201872550346672064 ) ) ;
#7343=CIRCLE ( 'NONE', #23433, 53.53553390275978785 ) ;
#7349=ORIENTED_EDGE ( 'NONE', *, *, #11244, .F. ) ;
#7355=CARTESIAN_POINT ( 'NONE',  ( -55.24390624410018802, 0.007245494385991800047, -0.007503127514277958821 ) ) ;
#7367=B_SPLINE_CURVE_WITH_KNOTS ( 'NONE', 3,
 ( #13052, #6441, #10619, #21838, #28298, #8888 ),
 .UNSPECIFIED., .F., .F.,
 ( 4, 2, 4 ),
 ( 0.000000000000000000, 0.003570751334075635691, 0.007141502668151271382 ),
 .UNSPECIFIED. ) ;
#7373=ORIENTED_EDGE ( 'NONE', *, *, #26238, .F. ) ;
#7375=CARTESIAN_POINT ( 'NONE',  ( -1.048172774974299282, 36.44231470008717366, -27.73787987941021171 ) ) ;
#7376=VECTOR ( 'NONE', #12825, 999.9999999999998863 ) ;
#7382=CARTESIAN_POINT ( 'NONE',  ( -20.20700224038492721, 18.19058640100257662, 23.35150625415638714 ) ) ;
#7385=CARTESIAN_POINT ( 'NONE',  ( -28.41354790283022069, -23.16239616762932130, -1.249099604786995332 ) ) ;
#7388=EDGE_CURVE ( 'NONE', #6927, #19163, #14253, .T. ) ;
#7390=CARTESIAN_POINT ( 'NONE',  ( -20.47566338032516597, -27.87687989047309145, 10.72601609985058957 ) ) ;
#7413=AXIS2_PLACEMENT_3D ( 'NONE', #10756, #15178, #17215 ) ;
#7419=EDGE_CURVE ( 'NONE', #11485, #5381, #15938, .T. ) ;
#7422=CARTESIAN_POINT ( 'NONE',  ( -55.24340739397742794, 0.009842732675349290250, 0.002421372372456403153 ) ) ;
#7424=CARTESIAN_POINT ( 'NONE',  ( -1.049819825607592794, -14.63675055554412374, -43.39756533277876827 ) ) ;
#7443=CARTESIAN_POINT ( 'NONE',  ( -55.25297051322618813, -0.01354497706059863693, -0.006313402748433391727 ) ) ;
#7444=CARTESIAN_POINT ( 'NONE',  ( -1.619063947482201282, -16.67502769180592992, -43.26576862488428077 ) ) ;
#7457=EDGE_CURVE ( 'NONE', #16092, #3709, #18320, .T. ) ;
#7458=FACE_OUTER_BOUND ( 'NONE', #27140, .T. ) ;
#7463=CARTESIAN_POINT ( 'NONE',  ( -1.056502255334264895, 26.51074901220504643, -37.35734037467642565 ) ) ;
#7478=CARTESIAN_POINT ( 'NONE',  ( -20.20700224038492721, -29.58392382092672790, 0.9908225410481621420 ) ) ;
#7489=AXIS2_PLACEMENT_3D ( 'NONE', #18635, #3652, #23117 ) ;
#7491=EDGE_CURVE ( 'NONE', #16414, #27068, #3258, .T. ) ;
#7495=CARTESIAN_POINT ( 'NONE',  ( -8.786685647604887350, -25.35688121747534751, -47.14957014837345639 ) ) ;
#7496=( BOUNDED_SURFACE ( )  B_SPLINE_SURFACE ( 3, 1, ( 
 ( #19407, #17519 ),
 ( #2110, #6458 ),
 ( #15070, #13193 ),
 ( #26303, #8902 ) ),
 .UNSPECIFIED., .F., .F., .F. ) 
 B_SPLINE_SURFACE_WITH_KNOTS ( ( 4, 4 ),
 ( 2, 2 ),
 ( 0.000000000000000000, 1.000000000000000000 ),
 ( 0.000000000000000000, 1.000000000000000000 ),
 .UNSPECIFIED. ) 
 GEOMETRIC_REPRESENTATION_ITEM ( )  RATIONAL_B_SPLINE_SURFACE ( (
 ( 1.000000000000000000, 1.000000000000000000),
 ( 0.9934239774497838349, 0.8357310067453913582),
 ( 0.9934239774497838349, 0.8357310067453913582),
 ( 1.000000000000000000, 1.000000000000000000) ) ) 
 REPRESENTATION_ITEM ( '' )  SURFACE ( )  );
#7497=CARTESIAN_POINT ( 'NONE',  ( -7.078251931573406708, -34.59014398252944034, -38.93060825814217196 ) ) ;
#7499=EDGE_CURVE ( 'NONE', #711, #9163, #25731, .T. ) ;
#7501=DIRECTION ( 'NONE',  ( 1.000000000000000000, -6.938893903907226837E-18, 1.734723475976806709E-18 ) ) ;
#7510=CARTESIAN_POINT ( 'NONE',  ( -1.045287976400362417, -43.05558670614257721, -15.59869763335051651 ) ) ;
#7515=CIRCLE ( 'NONE', #9792, 53.53553390275978785 ) ;
#7517=ORIENTED_EDGE ( 'NONE', *, *, #15453, .T. ) ;
#7520=VECTOR ( 'NONE', #7322, 1000.000000000000000 ) ;
#7533=CARTESIAN_POINT ( 'NONE',  ( -55.25719721206881729, -0.002847566758682281655, 0.01079965405819869988 ) ) ;
#7537=EDGE_CURVE ( 'NONE', #9976, #20677, #25596, .T. ) ;
#7540=CARTESIAN_POINT ( 'NONE',  ( -20.37983603106074426, -1.508851015062371292, 29.73529213200292531 ) ) ;
#7548=CARTESIAN_POINT ( 'NONE',  ( -8.786685647604890903, 7.199674155858966529, -53.04920435127184675 ) ) ;
#7549=CARTESIAN_POINT ( 'NONE',  ( -1.259920593601994376, 35.85909937955963755, 28.82601305773611600 ) ) ;
#7553=EDGE_CURVE ( 'NONE', #2725, #10615, #5736, .T. ) ;
#7562=ORIENTED_EDGE ( 'NONE', *, *, #20303, .F. ) ;
#7564=ADVANCED_FACE ( 'NONE', ( #3550 ), #12190, .F. ) ;
#7570=CARTESIAN_POINT ( 'NONE',  ( -1.539760825549688628, -2.469813586483410539, -46.22267384399379608 ) ) ;
#7579=ORIENTED_EDGE ( 'NONE', *, *, #26542, .T. ) ;
#7586=CARTESIAN_POINT ( 'NONE',  ( -1.583189561560252701, 16.68617981233703063, -43.29471907393747898 ) ) ;
#7593=CARTESIAN_POINT ( 'NONE',  ( -20.21097721712959583, 17.67178718142858429, -23.76068428613687189 ) ) ;
#7595=ADVANCED_FACE ( 'NONE', ( #84 ), #5095, .T. ) ;
#7609=CARTESIAN_POINT ( 'NONE',  ( -23.79248802219728987, 22.01156985585204851, 24.83956736572385893 ) ) ;
#7611=B_SPLINE_CURVE_WITH_KNOTS ( 'NONE', 3,
 ( #12147, #1201, #26817, #4942, #22517, #2783, #11563, #632, #26951, #768 ),
 .UNSPECIFIED., .F., .F.,
 ( 4, 2, 2, 2, 4 ),
 ( 1.301042606982605128E-18, 0.0003346267210630945186, 0.0006692534421261877361, 0.001003880163189281062, 0.001338506884252374171 ),
 .UNSPECIFIED. ) ;
#7615=CARTESIAN_POINT ( 'NONE',  ( -1.048994561756795729, 43.78680886990941445, -13.42228657661138058 ) ) ;
#7619=ORIENTED_EDGE ( 'NONE', *, *, #22055, .T. ) ;
#7624=CARTESIAN_POINT ( 'NONE',  ( -20.20700224038492010, -8.199606986804138131, 28.44216453106544762 ) ) ;
#7625=CARTESIAN_POINT ( 'NONE',  ( -21.81686047589429123, 26.62923599424970433, -27.83628745321458453 ) ) ;
#7630=CARTESIAN_POINT ( 'NONE',  ( -1.045287976400362417, -43.05558670614257721, -15.59869763335051651 ) ) ;
#7636=CARTESIAN_POINT ( 'NONE',  ( -20.20700224038492721, 16.58740185276746359, 24.51628800869029234 ) ) ;
#7666=ORIENTED_EDGE ( 'NONE', *, *, #1731, .T. ) ;
#7670=ADVANCED_FACE ( 'NONE', ( #20078 ), #983, .T. ) ;
#7684=B_SPLINE_CURVE_WITH_KNOTS ( 'NONE', 3,
 ( #27839, #19067, #16772, #25555, #12427, #1497 ),
 .UNSPECIFIED., .F., .F.,
 ( 4, 2, 4 ),
 ( 0.000000000000000000, 0.0004335184443140195285, 0.0008670368886280390569 ),
 .UNSPECIFIED. ) ;
#7686=CARTESIAN_POINT ( 'NONE',  ( -20.20700224038492721, -23.35150625415645820, 18.19058640100249491 ) ) ;
#7688=CARTESIAN_POINT ( 'NONE',  ( -55.24300891470650754, -0.008142823778061761275, -0.005486913146700541852 ) ) ;
#7691=CARTESIAN_POINT ( 'NONE',  ( -12.82751273423881777, 23.15139349681311387, -43.04932478553539710 ) ) ;
#7700=CARTESIAN_POINT ( 'NONE',  ( -1.113427685307011084, 35.91272432484659305, -28.52429901637181686 ) ) ;
#7711=( BOUNDED_SURFACE ( )  B_SPLINE_SURFACE ( 3, 1, ( 
 ( #13281, #2635 ),
 ( #10998, #9266 ),
 ( #197, #4501 ),
 ( #22067, #17453 ) ),
 .UNSPECIFIED., .F., .F., .F. ) 
 B_SPLINE_SURFACE_WITH_KNOTS ( ( 4, 4 ),
 ( 2, 2 ),
 ( 0.000000000000000000, 1.000000000000000000 ),
 ( 0.000000000000000000, 1.000000000000000000 ),
 .UNSPECIFIED. ) 
 GEOMETRIC_REPRESENTATION_ITEM ( )  RATIONAL_B_SPLINE_SURFACE ( (
 ( 1.000000000000000000, 1.000000000000000000),
 ( 0.7789835883360578528, 0.9689951854195403280),
 ( 0.7789835883360578528, 0.9689951854195403280),
 ( 1.000000000000000000, 1.000000000000000000) ) ) 
 REPRESENTATION_ITEM ( '' )  SURFACE ( )  );
#7716=CARTESIAN_POINT ( 'NONE',  ( -25.21435515916043002, 34.05351380035335040, -6.169479169075572145 ) ) ;
#7717=CARTESIAN_POINT ( 'NONE',  ( -1.239374126674604337, 44.48112152129347407, -11.92219841463844432 ) ) ;
#7728=CARTESIAN_POINT ( 'NONE',  ( -1.045287976400362417, 25.66401692420069125, 37.92705037016716574 ) ) ;
#7738=ORIENTED_EDGE ( 'NONE', *, *, #16035, .T. ) ;
#7739=CARTESIAN_POINT ( 'NONE',  ( -20.21097721650785672, 17.13687097598137399, -24.14932365326959030 ) ) ;
#7741=CARTESIAN_POINT ( 'NONE',  ( -4.178947244162641184, -47.46809051147732106, -11.88256963646720266 ) ) ;
#7742=ORIENTED_EDGE ( 'NONE', *, *, #16485, .T. ) ;
#7743=ORIENTED_EDGE ( 'NONE', *, *, #8006, .T. ) ;
#7752=B_SPLINE_CURVE_WITH_KNOTS ( 'NONE', 3,
 ( #5657, #26937, #14421, #7686 ),
 .UNSPECIFIED., .F., .F.,
 ( 4, 4 ),
 ( 1.895855152355442610E-16, 0.001982023823822945917 ),
 .UNSPECIFIED. ) ;
#7766=EDGE_CURVE ( 'NONE', #8983, #27304, #4645, .T. ) ;
#7767=CARTESIAN_POINT ( 'NONE',  ( -20.57838717382308502, 27.96569011373086866, -10.78122205917010135 ) ) ;
#7773=CARTESIAN_POINT ( 'NONE',  ( -1.583189561560256253, -36.01941156322767057, 29.24830400313204493 ) ) ;
#7780=CARTESIAN_POINT ( 'NONE',  ( -55.24390624410018802, 0.01027195578987812573, -0.001811362924359468263 ) ) ;
#7798=VERTEX_POINT ( 'NONE', #14736 ) ;
#7800=EDGE_CURVE ( 'NONE', #21937, #13776, #27967, .T. ) ;
#7803=CARTESIAN_POINT ( 'NONE',  ( -1.031422197589711987, -45.78027046666441890, 1.530725436377941673 ) ) ;
#7807=CARTESIAN_POINT ( 'NONE',  ( -1.045287976400365970, -45.76855895860942525, 1.530335034934587002 ) ) ;
#7819=VERTEX_POINT ( 'NONE', #25270 ) ;
#7821=CARTESIAN_POINT ( 'NONE',  ( -21.41430102051752016, -16.60879216503617073, 25.94791611261633690 ) ) ;
#7827=CARTESIAN_POINT ( 'NONE',  ( -20.21097721650786738, 17.67178726257392896, 23.76068422213738529 ) ) ;
#7835=LINE ( 'NONE', #18299, #19449 ) ;
#7841=CARTESIAN_POINT ( 'NONE',  ( -28.13707043255157103, -22.88591869784690402, 0.7675454997509406629 ) ) ;
#7846=VERTEX_POINT ( 'NONE', #298 ) ;
#7849=EDGE_LOOP ( 'NONE', ( #15780, #18437 ) ) ;
#7850=VECTOR ( 'NONE', #10777, 1000.000000000000114 ) ;
#7854=EDGE_CURVE ( 'NONE', #9726, #18571, #6259, .T. ) ;
#7855=CARTESIAN_POINT ( 'NONE',  ( -1.583189561560256253, -43.29471907393730135, 16.68617981233747827 ) ) ;
#7860=B_SPLINE_CURVE_WITH_KNOTS ( 'NONE', 3,
 ( #13403, #6959, #18005, #26790, #22203, #24673 ),
 .UNSPECIFIED., .F., .F.,
 ( 4, 2, 4 ),
 ( 0.000000000000000000, 0.0004335184443140181732, 0.0008670368886280363464 ),
 .UNSPECIFIED. ) ;
#7863=B_SPLINE_CURVE_WITH_KNOTS ( 'NONE', 3,
 ( #283, #26337, #28345, #24336, #21889, #2581 ),
 .UNSPECIFIED., .F., .F.,
 ( 4, 2, 4 ),
 ( 0.000000000000000000, 0.0004335151646191513579, 0.0008670303292383027159 ),
 .UNSPECIFIED. ) ;
#7865=CARTESIAN_POINT ( 'NONE',  ( -1.044556982611269058, -44.03203163107536966, -12.57890920527759171 ) ) ;
#7866=DIRECTION ( 'NONE',  ( 1.000000000000000000, -6.938893903907226837E-18, 1.734723475976806709E-18 ) ) ;
#7870=ORIENTED_EDGE ( 'NONE', *, *, #14371, .F. ) ;
#7873=CARTESIAN_POINT ( 'NONE',  ( -1.155001620486246994, 25.28075036143276932, 38.31519699443472859 ) ) ;
#7874=CARTESIAN_POINT ( 'NONE',  ( -20.47566262905010603, -7.708089517695397852, -28.85746289809576126 ) ) ;
#7887=CIRCLE ( 'NONE', #11990, 34.60786435723138510 ) ;
#7906=CARTESIAN_POINT ( 'NONE',  ( -20.38016308990357572, -1.509191766064412299, -29.73560196176845238 ) ) ;
#7907=ORIENTED_EDGE ( 'NONE', *, *, #15140, .T. ) ;
#7914=CARTESIAN_POINT ( 'NONE',  ( -20.20700224038492010, 18.19058640100223556, -23.35150625415664649 ) ) ;
#7916=CARTESIAN_POINT ( 'NONE',  ( -1.048996300304501972, -43.31387123529967909, 14.87787369922214076 ) ) ;
#7922=CARTESIAN_POINT ( 'NONE',  ( -55.24271866751342941, 0.004365563123935787236, 0.008433070970613791573 ) ) ;
#7923=AXIS2_PLACEMENT_3D ( 'NONE', #5484, #27206, #5194 ) ;
#7940=EDGE_CURVE ( 'NONE', #17492, #1901, #19354, .T. ) ;
#7950=ORIENTED_EDGE ( 'NONE', *, *, #28360, .F. ) ;
#7953=LINE ( 'NONE', #16981, #14258 ) ;
#7959=CARTESIAN_POINT ( 'NONE',  ( 0.000000000000000000, 0.000000000000000000, 0.000000000000000000 ) ) ;
#7966=CARTESIAN_POINT ( 'NONE',  ( -1.619063947482201282, 38.92136151114908671, -25.20140673341387227 ) ) ;
#7968=ORIENTED_EDGE ( 'NONE', *, *, #6932, .T. ) ;
#7972=EDGE_CURVE ( 'NONE', #13800, #25441, #15197, .T. ) ;
#7975=( BOUNDED_SURFACE ( )  B_SPLINE_SURFACE ( 3, 1, ( 
 ( #15337, #4129 ),
 ( #12899, #1963 ),
 ( #2097, #10767 ),
 ( #17358, #26149 ) ),
 .UNSPECIFIED., .F., .F., .F. ) 
 B_SPLINE_SURFACE_WITH_KNOTS ( ( 4, 4 ),
 ( 2, 2 ),
 ( 0.000000000000000000, 1.000000000000000000 ),
 ( 0.000000000000000000, 1.000000000000000000 ),
 .UNSPECIFIED. ) 
 GEOMETRIC_REPRESENTATION_ITEM ( )  RATIONAL_B_SPLINE_SURFACE ( (
 ( 1.000000000000000000, 1.000000000000000000),
 ( 0.9934239774497837239, 0.8357310067453919133),
 ( 0.9934239774497837239, 0.8357310067453919133),
 ( 1.000000000000000000, 1.000000000000000000) ) ) 
 REPRESENTATION_ITEM ( '' )  SURFACE ( )  );
#7984=B_SPLINE_CURVE_WITH_KNOTS ( 'NONE', 3,
 ( #20760, #27079, #5070, #3488, #11706, #7691, #16592 ),
 .UNSPECIFIED., .F., .F.,
 ( 4, 3, 4 ),
 ( 0.000000000000000000, 0.006568092053401780595, 0.02506242213020846640 ),
 .UNSPECIFIED. ) ;
#7985=EDGE_CURVE ( 'NONE', #4018, #23277, #10815, .T. ) ;
#7989=CARTESIAN_POINT ( 'NONE',  ( -1.463510566862832096, 35.90603835816546763, 29.09194585123793786 ) ) ;
#7991=VECTOR ( 'NONE', #12997, 1000.000000000000000 ) ;
#7998=FACE_OUTER_BOUND ( 'NONE', #97, .T. ) ;
#8003=AXIS2_PLACEMENT_3D ( 'NONE', #27161, #16231, #27452 ) ;
#8005=EDGE_CURVE ( 'NONE', #19578, #25057, #1869, .T. ) ;
#8006=EDGE_CURVE ( 'NONE', #12467, #13110, #27494, .T. ) ;
#8009=CARTESIAN_POINT ( 'NONE',  ( -22.23226125620929494, -30.68305173820431619, -7.677408153693907167 ) ) ;
#8010=CARTESIAN_POINT ( 'NONE',  ( -20.20898968516257810, 0.6607166829023055632, 29.59696826051171925 ) ) ;
#8019=CARTESIAN_POINT ( 'NONE',  ( -25.21435515916025594, 1.749597353048488237E-16, -4.373993382621220594E-17 ) ) ;
#8023=CARTESIAN_POINT ( 'NONE',  ( -1.619063947482194177, 35.99532424477422410, 29.22875152547716482 ) ) ;
#8030=FACE_OUTER_BOUND ( 'NONE', #12702, .T. ) ;
#8038=CARTESIAN_POINT ( 'NONE',  ( -9.156249394959713683, 53.90509764945130655, -8.027840202794127578 ) ) ;
#8043=CARTESIAN_POINT ( 'NONE',  ( -20.20700224038492721, 28.44216453106536946, -8.199606986804427677 ) ) ;
#8045=CARTESIAN_POINT ( 'NONE',  ( -1.048996300304477769, -13.42280206896947092, 43.78665266739852058 ) ) ;
#8047=CARTESIAN_POINT ( 'NONE',  ( -1.050229599974473516, 43.63650726458064355, -13.90955673306141627 ) ) ;
#8050=ORIENTED_EDGE ( 'NONE', *, *, #27976, .F. ) ;
#8057=CARTESIAN_POINT ( 'NONE',  ( -1.619063947482201282, -44.80407745103776307, 11.94059994246206635 ) ) ;
#8060=CARTESIAN_POINT ( 'NONE',  ( -22.34422965417126505, 5.100074259623119666, 37.57019010019537575 ) ) ;
#8065=CARTESIAN_POINT ( 'NONE',  ( -4.473127245936431073, 3.196405119333807221, -49.22197550883368677 ) ) ;
#8066=ADVANCED_FACE ( 'NONE', ( #12938 ), #13835, .T. ) ;
#8080=CARTESIAN_POINT ( 'NONE',  ( -1.619063947482201282, 44.80407745103784123, -11.94059994246174838 ) ) ;
#8084=CARTESIAN_POINT ( 'NONE',  ( -20.38016308990359349, -10.62413300761005353, -27.81387210821418776 ) ) ;
#8088=CARTESIAN_POINT ( 'NONE',  ( -20.57838717382308147, -23.26537097894118133, -18.89542499756491978 ) ) ;
#8091=DIRECTION ( 'NONE',  ( 0.000000000000000000, 5.223019709707975211E-21, -1.000000000000000000 ) ) ;
#8093=CARTESIAN_POINT ( 'NONE',  ( -1.049817751779892117, -45.79652915392414769, -0.5106138415325238711 ) ) ;
#8096=CARTESIAN_POINT ( 'NONE',  ( 180.4657679828686980, -1.252232817320263489E-15, 3.130582043300658722E-16 ) ) ;
#8106=ORIENTED_EDGE ( 'NONE', *, *, #7553, .T. ) ;
#8112=DIRECTION ( 'NONE',  ( 1.000000000000000000, -6.938893903907226837E-18, 1.734723475976806709E-18 ) ) ;
#8113=EDGE_CURVE ( 'NONE', #20148, #10460, #18441, .T. ) ;
#8132=VERTEX_POINT ( 'NONE', #5923 ) ;
#8135=CARTESIAN_POINT ( 'NONE',  ( -1.019300379054419725, 16.06793277092052818, 42.90269154183410194 ) ) ;
#8148=CARTESIAN_POINT ( 'NONE',  ( -19.53423201713129842, 4.045852573675910766E-15, -28.92774122539760384 ) ) ;
#8155=CARTESIAN_POINT ( 'NONE',  ( -55.24390624410018802, 0.001811362924359719581, 0.01027195578987765215 ) ) ;
#8157=CARTESIAN_POINT ( 'NONE',  ( -1.619063947482197729, -44.80407745103793360, -11.94059994246142331 ) ) ;
#8159=EDGE_LOOP ( 'NONE', ( #10532, #12670, #14995, #8636 ) ) ;
#8163=VERTEX_POINT ( 'NONE', #20121 ) ;
#8172=EDGE_CURVE ( 'NONE', #1672, #6924, #22442, .T. ) ;
#8174=CARTESIAN_POINT ( 'NONE',  ( -28.41354790283022069, 14.62505768302800924, -18.00456980371904692 ) ) ;
#8177=ORIENTED_EDGE ( 'NONE', *, *, #15988, .F. ) ;
#8202=CARTESIAN_POINT ( 'NONE',  ( -7.733045908741333463, 51.44704017882777691, -10.42750254442556290 ) ) ;
#8205=EDGE_CURVE ( 'NONE', #8855, #19774, #4076, .T. ) ;
#8221=CARTESIAN_POINT ( 'NONE',  ( -55.24198130335446422, 0.009170435128245552417, -0.001516807524704325135 ) ) ;
#8232=CIRCLE ( 'NONE', #10121, 53.53553390275978785 ) ;
#8233=EDGE_LOOP ( 'NONE', ( #18321, #25024, #18086, #22379 ) ) ;
#8237=CARTESIAN_POINT ( 'NONE',  ( -55.25297051322618813, 0.01466904165775564234, -0.002853887643044135131 ) ) ;
#8241=CARTESIAN_POINT ( 'NONE',  ( -1.045287976400383290, -12.68782741917353185, -44.00138577190637079 ) ) ;
#8247=CARTESIAN_POINT ( 'NONE',  ( -1.045287976400383290, -12.68782741917353185, -44.00138577190637079 ) ) ;
#8249=B_SPLINE_CURVE_WITH_KNOTS ( 'NONE', 3,
 ( #16775, #4493, #13136, #15283, #13416, #13271, #22057 ),
 .UNSPECIFIED., .F., .F.,
 ( 4, 3, 4 ),
 ( 1.105886215935214523E-17, 0.0007657099931970557912, 0.001530725384384964971 ),
 .UNSPECIFIED. ) ;
#8253=CARTESIAN_POINT ( 'NONE',  ( -55.24198130335446422, 0.006527480770976314475, -0.006617369590168970667 ) ) ;
#8254=CARTESIAN_POINT ( 'NONE',  ( -7.078251931573400491, -5.101176922830306104, 51.82710018979479116 ) ) ;
#8258=CARTESIAN_POINT ( 'NONE',  ( -1.155031165708877872, 38.31525684316177660, 25.28071330859845389 ) ) ;
#8259=CARTESIAN_POINT ( 'NONE',  ( -1.048172774974279076, 45.78636862970795107, -1.020161070261278224 ) ) ;
#8260=EDGE_LOOP ( 'NONE', ( #12288, #17744 ) ) ;
#8261=ADVANCED_FACE ( 'NONE', ( #9921 ), #416, .F. ) ;
#8266=CARTESIAN_POINT ( 'NONE',  ( -23.79248802219724368, 7.157555990716900851, -32.40806545715334153 ) ) ;
#8272=CARTESIAN_POINT ( 'NONE',  ( 6.505213034913034000E-17, 4.541450660883840889E-15, -37.50000000000001421 ) ) ;
#8286=ORIENTED_EDGE ( 'NONE', *, *, #22055, .F. ) ;
#8289=ORIENTED_EDGE ( 'NONE', *, *, #7137, .F. ) ;
#8296=B_SPLINE_CURVE_WITH_KNOTS ( 'NONE', 3,
 ( #20243, #27699, #8009, #16771, #25553, #536 ),
 .UNSPECIFIED., .F., .F.,
 ( 4, 2, 4 ),
 ( 4.906538933386797396E-18, 0.003570751334075636559, 0.007141502668151274852 ),
 .UNSPECIFIED. ) ;
#8298=CARTESIAN_POINT ( 'NONE',  ( -20.20700224038492010, 18.19058640100223556, -23.35150625415664649 ) ) ;
#8306=CARTESIAN_POINT ( 'NONE',  ( -20.20700224038492721, -27.82980252387826781, -10.08426345511578504 ) ) ;
#8308=CARTESIAN_POINT ( 'NONE',  ( -28.41354790283022069, 8.345538364877384652, 21.64275480268738860 ) ) ;
#8309=ORIENTED_EDGE ( 'NONE', *, *, #18091, .T. ) ;
#8316=B_SPLINE_CURVE_WITH_KNOTS ( 'NONE', 3,
 ( #25386, #16449, #27380, #16157, #7390, #20615 ),
 .UNSPECIFIED., .F., .F.,
 ( 4, 2, 4 ),
 ( 0.000000000000000000, 0.0004335184443140221305, 0.0008670368886280442611 ),
 .UNSPECIFIED. ) ;
#8319=CARTESIAN_POINT ( 'NONE',  ( -24.53237795827027412, -22.94498492516361310, -24.99972053297897290 ) ) ;
#8321=CARTESIAN_POINT ( 'NONE',  ( -1.056502255334265339, 13.66916755949911177, 43.72121397317208391 ) ) ;
#8328=ORIENTED_EDGE ( 'NONE', *, *, #2318, .F. ) ;
#8329=CARTESIAN_POINT ( 'NONE',  ( -1.583189561560253589, -16.68617981233733616, -43.29471907393735819 ) ) ;
#8349=AXIS2_PLACEMENT_3D ( 'NONE', #23776, #10388, #8091 ) ;
#8367=CARTESIAN_POINT ( 'NONE',  ( -8.786685647604890903, -9.545808661480982948, -52.67761315067281913 ) ) ;
#8376=EDGE_CURVE ( 'NONE', #17227, #6927, #10288, .T. ) ;
#8392=CARTESIAN_POINT ( 'NONE',  ( -20.90916690077961348, 38.93431874629082756, 7.054312691028585824 ) ) ;
#8395=VECTOR ( 'NONE', #8544, 1000.000000000000114 ) ;
#8398=ORIENTED_EDGE ( 'NONE', *, *, #20632, .T. ) ;
#8406=ORIENTED_EDGE ( 'NONE', *, *, #21501, .F. ) ;
#8408=B_SPLINE_CURVE_WITH_KNOTS ( 'NONE', 3,
 ( #19969, #9040, #17798, #27149, #4716, #26719, #24603 ),
 .UNSPECIFIED., .F., .F.,
 ( 4, 3, 4 ),
 ( 8.845388854693243284E-18, 0.009512539173626400127, 0.02506242213020845599 ),
 .UNSPECIFIED. ) ;
#8410=VECTOR ( 'NONE', #4115, 1000.000000000000000 ) ;
#8430=CARTESIAN_POINT ( 'NONE',  ( -1.050231094221220296, -37.20185272688478051, -26.71409683968603588 ) ) ;
#8434=CARTESIAN_POINT ( 'NONE',  ( -1.619063947482201282, -11.94059994246191359, -44.80407745103779860 ) ) ;
#8438=CIRCLE ( 'NONE', #13472, 53.53553390275978785 ) ;
#8441=CARTESIAN_POINT ( 'NONE',  ( -20.20612091757425688, 18.30568244821375501, -23.26073043121635919 ) ) ;
#8445=CARTESIAN_POINT ( 'NONE',  ( -1.050230346682680560, 14.15335421912582170, -43.55729751025868524 ) ) ;
#8446=DIRECTION ( 'NONE',  ( 0.7563875759206388771, 0.6531865459554678788, 0.03500244528122787441 ) ) ;
#8454=B_SPLINE_CURVE_WITH_KNOTS ( 'NONE', 3,
 ( #21142, #16403, #3165, #3731, #1426, #14382, #12094 ),
 .UNSPECIFIED., .F., .F.,
 ( 4, 3, 4 ),
 ( 2.695974601917670536E-16, 0.009512539173626363698, 0.02506242213020817844 ),
 .UNSPECIFIED. ) ;
#8456=DIRECTION ( 'NONE',  ( 1.000000000000000000, -6.938893903907226837E-18, 1.734723475976806709E-18 ) ) ;
#8473=EDGE_LOOP ( 'NONE', ( #18670, #8289, #4761, #15861 ) ) ;
#8485=CARTESIAN_POINT ( 'NONE',  ( -55.25297051322618813, 0.01354497706059544504, -0.006313402748432239003 ) ) ;
#8487=CARTESIAN_POINT ( 'NONE',  ( -20.57838717382308147, -10.78122205917020437, -27.96569011373082603 ) ) ;
#8488=ORIENTED_EDGE ( 'NONE', *, *, #17702, .T. ) ;
#8492=CARTESIAN_POINT ( 'NONE',  ( -1.058473599757810746, -42.99101666105219977, 15.81436910992565004 ) ) ;
#8499=FACE_OUTER_BOUND ( 'NONE', #15941, .T. ) ;
#8501=CARTESIAN_POINT ( 'NONE',  ( -1.056502255334264895, -43.72121397317232550, -13.66916755949833373 ) ) ;
#8507=EDGE_CURVE ( 'NONE', #13254, #11834, #13001, .T. ) ;
#8511=VERTEX_POINT ( 'NONE', #7012 ) ;
#8528=CARTESIAN_POINT ( 'NONE',  ( -55.24340739397742794, -0.01010924026184046101, 0.0007387096945705813253 ) ) ;
#8533=( BOUNDED_SURFACE ( )  B_SPLINE_SURFACE ( 3, 1, ( 
 ( #13854, #20331 ),
 ( #7119, #11411 ),
 ( #191, #22367 ),
 ( #26518, #15876 ) ),
 .UNSPECIFIED., .F., .F., .F. ) 
 B_SPLINE_SURFACE_WITH_KNOTS ( ( 4, 4 ),
 ( 2, 2 ),
 ( 0.000000000000000000, 1.000000000000000000 ),
 ( 0.000000000000000000, 1.000000000000000000 ),
 .UNSPECIFIED. ) 
 GEOMETRIC_REPRESENTATION_ITEM ( )  RATIONAL_B_SPLINE_SURFACE ( (
 ( 1.000000000000000000, 1.000000000000000000),
 ( 0.7789835883360576307, 0.9689951854195403280),
 ( 0.7789835883360576307, 0.9689951854195403280),
 ( 1.000000000000000000, 1.000000000000000000) ) ) 
 REPRESENTATION_ITEM ( '' )  SURFACE ( )  );
#8536=CARTESIAN_POINT ( 'NONE',  ( -28.41354790283022069, -19.47297445639540214, 12.60397206714853624 ) ) ;
#8538=ORIENTED_EDGE ( 'NONE', *, *, #15862, .F. ) ;
#8544=DIRECTION ( 'NONE',  ( -0.7563875759206389882, 0.1685564395263298709, -0.6320336713238514648 ) ) ;
#8550=EDGE_LOOP ( 'NONE', ( #25279, #21950, #11462, #23712 ) ) ;
#8554=CARTESIAN_POINT ( 'NONE',  ( -55.25719721206881729, -0.0006290797159201363779, 0.01115102788683008592 ) ) ;
#8558=CARTESIAN_POINT ( 'NONE',  ( -4.780792508754334591, -3.764354093953240277, 49.38761389561005188 ) ) ;
#8560=CARTESIAN_POINT ( 'NONE',  ( -1.048171036023509917, -26.08692787913895472, -37.64178826568597458 ) ) ;
#8562=VERTEX_POINT ( 'NONE', #26424 ) ;
#8563=CARTESIAN_POINT ( 'NONE',  ( -55.24271866751342941, 0.001545935011627245191, 0.009369360294294363373 ) ) ;
#8570=ORIENTED_EDGE ( 'NONE', *, *, #6380, .F. ) ;
#8572=VECTOR ( 'NONE', #21005, 999.9999999999998863 ) ;
#8573=CARTESIAN_POINT ( 'NONE',  ( -20.47566262905009538, 18.81547655725247381, -23.19796652405680248 ) ) ;
#8577=CARTESIAN_POINT ( 'NONE',  ( -25.21435515916043357, -6.169479169075226643, 34.05351380035340014 ) ) ;
#8589=CARTESIAN_POINT ( 'NONE',  ( -4.780792508754326597, -48.13366140756551914, 11.68149851467511446 ) ) ;
#8594=ORIENTED_EDGE ( 'NONE', *, *, #22050, .T. ) ;
#8605=( BOUNDED_SURFACE ( )  B_SPLINE_SURFACE ( 3, 1, ( 
 ( #2133, #28469 ),
 ( #8253, #21878 ),
 ( #16753, #8775 ),
 ( #26464, #19044 ) ),
 .UNSPECIFIED., .F., .F., .F. ) 
 B_SPLINE_SURFACE_WITH_KNOTS ( ( 4, 4 ),
 ( 2, 2 ),
 ( 0.000000000000000000, 1.000000000000000000 ),
 ( 0.000000000000000000, 1.000000000000000000 ),
 .UNSPECIFIED. ) 
 GEOMETRIC_REPRESENTATION_ITEM ( )  RATIONAL_B_SPLINE_SURFACE ( (
 ( 1.000000000000000000, 1.000000000000000000),
 ( 0.9593753223639863714, 0.9995975284513187731),
 ( 0.9593753223639863714, 0.9995975284513187731),
 ( 1.000000000000000000, 1.000000000000000000) ) ) 
 REPRESENTATION_ITEM ( '' )  SURFACE ( )  );
#8610=EDGE_CURVE ( 'NONE', #1523, #2580, #21885, .T. ) ;
#8614=DIRECTION ( 'NONE',  ( 1.000000000000000000, -6.938893903907226837E-18, 1.734723475976806709E-18 ) ) ;
#8615=CARTESIAN_POINT ( 'NONE',  ( -25.21435515916042647, 15.02493970636146692, -31.17620025257592786 ) ) ;
#8622=ORIENTED_EDGE ( 'NONE', *, *, #20880, .T. ) ;
#8624=CARTESIAN_POINT ( 'NONE',  ( -22.34422965417125440, -16.46028608106132651, -34.15536449444082479 ) ) ;
#8630=CARTESIAN_POINT ( 'NONE',  ( -4.473127245936434626, -47.80062405537809411, -12.17046501147497750 ) ) ;
#8636=ORIENTED_EDGE ( 'NONE', *, *, #20530, .T. ) ;
#8652=B_SPLINE_CURVE_WITH_KNOTS ( 'NONE', 3,
 ( #8434, #17199, #25985, #8703, #4236, #21807, #2067, #10872 ),
 .UNSPECIFIED., .F., .F.,
 ( 4, 2, 2, 4 ),
 ( 2.225109362706117716E-16, 0.002761568181852862899, 0.005523136363705503753, 0.01104627272741078546 ),
 .UNSPECIFIED. ) ;
#8655=CARTESIAN_POINT ( 'NONE',  ( -1.019300379054419725, -2.023851374322995778, -45.76814864815089123 ) ) ;
#8656=DIRECTION ( 'NONE',  ( 1.000000000000000000, -6.938893903907226837E-18, 1.734723475976806709E-18 ) ) ;
#8659=CARTESIAN_POINT ( 'NONE',  ( -55.24271866751342941, -0.004256484107792937385, -0.008488649505346276131 ) ) ;
#8661=CARTESIAN_POINT ( 'NONE',  ( -1.045287976400386842, -28.14015102489780062, 36.12803364096639314 ) ) ;
#8669=ORIENTED_EDGE ( 'NONE', *, *, #27027, .T. ) ;
#8682=CARTESIAN_POINT ( 'NONE',  ( -1.044557008772713402, 43.01636061109007159, 15.70482370518772086 ) ) ;
#8695=CARTESIAN_POINT ( 'NONE',  ( -1.464342487929870096, 35.90631960086420094, -29.09292098541673965 ) ) ;
#8698=CARTESIAN_POINT ( 'NONE',  ( -20.20700224038492721, -18.19058640100206503, 23.35150625415678860 ) ) ;
#8699=CARTESIAN_POINT ( 'NONE',  ( -1.046936909428679341, -27.93981068760648157, -36.28616897897442328 ) ) ;
#8701=ORIENTED_EDGE ( 'NONE', *, *, #24070, .F. ) ;
#8703=CARTESIAN_POINT ( 'NONE',  ( -4.162674018437137136, -11.82104147411594752, -47.46216648493552981 ) ) ;
#8706=ORIENTED_EDGE ( 'NONE', *, *, #7280, .F. ) ;
#8707=EDGE_CURVE ( 'NONE', #10702, #18351, #2277, .T. ) ;
#8712=CARTESIAN_POINT ( 'NONE',  ( -20.24399999263414429, 18.44171895251396265, -23.20123049637371793 ) ) ;
#8715=CARTESIAN_POINT ( 'NONE',  ( -55.25719721206881729, -0.01041086141212477223, 0.004044147484878232723 ) ) ;
#8720=CARTESIAN_POINT ( 'NONE',  ( -28.13707043255157103, -0.7675454997508607269, -22.88591869784690402 ) ) ;
#8722=EDGE_LOOP ( 'NONE', ( #8488, #22758, #14839, #4479 ) ) ;
#8729=B_SPLINE_CURVE_WITH_KNOTS ( 'NONE', 3,
 ( #6142, #14892, #6403, #3958, #15156, #28399 ),
 .UNSPECIFIED., .F., .F.,
 ( 4, 2, 4 ),
 ( 0.000000000000000000, 0.0004335184443140241905, 0.0008670368886280483810 ),
 .UNSPECIFIED. ) ;
#8738=CARTESIAN_POINT ( 'NONE',  ( -55.24390624410018802, -0.01032895241566633357, -0.001451500391952961289 ) ) ;
#8740=CARTESIAN_POINT ( 'NONE',  ( -20.20700224038492721, -28.44216453106542986, -8.199606986804219844 ) ) ;
#8743=EDGE_LOOP ( 'NONE', ( #16518, #20875, #22314, #1845 ) ) ;
#8744=CARTESIAN_POINT ( 'NONE',  ( -8.786685647604885574, 6.096987947571466530E-17, -1.524246986892866633E-17 ) ) ;
#8775=CARTESIAN_POINT ( 'NONE',  ( -1.056502255334264895, -36.75727364034712963, 27.33667001641208572 ) ) ;
#8792=CARTESIAN_POINT ( 'NONE',  ( -55.24300891470648622, 0.009812809446890878931, 0.0003472257464245802360 ) ) ;
#8794=ORIENTED_EDGE ( 'NONE', *, *, #18898, .T. ) ;
#8799=CARTESIAN_POINT ( 'NONE',  ( -9.156249394959713683, 48.32878616081047340, 25.18996226954561735 ) ) ;
#8801=CARTESIAN_POINT ( 'NONE',  ( -1.045287976400365970, 45.76855895860946077, 1.530335034933974381 ) ) ;
#8802=CARTESIAN_POINT ( 'NONE',  ( -25.21435515916043713, 34.05351380035342146, 6.169479169075106739 ) ) ;
#8803=LINE ( 'NONE', #21336, #7376 ) ;
#8804=CARTESIAN_POINT ( 'NONE',  ( -1.031422197589711764, 36.13727897780167808, 28.14735071801703725 ) ) ;
#8820=ADVANCED_FACE ( 'NONE', ( #8499 ), #27985, .F. ) ;
#8828=B_SPLINE_CURVE_WITH_KNOTS ( 'NONE', 3,
 ( #20482, #16163, #20766, #1333, #18305, #9992, #23241, #20620, #21043, #27531 ),
 .UNSPECIFIED., .F., .F.,
 ( 4, 2, 2, 2, 4 ),
 ( 2.888718286224068903E-16, 0.0003346187017559086596, 0.0006692374035115283793, 0.001003856105267148099, 0.001338474807022767927 ),
 .UNSPECIFIED. ) ;
#8829=CARTESIAN_POINT ( 'NONE',  ( -1.155001620486248770, -25.28075036143248866, -38.31519699443491334 ) ) ;
#8831=VECTOR ( 'NONE', #10542, 1000.000000000000114 ) ;
#8832=CARTESIAN_POINT ( 'NONE',  ( -1.045287976400362417, 37.92705037016796155, 25.66401692419947977 ) ) ;
#8845=CARTESIAN_POINT ( 'NONE',  ( 0.000000000000000000, 0.000000000000000000, 0.000000000000000000 ) ) ;
#8851=ORIENTED_EDGE ( 'NONE', *, *, #460, .F. ) ;
#8855=VERTEX_POINT ( 'NONE', #3894 ) ;
#8856=CARTESIAN_POINT ( 'NONE',  ( -1.044556982611268170, -28.22896456560694034, -36.05793013899088351 ) ) ;
#8862=LINE ( 'NONE', #214, #5521 ) ;
#8870=CARTESIAN_POINT ( 'NONE',  ( -55.24390624410018802, 0.007503127514282199352, -0.007245494385991655198 ) ) ;
#8877=ADVANCED_FACE ( 'NONE', ( #5925 ), #27832, .F. ) ;
#8880=EDGE_CURVE ( 'NONE', #3267, #20088, #13572, .T. ) ;
#8881=CARTESIAN_POINT ( 'NONE',  ( -1.056502255334265339, 45.80535052436398047, 0.5104472526221617290 ) ) ;
#8888=CARTESIAN_POINT ( 'NONE',  ( -25.21435515916043713, -34.29329011225952684, 4.655591116594705703 ) ) ;
#8902=CARTESIAN_POINT ( 'NONE',  ( -1.583189561560256253, 44.83405390829688741, 11.94859433442855412 ) ) ;
#8903=LINE ( 'NONE', #13194, #14729 ) ;
#8905=CARTESIAN_POINT ( 'NONE',  ( -8.786685647604885574, 6.096987947571466530E-17, -1.524246986892866633E-17 ) ) ;
#8914=EDGE_LOOP ( 'NONE', ( #5237, #4042, #21080, #15314 ) ) ;
#8926=CARTESIAN_POINT ( 'NONE',  ( -25.21435515916043357, 31.17620025257608418, 15.02493970636113474 ) ) ;
#8930=EDGE_CURVE ( 'NONE', #15242, #20933, #5799, .T. ) ;
#8933=EDGE_CURVE ( 'NONE', #18539, #23610, #18460, .T. ) ;
#8934=VERTEX_POINT ( 'NONE', #24359 ) ;
#8945=CARTESIAN_POINT ( 'NONE',  ( -2.904412668506657358, 30.27712468694988601, -36.79926976721460363 ) ) ;
#8950=CARTESIAN_POINT ( 'NONE',  ( -21.41430102051745266, 29.81033373822138799, 7.777552968935449229 ) ) ;
#8955=CARTESIAN_POINT ( 'NONE',  ( -20.20700224038492721, 18.19058640100257662, 23.35150625415638714 ) ) ;
#8956=CARTESIAN_POINT ( 'NONE',  ( -4.780792508754313275, -42.16805077400938728, 25.98388465890126042 ) ) ;
#8957=DIRECTION ( 'NONE',  ( 1.000000000000000000, -6.938893903907226837E-18, 1.734723475976806709E-18 ) ) ;
#8958=CARTESIAN_POINT ( 'NONE',  ( -20.21097721712959938, -17.13687106192361398, -24.14932359587282917 ) ) ;
#8959=CARTESIAN_POINT ( 'NONE',  ( -23.79248802219730052, 30.42578156345387086, -13.25839849636368584 ) ) ;
#8962=CARTESIAN_POINT ( 'NONE',  ( -1.464342487929851222, 44.64187261869797396, 11.94843286121871273 ) ) ;
#8971=CARTESIAN_POINT ( 'NONE',  ( -1.619063947482197729, -46.30105812165550105, -2.489035965909997206 ) ) ;
#8974=ADVANCED_FACE ( 'NONE', ( #9090 ), #11429, .F. ) ;
#8975=CARTESIAN_POINT ( 'NONE',  ( -16.86833981943426508, 38.94907963570754106, 20.94590537750566028 ) ) ;
#8983=VERTEX_POINT ( 'NONE', #4079 ) ;
#8985=DIRECTION ( 'NONE',  ( 0.000000000000000000, 5.223019709708233256E-21, -1.000000000000000000 ) ) ;
#8986=CARTESIAN_POINT ( 'NONE',  ( -1.044557008772710960, 36.05793264791386576, 28.22896138707331204 ) ) ;
#8988=CARTESIAN_POINT ( 'NONE',  ( -2.265401668238146815, 11.98901689611106036, 45.46007138824028004 ) ) ;
#8990=ORIENTED_EDGE ( 'NONE', *, *, #25404, .F. ) ;
#9005=B_SPLINE_CURVE_WITH_KNOTS ( 'NONE', 3,
 ( #11944, #11660, #13663, #17832, #2583, #11367 ),
 .UNSPECIFIED., .F., .F.,
 ( 4, 2, 4 ),
 ( 0.000000000000000000, 0.0004335184443140274431, 0.0008670368886280548863 ),
 .UNSPECIFIED. ) ;
#9011=CARTESIAN_POINT ( 'NONE',  ( -7.078251931573406708, -44.92740138729184451, -26.33626633876207634 ) ) ;
#9014=CARTESIAN_POINT ( 'NONE',  ( -20.20700224038492721, -29.58392382092674211, -0.9908225410477480288 ) ) ;
#9019=CARTESIAN_POINT ( 'NONE',  ( -4.162674018437154899, -48.79210541969629844, -3.424137510344775759 ) ) ;
#9025=EDGE_LOOP ( 'NONE', ( #3817, #7738, #8669, #5846 ) ) ;
#9029=CARTESIAN_POINT ( 'NONE',  ( -9.156249394959713683, -9.022661520477402775, 53.74753343182710807 ) ) ;
#9034=EDGE_CURVE ( 'NONE', #1898, #10065, #28378, .T. ) ;
#9035=VERTEX_POINT ( 'NONE', #8272 ) ;
#9040=CARTESIAN_POINT ( 'NONE',  ( -10.86508079875781263, 9.118642906269942117, 50.32133009257457701 ) ) ;
#9042=ORIENTED_EDGE ( 'NONE', *, *, #16075, .T. ) ;
#9043=CARTESIAN_POINT ( 'NONE',  ( -20.20700224038492365, 10.08426345511628597, 27.82980252387807951 ) ) ;
#9046=CARTESIAN_POINT ( 'NONE',  ( -55.24198130335446422, -0.004163123460805480056, 0.008310594958150618883 ) ) ;
#9047=FACE_OUTER_BOUND ( 'NONE', #21916, .T. ) ;
#9051=DIRECTION ( 'NONE',  ( -0.7563875759206387661, -0.5078650950445656731, 0.4122509917856767570 ) ) ;
#9054=CARTESIAN_POINT ( 'NONE',  ( -4.162674018437141576, 48.79210541969627712, 3.424137510345119484 ) ) ;
#9059=DIRECTION ( 'NONE',  ( 0.000000000000000000, 5.223019709707975211E-21, -1.000000000000000000 ) ) ;
#9062=CARTESIAN_POINT ( 'NONE',  ( -28.13707043255157103, -21.52861750560944998, -7.802116958608919184 ) ) ;
#9063=VERTEX_POINT ( 'NONE', #25241 ) ;
#9068=ORIENTED_EDGE ( 'NONE', *, *, #7854, .F. ) ;
#9073=CARTESIAN_POINT ( 'NONE',  ( -28.41354790283022069, 14.62505768302827036, 18.00456980371883731 ) ) ;
#9076=CARTESIAN_POINT ( 'NONE',  ( -4.780792508754314163, 32.07473752860781246, -37.74278713234406979 ) ) ;
#9078=CARTESIAN_POINT ( 'NONE',  ( -1.049817751779876351, -0.5106138415323642210, 45.79652915392416190 ) ) ;
#9082=CARTESIAN_POINT ( 'NONE',  ( -1.619063947482201282, 43.26576862488434472, -16.67502769180576649 ) ) ;
#9086=CARTESIAN_POINT ( 'NONE',  ( -24.53239521893626218, 33.71193723315153790, 3.868435622621383629 ) ) ;
#9090=FACE_OUTER_BOUND ( 'NONE', #21514, .T. ) ;
#9101=ADVANCED_FACE ( 'NONE', ( #23935 ), #7244, .F. ) ;
#9109=CARTESIAN_POINT ( 'NONE',  ( -8.786685647604931759, 47.14957014837394667, 25.35688121747446999 ) ) ;
#9110=CARTESIAN_POINT ( 'NONE',  ( -20.20700224038492721, 24.51628800869048419, -16.58740185276719359 ) ) ;
#9112=CARTESIAN_POINT ( 'NONE',  ( -4.780792508754321268, -45.80716263181250980, -18.84172549606854119 ) ) ;
#9121=CARTESIAN_POINT ( 'NONE',  ( -55.24390624410018802, -0.01027195578987734684, 0.001811362924359352471 ) ) ;
#9126=ORIENTED_EDGE ( 'NONE', *, *, #16929, .T. ) ;
#9127=CARTESIAN_POINT ( 'NONE',  ( -20.47566338032520861, -29.82700953060484395, 1.586617869344197018 ) ) ;
#9130=ORIENTED_EDGE ( 'NONE', *, *, #7457, .F. ) ;
#9136=EDGE_CURVE ( 'NONE', #14557, #18539, #8803, .T. ) ;
#9138=AXIS2_PLACEMENT_3D ( 'NONE', #10321, #19078, #21371 ) ;
#9141=CARTESIAN_POINT ( 'NONE',  ( -7.711401346138408108, 51.42722225669434266, 10.36923727626067304 ) ) ;
#9143=CARTESIAN_POINT ( 'NONE',  ( -22.34422965417126505, -33.39267070835835227, -17.95715691811035342 ) ) ;
#9145=CARTESIAN_POINT ( 'NONE',  ( -22.23342874802669300, 20.31166691703127114, -24.24669006619380696 ) ) ;
#9150=CARTESIAN_POINT ( 'NONE',  ( -4.178947244162628749, 18.28784278438515543, 45.38689110596700260 ) ) ;
#9163=VERTEX_POINT ( 'NONE', #1888 ) ;
#9164=CARTESIAN_POINT ( 'NONE',  ( -25.21435515916043002, 31.17620025257588523, -15.02493970636157705 ) ) ;
#9165=EDGE_LOOP ( 'NONE', ( #2260, #7100, #25158, #16083 ) ) ;
#9172=LINE ( 'NONE', #27736, #6552 ) ;
#9180=VERTEX_POINT ( 'NONE', #2453 ) ;
#9183=CARTESIAN_POINT ( 'NONE',  ( -19.53423201713130197, 1.355459634611817678E-16, -3.388649086529544194E-17 ) ) ;
#9186=CARTESIAN_POINT ( 'NONE',  ( -1.049817751779889008, 0.5106138415326839652, -45.79652915392414769 ) ) ;
#9195=CARTESIAN_POINT ( 'NONE',  ( -55.24198130335446422, 0.006527480770974009895, 0.006617369590171991688 ) ) ;
#9196=ADVANCED_FACE ( 'NONE', ( #4769 ), #4673, .F. ) ;
#9205=CARTESIAN_POINT ( 'NONE',  ( -1.583189561560253589, 25.21827308671232259, -38.94740041318303270 ) ) ;
#9209=ORIENTED_EDGE ( 'NONE', *, *, #22369, .F. ) ;
#9211=FACE_OUTER_BOUND ( 'NONE', #2879, .T. ) ;
#9213=AXIS2_PLACEMENT_3D ( 'NONE', #16805, #27868, #12598 ) ;
#9215=B_SPLINE_CURVE_WITH_KNOTS ( 'NONE', 3,
 ( #26932, #15997, #7375, #22353, #12226, #16697, #14377, #20031, #22498, #13554, #745, #312, #18287 ),
 .UNSPECIFIED., .F., .F.,
 ( 4, 3, 3, 3, 4 ),
 ( 1.250926888277100149E-17, 0.0007657099931970565501, 0.001531419946797910915, 0.002296279302920149062, 0.003061450627205762869 ),
 .UNSPECIFIED. ) ;
#9224=VERTEX_POINT ( 'NONE', #16277 ) ;
#9228=CARTESIAN_POINT ( 'NONE',  ( -1.046936909428682894, 15.35929614323726256, 43.14407378092978718 ) ) ;
#9233=EDGE_CURVE ( 'NONE', #710, #14740, #12590, .T. ) ;
#9238=ORIENTED_EDGE ( 'NONE', *, *, #17025, .F. ) ;
#9239=VERTEX_POINT ( 'NONE', #25511 ) ;
#9243=CARTESIAN_POINT ( 'NONE',  ( -55.24728320129491266, 0.01362040845703433277, 0.005114031043468512429 ) ) ;
#9246=VERTEX_POINT ( 'NONE', #16564 ) ;
#9251=CARTESIAN_POINT ( 'NONE',  ( -1.049817751779883457, 43.39729912094399822, 14.63752841325003295 ) ) ;
#9252=FACE_OUTER_BOUND ( 'NONE', #2648, .T. ) ;
#9265=ORIENTED_EDGE ( 'NONE', *, *, #12850, .F. ) ;
#9266=CARTESIAN_POINT ( 'NONE',  ( -7.078251931573400491, 44.92740138729166688, -26.33626633876239609 ) ) ;
#9270=CARTESIAN_POINT ( 'NONE',  ( -55.24198130335446422, 0.001516807524704581441, 0.009170435128245077103 ) ) ;
#9271=CARTESIAN_POINT ( 'NONE',  ( -21.41427618760457818, -25.94789270595494202, 16.60878262545447726 ) ) ;
#9286=VERTEX_POINT ( 'NONE', #6739 ) ;
#9290=B_SPLINE_CURVE_WITH_KNOTS ( 'NONE', 3,
 ( #6244, #14994, #8962, #15858, #19888, #24666, #15700, #15992, #2753, #15549 ),
 .UNSPECIFIED., .F., .F.,
 ( 4, 2, 2, 2, 4 ),
 ( 2.168404344971008868E-19, 0.0003346267210630925128, 0.0006692534421261848087, 0.001003880163189277159, 0.001338506884252369401 ),
 .UNSPECIFIED. ) ;
#9291=CARTESIAN_POINT ( 'NONE',  ( -8.786685647604890903, 52.67761315067286176, -9.545808661480789326 ) ) ;
#9299=CARTESIAN_POINT ( 'NONE',  ( -1.046936909428678675, 25.87632113675161349, -37.78538189376516954 ) ) ;
#9306=DIRECTION ( 'NONE',  ( 1.000000000000000000, -6.938893903907226837E-18, 1.734723475976806709E-18 ) ) ;
#9313=CARTESIAN_POINT ( 'NONE',  ( -15.02187109954776290, -45.93032478317472567, -6.234056423739352759 ) ) ;
#9318=CARTESIAN_POINT ( 'NONE',  ( -1.044556982611275497, -15.70482750345265899, -43.01635920718344153 ) ) ;
#9320=ORIENTED_EDGE ( 'NONE', *, *, #2319, .F. ) ;
#9322=ORIENTED_EDGE ( 'NONE', *, *, #4511, .T. ) ;
#9326=CONICAL_SURFACE ( 'NONE', #18041, 34.60786435723138510, 0.8559913436420825139 ) ;
#9337=B_SPLINE_CURVE_WITH_KNOTS ( 'NONE', 3,
 ( #17567, #26355, #4472, #6797, #24356, #20593 ),
 .UNSPECIFIED., .F., .F.,
 ( 4, 2, 4 ),
 ( 0.000000000000000000, 0.0004335151646191496774, 0.0008670303292382993549 ),
 .UNSPECIFIED. ) ;
#9349=LINE ( 'NONE', #16235, #16200 ) ;
#9356=CARTESIAN_POINT ( 'NONE',  ( -22.23226125620942284, 11.82389163795251541, 29.33577758406437042 ) ) ;
#9362=ORIENTED_EDGE ( 'NONE', *, *, #27061, .T. ) ;
#9363=CARTESIAN_POINT ( 'NONE',  ( -12.94347594948484037, 48.30328466416762723, 6.555928820869474372 ) ) ;
#9383=CARTESIAN_POINT ( 'NONE',  ( -1.539760825549693068, 43.19716078875438825, -16.63252404870369006 ) ) ;
#9397=VERTEX_POINT ( 'NONE', #6875 ) ;
#9401=CARTESIAN_POINT ( 'NONE',  ( -1.050229599974464634, 43.47850826583074735, 14.39582765040416668 ) ) ;
#9404=ADVANCED_FACE ( 'NONE', ( #19401 ), #23230, .F. ) ;
#9406=CARTESIAN_POINT ( 'NONE',  ( -20.47566262905010248, -16.24827521404668929, -25.06314747784830388 ) ) ;
#9409=FACE_OUTER_BOUND ( 'NONE', #21153, .T. ) ;
#9413=CARTESIAN_POINT ( 'NONE',  ( -21.41427618760446094, -1.815001260755626733, 30.75468365310880259 ) ) ;
#9418=CARTESIAN_POINT ( 'NONE',  ( -55.24271866751342941, 0.004365563123935787236, 0.008433070970613791573 ) ) ;
#9420=ORIENTED_EDGE ( 'NONE', *, *, #27846, .F. ) ;
#9423=CARTESIAN_POINT ( 'NONE',  ( -20.24419206586952313, -29.61012937815440083, 1.282847120831551280 ) ) ;
#9427=( BOUNDED_SURFACE ( )  B_SPLINE_SURFACE ( 3, 1, ( 
 ( #28090, #23521 ),
 ( #1479, #8254 ),
 ( #10287, #21615 ),
 ( #1617, #23670 ) ),
 .UNSPECIFIED., .F., .F., .F. ) 
 B_SPLINE_SURFACE_WITH_KNOTS ( ( 4, 4 ),
 ( 2, 2 ),
 ( 0.000000000000000000, 1.000000000000000000 ),
 ( 0.000000000000000000, 1.000000000000000000 ),
 .UNSPECIFIED. ) 
 GEOMETRIC_REPRESENTATION_ITEM ( )  RATIONAL_B_SPLINE_SURFACE ( (
 ( 1.000000000000000000, 1.000000000000000000),
 ( 0.7789835883360578528, 0.9689951854195403280),
 ( 0.7789835883360578528, 0.9689951854195403280),
 ( 1.000000000000000000, 1.000000000000000000) ) ) 
 REPRESENTATION_ITEM ( '' )  SURFACE ( )  );
#9435=CARTESIAN_POINT ( 'NONE',  ( -55.24390624410018802, -0.01027195578987978239, -0.001811362924362686826 ) ) ;
#9437=CARTESIAN_POINT ( 'NONE',  ( -23.79223135445720061, 3.207301057648340503, -33.03345552685145492 ) ) ;
#9439=CARTESIAN_POINT ( 'NONE',  ( -20.57838717382308147, 18.89542499756500149, -23.26537097894111383 ) ) ;
#9445=CARTESIAN_POINT ( 'NONE',  ( -5.986830583229317604, -43.56094206392958768, -26.01297580803309728 ) ) ;
#9450=CARTESIAN_POINT ( 'NONE',  ( -25.21435515916043713, 16.39063784838786475, 30.48034229288620622 ) ) ;
#9456=CARTESIAN_POINT ( 'NONE',  ( -20.57838717382308147, -29.92853265176832878, -1.611677988432255848 ) ) ;
#9463=CARTESIAN_POINT ( 'NONE',  ( -55.24271866751342941, -0.001545935011630304593, 0.009369360294295640129 ) ) ;
#9465=VERTEX_POINT ( 'NONE', #20669 ) ;
#9470=CARTESIAN_POINT ( 'NONE',  ( -1.539763995773694827, 16.63252574783043869, -43.19716353142335663 ) ) ;
#9478=ORIENTED_EDGE ( 'NONE', *, *, #9861, .T. ) ;
#9484=CARTESIAN_POINT ( 'NONE',  ( -2.904412668506668460, 47.56768199507434502, 2.864640348250799828 ) ) ;
#9491=CARTESIAN_POINT ( 'NONE',  ( -55.24198130335446422, 0.008310594958151115014, 0.004163123460805739397 ) ) ;
#9496=ORIENTED_EDGE ( 'NONE', *, *, #27041, .F. ) ;
#9499=ORIENTED_EDGE ( 'NONE', *, *, #909, .T. ) ;
#9510=CARTESIAN_POINT ( 'NONE',  ( -12.94347594948480662, 35.22469990145658159, 33.69581619287838947 ) ) ;
#9515=ORIENTED_EDGE ( 'NONE', *, *, #16387, .F. ) ;
#9522=CARTESIAN_POINT ( 'NONE',  ( -55.24271866751342941, -0.009369360294295348696, -0.001545935011630817420 ) ) ;
#9524=CARTESIAN_POINT ( 'NONE',  ( -2.904412668506659578, -36.79926976721470311, -30.27712468694973325 ) ) ;
#9536=CARTESIAN_POINT ( 'NONE',  ( -1.049819825607592794, 43.71263398674771139, 13.66706894614392986 ) ) ;
#9550=CARTESIAN_POINT ( 'NONE',  ( -1.056502255334265339, 0.5104472526220019679, -45.80535052436397336 ) ) ;
#9567=CARTESIAN_POINT ( 'NONE',  ( -8.259864102781675044, 52.06232470801727885, 9.986657004933084281 ) ) ;
#9568=CARTESIAN_POINT ( 'NONE',  ( -8.786685647604890903, 25.35688121747502066, -47.14957014837363403 ) ) ;
#9572=CARTESIAN_POINT ( 'NONE',  ( -25.21435515916025594, 34.29329011225976842, -4.655591116594504086 ) ) ;
#9577=CARTESIAN_POINT ( 'NONE',  ( -1.045287976400379737, 44.00138577190644185, -12.68782741917337198 ) ) ;
#9583=CARTESIAN_POINT ( 'NONE',  ( -55.24390624410018802, 0.004896917417128144288, 0.009209468562451129242 ) ) ;
#9584=( BOUNDED_SURFACE ( )  B_SPLINE_SURFACE ( 3, 1, ( 
 ( #15072, #2250 ),
 ( #23894, #22284 ),
 ( #13490, #11332 ),
 ( #28179, #12920 ) ),
 .UNSPECIFIED., .F., .F., .F. ) 
 B_SPLINE_SURFACE_WITH_KNOTS ( ( 4, 4 ),
 ( 2, 2 ),
 ( 0.000000000000000000, 1.000000000000000000 ),
 ( 0.000000000000000000, 1.000000000000000000 ),
 .UNSPECIFIED. ) 
 GEOMETRIC_REPRESENTATION_ITEM ( )  RATIONAL_B_SPLINE_SURFACE ( (
 ( 1.000000000000000000, 1.000000000000000000),
 ( 0.9934239774497837239, 0.8357310067453919133),
 ( 0.9934239774497837239, 0.8357310067453919133),
 ( 1.000000000000000000, 1.000000000000000000) ) ) 
 REPRESENTATION_ITEM ( '' )  SURFACE ( )  );
#9585=VERTEX_POINT ( 'NONE', #1380 ) ;
#9590=CARTESIAN_POINT ( 'NONE',  ( -1.583189561560252701, -43.29471907393753582, -16.68617981233686365 ) ) ;
#9591=ADVANCED_FACE ( 'NONE', ( #19095 ), #17018, .T. ) ;
#9592=ORIENTED_EDGE ( 'NONE', *, *, #21808, .T. ) ;
#9595=CARTESIAN_POINT ( 'NONE',  ( -55.25297051322618813, -0.01306918787467238607, -0.007247191603129069307 ) ) ;
#9603=CARTESIAN_POINT ( 'NONE',  ( -1.464342487929844783, -38.76467504336602588, -25.15873223207679743 ) ) ;
#9610=CARTESIAN_POINT ( 'NONE',  ( -1.239374126674604337, -44.48112152129338170, 11.92219841463876229 ) ) ;
#9612=EDGE_LOOP ( 'NONE', ( #23976, #26859, #5236, #2889 ) ) ;
#9613=ORIENTED_EDGE ( 'NONE', *, *, #17412, .T. ) ;
#9616=CARTESIAN_POINT ( 'NONE',  ( -55.24271866751342941, 0.006757859501010507128, -0.006671293903668127322 ) ) ;
#9617=CARTESIAN_POINT ( 'NONE',  ( -8.786685647604892679, -53.04920435127177569, 7.199674155859498548 ) ) ;
#9625=CARTESIAN_POINT ( 'NONE',  ( -20.24419206586950892, -23.20105925399712987, 18.44224248888897577 ) ) ;
#9628=CARTESIAN_POINT ( 'NONE',  ( -1.056502255334265339, -36.75727364034752043, -27.33667001641156702 ) ) ;
#9630=CARTESIAN_POINT ( 'NONE',  ( -55.24390624410018802, 0.007503127514278223366, 0.007245494385991344682 ) ) ;
#9640=AXIS2_PLACEMENT_3D ( 'NONE', #19422, #19693, #25773 ) ;
#9642=CARTESIAN_POINT ( 'NONE',  ( -28.13707043255157103, -18.06394523322463641, -14.07296284901326189 ) ) ;
#9654=CARTESIAN_POINT ( 'NONE',  ( -1.050230346682677007, -37.05264119692671443, 26.91946103437146931 ) ) ;
#9659=LINE ( 'NONE', #14241, #11651 ) ;
#9674=ORIENTED_EDGE ( 'NONE', *, *, #12882, .T. ) ;
#9680=LINE ( 'NONE', #25092, #21667 ) ;
#9681=CARTESIAN_POINT ( 'NONE',  ( -28.41354790283022069, 1.249099604787400564, 23.16239616762929288 ) ) ;
#9684=EDGE_CURVE ( 'NONE', #26638, #18375, #28035, .T. ) ;
#9706=AXIS2_PLACEMENT_3D ( 'NONE', #14265, #2924, #18606 ) ;
#9707=EDGE_CURVE ( 'NONE', #9246, #23016, #16730, .T. ) ;
#9715=CIRCLE ( 'NONE', #6500, 53.53553390275978785 ) ;
#9716=EDGE_CURVE ( 'NONE', #14341, #23222, #23502, .T. ) ;
#9718=B_SPLINE_CURVE_WITH_KNOTS ( 'NONE', 3,
 ( #11619, #20533, #18363, #17795 ),
 .UNSPECIFIED., .F., .F.,
 ( 4, 4 ),
 ( 1.906343156168367839E-16, 0.0009910334943227156780 ),
 .UNSPECIFIED. ) ;
#9723=CARTESIAN_POINT ( 'NONE',  ( -1.048171036023497038, -13.17819047681634537, -43.86077206077064261 ) ) ;
#9725=EDGE_CURVE ( 'NONE', #4266, #9035, #8903, .T. ) ;
#9726=VERTEX_POINT ( 'NONE', #7032 ) ;
#9735=EDGE_CURVE ( 'NONE', #1672, #10456, #2623, .T. ) ;
#9749=ORIENTED_EDGE ( 'NONE', *, *, #26566, .T. ) ;
#9751=CARTESIAN_POINT ( 'NONE',  ( -55.24340739397742084, -0.002421372372453905585, -0.009842732675352267036 ) ) ;
#9753=B_SPLINE_CURVE_WITH_KNOTS ( 'NONE', 3,
 ( #13928, #27453, #5152, #3003, #22882, #11785, #9617 ),
 .UNSPECIFIED., .F., .F.,
 ( 4, 3, 4 ),
 ( 0.000000000000000000, 0.006568092053401802279, 0.02506242213020847681 ),
 .UNSPECIFIED. ) ;
#9762=CARTESIAN_POINT ( 'NONE',  ( -1.045287976400362417, -15.59869763335038506, 43.05558670614261985 ) ) ;
#9765=VERTEX_POINT ( 'NONE', #26128 ) ;
#9767=EDGE_CURVE ( 'NONE', #4266, #10555, #27602, .T. ) ;
#9770=DIRECTION ( 'NONE',  ( 1.000000000000000000, -6.938893903907226837E-18, -5.541455922705464902E-20 ) ) ;
#9777=CARTESIAN_POINT ( 'NONE',  ( -55.24300891470650754, 0.009812809446893281523, -0.0003472257464216086005 ) ) ;
#9785=CARTESIAN_POINT ( 'NONE',  ( -20.24399999263414784, 16.36687688782894412, 24.70869149526185282 ) ) ;
#9790=B_SPLINE_CURVE_WITH_KNOTS ( 'NONE', 3,
 ( #6746, #6461, #10642, #28043, #14941, #113 ),
 .UNSPECIFIED., .F., .F.,
 ( 4, 2, 4 ),
 ( 1.528920360908313465E-16, 0.003570751334075640462, 0.007141502668151127400 ),
 .UNSPECIFIED. ) ;
#9791=CARTESIAN_POINT ( 'NONE',  ( -1.113548883309542603, 12.28732181966579695, 44.18588492042577798 ) ) ;
#9792=AXIS2_PLACEMENT_3D ( 'NONE', #6750, #26038, #19828 ) ;
#9803=CARTESIAN_POINT ( 'NONE',  ( -15.02187109954783928, 20.12219089991090115, -41.75590530176315696 ) ) ;
#9809=EDGE_CURVE ( 'NONE', #11495, #11877, #27362, .T. ) ;
#9810=ORIENTED_EDGE ( 'NONE', *, *, #4383, .T. ) ;
#9812=LINE ( 'NONE', #3745, #11620 ) ;
#9814=ADVANCED_FACE ( 'NONE', ( #5246 ), #25978, .F. ) ;
#9816=CARTESIAN_POINT ( 'NONE',  ( -4.162674018437137136, 37.46098494546635038, 31.44946543094254920 ) ) ;
#9820=AXIS2_PLACEMENT_3D ( 'NONE', #3984, #12756, #26145 ) ;
#9821=LINE ( 'NONE', #20888, #23 ) ;
#9829=ORIENTED_EDGE ( 'NONE', *, *, #15631, .T. ) ;
#9850=CARTESIAN_POINT ( 'NONE',  ( -20.20997486282892552, 1.395963739018065216E-16, 29.60348406988233450 ) ) ;
#9852=DIRECTION ( 'NONE',  ( 0.000000000000000000, 5.223019709708233256E-21, -1.000000000000000000 ) ) ;
#9855=ORIENTED_EDGE ( 'NONE', *, *, #3260, .T. ) ;
#9861=EDGE_CURVE ( 'NONE', #4452, #8562, #11440, .T. ) ;
#9863=ADVANCED_FACE ( 'NONE', ( #5531 ), #16217, .F. ) ;
#9864=CARTESIAN_POINT ( 'NONE',  ( -55.24340739397742794, -0.005344433640973866861, 0.008612749836242647450 ) ) ;
#9869=CARTESIAN_POINT ( 'NONE',  ( -1.259972190295308936, 25.19627397134298263, -38.49631882650656678 ) ) ;
#9876=CARTESIAN_POINT ( 'NONE',  ( -1.046935749539997573, -27.93995161054667875, 36.28605774377793125 ) ) ;
#9885=CARTESIAN_POINT ( 'NONE',  ( -55.25297051322618813, -0.001818774723749082148, -0.01483298743814642773 ) ) ;
#9886=CARTESIAN_POINT ( 'NONE',  ( -55.24271866751342941, -0.001425019990781919424, 0.009388511352197656881 ) ) ;
#9891=B_SPLINE_CURVE_WITH_KNOTS ( 'NONE', 3,
 ( #16354, #11612, #22718, #22566, #9895, #20818 ),
 .UNSPECIFIED., .F., .F.,
 ( 4, 2, 4 ),
 ( 0.000000000000000000, 0.0004335151646191517374, 0.0008670303292383034748 ),
 .UNSPECIFIED. ) ;
#9892=B_SPLINE_CURVE_WITH_KNOTS ( 'NONE', 3,
 ( #3465, #27640, #21015, #18425, #18722, #1299, #18868, #16563 ),
 .UNSPECIFIED., .F., .F.,
 ( 4, 2, 2, 4 ),
 ( 0.000000000000000000, 0.002761524886576650645, 0.005523049773153301291, 0.01104609954630661299 ),
 .UNSPECIFIED. ) ;
#9895=CARTESIAN_POINT ( 'NONE',  ( -20.20612091757420004, -27.77903622052264865, -10.22177757278304888 ) ) ;
#9902=CARTESIAN_POINT ( 'NONE',  ( -55.24300891470650754, -0.003362556190412219030, -0.009225237711101438864 ) ) ;
#9910=CARTESIAN_POINT ( 'NONE',  ( -12.82751273423878757, -33.78816682541312844, -35.32125660155435298 ) ) ;
#9914=DIRECTION ( 'NONE',  ( 0.000000000000000000, 5.223019709708116647E-21, -1.000000000000000000 ) ) ;
#9921=FACE_OUTER_BOUND ( 'NONE', #10652, .T. ) ;
#9923=ORIENTED_EDGE ( 'NONE', *, *, #24422, .F. ) ;
#9924=CARTESIAN_POINT ( 'NONE',  ( -21.81686047589425570, 33.92779429964205917, -18.24499610240053116 ) ) ;
#9928=AXIS2_PLACEMENT_3D ( 'NONE', #20289, #860, #26905 ) ;
#9956=CARTESIAN_POINT ( 'NONE',  ( -28.13707043255157103, 7.802116958609002673, -21.52861750560941800 ) ) ;
#9957=B_SPLINE_CURVE_WITH_KNOTS ( 'NONE', 3,
 ( #8043, #18809, #25157, #12326 ),
 .UNSPECIFIED., .F., .F.,
 ( 4, 4 ),
 ( 1.904170172768910460E-16, 0.001982023823822945917 ),
 .UNSPECIFIED. ) ;
#9958=CARTESIAN_POINT ( 'NONE',  ( -1.583189561560256253, -46.33203782964459805, 2.490696082060350314 ) ) ;
#9961=CARTESIAN_POINT ( 'NONE',  ( -1.619063947482197729, 2.489035965910801895, 46.30105812165545842 ) ) ;
#9964=CARTESIAN_POINT ( 'NONE',  ( -1.045287976400365970, -45.76855895860947498, -1.530335034933654859 ) ) ;
#9967=CARTESIAN_POINT ( 'NONE',  ( -12.94347594948484037, -35.22469990145630447, -33.69581619287863106 ) ) ;
#9973=CARTESIAN_POINT ( 'NONE',  ( -21.81686047589426636, -5.181745222995193245, 38.17230180719262478 ) ) ;
#9974=ORIENTED_EDGE ( 'NONE', *, *, #5946, .T. ) ;
#9976=VERTEX_POINT ( 'NONE', #26488 ) ;
#9978=EDGE_CURVE ( 'NONE', #6273, #19910, #8, .T. ) ;
#9992=CARTESIAN_POINT ( 'NONE',  ( -1.259920593601972838, -2.243284667987463621, 45.95412615877144447 ) ) ;
#10002=EDGE_CURVE ( 'NONE', #11368, #9397, #21610, .T. ) ;
#10003=VERTEX_POINT ( 'NONE', #8801 ) ;
#10004=ORIENTED_EDGE ( 'NONE', *, *, #10601, .F. ) ;
#10006=EDGE_CURVE ( 'NONE', #23613, #20885, #19779, .T. ) ;
#10010=CARTESIAN_POINT ( 'NONE',  ( -21.81686047589426991, 37.90526371014259155, -6.867757412720813193 ) ) ;
#10011=CARTESIAN_POINT ( 'NONE',  ( -20.57838717382308147, 23.26537097894132344, 18.89542499756474569 ) ) ;
#10026=CARTESIAN_POINT ( 'NONE',  ( -55.24728320129491266, 0.01214321324516798306, 0.008013189884950450148 ) ) ;
#10033=CARTESIAN_POINT ( 'NONE',  ( -20.20700224038492010, 16.58740185276710832, -24.51628800869052682 ) ) ;
#10036=ORIENTED_EDGE ( 'NONE', *, *, #27227, .T. ) ;
#10037=CARTESIAN_POINT ( 'NONE',  ( -20.20700224038492721, 28.44216453106536946, -8.199606986804427677 ) ) ;
#10038=EDGE_LOOP ( 'NONE', ( #26783, #28158, #6950, #15121, #795, #9238, #9499, #14997, #21748, #24717, #20838, #21490, #3987, #4947, #21659, #16996, #26928, #16852, #12450, #15455, #13755, #24945, #19261, #23446, #3053, #11202, #1526, #26334, #6612, #3292, #9592, #28169, #529, #514, #22418, #20798, #20774, #4832, #24494, #14408, #18881, #3243, #4744, #24018, #13325, #22268, #9855, #21054, #6708, #25848, #1756, #3423, #17217, #23283, #20024, #18858, #19631, #1540, #27913, #6308, #18436, #27128, #6130, #14838 ) ) ;
#10046=ORIENTED_EDGE ( 'NONE', *, *, #5717, .F. ) ;
#10048=CARTESIAN_POINT ( 'NONE',  ( -1.239374126674604337, 38.61989855450939046, -25.08410696974256027 ) ) ;
#10051=ORIENTED_EDGE ( 'NONE', *, *, #23561, .T. ) ;
#10054=CARTESIAN_POINT ( 'NONE',  ( -1.619063947482197729, 2.489035965910159298, -46.30105812165548684 ) ) ;
#10065=VERTEX_POINT ( 'NONE', #4192 ) ;
#10070=EDGE_CURVE ( 'NONE', #15181, #733, #20698, .T. ) ;
#10072=CARTESIAN_POINT ( 'NONE',  ( -55.25297051322618813, 0.007247191603129411047, -0.01306918787467283537 ) ) ;
#10100=DIRECTION ( 'NONE',  ( -1.000000000000000000, 6.938893903907226837E-18, -1.734723475976806709E-18 ) ) ;
#10101=ORIENTED_EDGE ( 'NONE', *, *, #11159, .F. ) ;
#10102=CARTESIAN_POINT ( 'NONE',  ( -15.02187109954786060, -8.264310930412701595, -45.60876405941874623 ) ) ;
#10106=CARTESIAN_POINT ( 'NONE',  ( -8.786685647604885574, 6.069026232697080105E-17, 53.53553390275978785 ) ) ;
#10115=ORIENTED_EDGE ( 'NONE', *, *, #28046, .F. ) ;
#10117=CARTESIAN_POINT ( 'NONE',  ( -9.156249394959713683, 24.29252099376560281, 48.78605533024713026 ) ) ;
#10121=AXIS2_PLACEMENT_3D ( 'NONE', #25179, #20855, #5891 ) ;
#10122=CARTESIAN_POINT ( 'NONE',  ( -1.323439229708125886, 2.317790194800380288, 46.01398008004440499 ) ) ;
#10123=EDGE_LOOP ( 'NONE', ( #17720, #1729, #3794, #3431, #22435, #26984 ) ) ;
#10124=EDGE_CURVE ( 'NONE', #10550, #6273, #14967, .T. ) ;
#10133=CARTESIAN_POINT ( 'NONE',  ( -55.25719721206881729, 0.008651607285660455754, 0.007063345920777159767 ) ) ;
#10137=CARTESIAN_POINT ( 'NONE',  ( -8.786685647604890903, -9.545808661480982948, -52.67761315067281913 ) ) ;
#10153=CARTESIAN_POINT ( 'NONE',  ( -18.41936578851709427, -38.22933728004704790, -18.42310649277614232 ) ) ;
#10154=VECTOR ( 'NONE', #499, 1000.000000000000000 ) ;
#10158=CARTESIAN_POINT ( 'NONE',  ( -22.23226125620930205, 31.55376588768478285, -2.179935373562563061 ) ) ;
#10159=CARTESIAN_POINT ( 'NONE',  ( -1.323439229708128106, -44.47813215539053999, -12.01475235539429143 ) ) ;
#10160=CARTESIAN_POINT ( 'NONE',  ( -8.786685647604885574, 6.096987947571466530E-17, -1.524246986892866633E-17 ) ) ;
#10161=CARTESIAN_POINT ( 'NONE',  ( -20.57838717382308147, -7.715628353033481268, 28.96176188950225949 ) ) ;
#10175=FACE_OUTER_BOUND ( 'NONE', #7127, .T. ) ;
#10177=CARTESIAN_POINT ( 'NONE',  ( -1.583189561560253589, 11.94859433442901597, -44.83405390829675952 ) ) ;
#10178=CARTESIAN_POINT ( 'NONE',  ( -1.464342487929856107, -29.09292098541686755, -35.90631960086405883 ) ) ;
#10182=VECTOR ( 'NONE', #12611, 1000.000000000000000 ) ;
#10192=CARTESIAN_POINT ( 'NONE',  ( -4.473127245936434626, 49.22197550883368677, -3.196405119333975087 ) ) ;
#10194=CARTESIAN_POINT ( 'NONE',  ( -55.24390624410018802, -0.007245494385991085341, 0.007503127514277716827 ) ) ;
#10199=CARTESIAN_POINT ( 'NONE',  ( -1.031422197589711764, 37.93675465142472802, -25.67058493451456158 ) ) ;
#10201=CARTESIAN_POINT ( 'NONE',  ( -28.41354790283022069, 5.969609727608021998, -22.41474081378002836 ) ) ;
#10202=ORIENTED_EDGE ( 'NONE', *, *, #6903, .T. ) ;
#10209=CARTESIAN_POINT ( 'NONE',  ( -20.57838717382308147, -27.96569011373078339, 10.78122205917029675 ) ) ;
#10210=CARTESIAN_POINT ( 'NONE',  ( -2.904412668506669348, -46.12477647685265936, 11.97478724945559136 ) ) ;
#10213=CARTESIAN_POINT ( 'NONE',  ( -21.41427618760457818, 28.68857606049983744, 11.22988868156155640 ) ) ;
#10216=CARTESIAN_POINT ( 'NONE',  ( -1.323830074806776391, -44.47857376182260936, 12.01461446423248169 ) ) ;
#10219=CARTESIAN_POINT ( 'NONE',  ( -20.20700224038492010, 16.58740185276710832, -24.51628800869052682 ) ) ;
#10223=CARTESIAN_POINT ( 'NONE',  ( -7.078251931573400491, -50.86685171665403260, 11.16394717458729957 ) ) ;
#10231=VERTEX_POINT ( 'NONE', #5331 ) ;
#10233=B_SPLINE_CURVE_WITH_KNOTS ( 'NONE', 3,
 ( #9450, #15917, #13467, #24857, #22707, #13748 ),
 .UNSPECIFIED., .F., .F.,
 ( 4, 2, 4 ),
 ( 4.341940435234061368E-16, 0.003576372551511239426, 0.007152745103022045171 ),
 .UNSPECIFIED. ) ;
#10241=EDGE_CURVE ( 'NONE', #3267, #27654, #7089, .T. ) ;
#10243=DIRECTION ( 'NONE',  ( 0.000000000000000000, -5.223019709708233256E-21, 1.000000000000000000 ) ) ;
#10244=CARTESIAN_POINT ( 'NONE',  ( -1.259972190295307382, 28.82609802125311660, 35.85909728507018457 ) ) ;
#10248=CARTESIAN_POINT ( 'NONE',  ( -55.24340739397742084, 0.007744344507855094144, 0.006539691034612383526 ) ) ;
#10254=ORIENTED_EDGE ( 'NONE', *, *, #2162, .T. ) ;
#10258=CARTESIAN_POINT ( 'NONE',  ( -55.25297051322618813, 0.006313402748433540913, -0.01354497706059917470 ) ) ;
#10272=B_SPLINE_CURVE_WITH_KNOTS ( 'NONE', 3,
 ( #24064, #22462, #4456, #4324, #10947, #13368 ),
 .UNSPECIFIED., .F., .F.,
 ( 4, 2, 4 ),
 ( 3.409603294638168262E-16, 0.003576372551511143149, 0.007152745103021945425 ),
 .UNSPECIFIED. ) ;
#10287=CARTESIAN_POINT ( 'NONE',  ( -55.24728320129491266, -0.01402509393918105647, -0.003868537197316873795 ) ) ;
#10288=B_SPLINE_CURVE_WITH_KNOTS ( 'NONE', 3,
 ( #21542, #25876, #14921, #21408, #8319, #12483 ),
 .UNSPECIFIED., .F., .F.,
 ( 4, 2, 4 ),
 ( 1.491862189340054101E-16, 0.003570751334075637860, 0.007141502668151126533 ),
 .UNSPECIFIED. ) ;
#10296=CARTESIAN_POINT ( 'NONE',  ( -20.47566262905010603, 23.19796652405701565, 18.81547655725221091 ) ) ;
#10308=CARTESIAN_POINT ( 'NONE',  ( -1.031422197589716205, -25.67058493451416368, 37.93675465142500514 ) ) ;
#10310=LINE ( 'NONE', #21362, #8395 ) ;
#10312=CARTESIAN_POINT ( 'NONE',  ( -1.619063947482197729, -44.80407745103793360, -11.94059994246142331 ) ) ;
#10318=CARTESIAN_POINT ( 'NONE',  ( -1.056502255334264895, -13.66916755949820583, 43.72121397317236102 ) ) ;
#10320=CARTESIAN_POINT ( 'NONE',  ( -20.20700224038492365, 8.199606986804329978, -28.44216453106539078 ) ) ;
#10321=CARTESIAN_POINT ( 'NONE',  ( -25.21435515916025594, 1.749597353048488237E-16, -4.373993382621220594E-17 ) ) ;
#10327=ORIENTED_EDGE ( 'NONE', *, *, #23843, .T. ) ;
#10335=CARTESIAN_POINT ( 'NONE',  ( -20.20612092514784663, 8.058517256681097862, -28.48192215759668855 ) ) ;
#10338=DIRECTION ( 'NONE',  ( 0.7563875759206388771, 0.5078650950445714463, 0.4122509917856694850 ) ) ;
#10342=CARTESIAN_POINT ( 'NONE',  ( -25.21435515916043002, 34.05351380035335040, -6.169479169075572145 ) ) ;
#10344=CARTESIAN_POINT ( 'NONE',  ( -1.045287976400379737, 44.00138577190644185, -12.68782741917337198 ) ) ;
#10345=CARTESIAN_POINT ( 'NONE',  ( -1.058197053496163109, 28.32422455455077781, -36.00048521498961662 ) ) ;
#10354=ORIENTED_EDGE ( 'NONE', *, *, #12566, .T. ) ;
#10356=DIRECTION ( 'NONE',  ( 5.541455922705464902E-20, -5.223019709708320524E-21, 1.000000000000000000 ) ) ;
#10358=CARTESIAN_POINT ( 'NONE',  ( -55.24198130335446422, -0.004276389980775889554, -0.008252882783650218948 ) ) ;
#10363=ORIENTED_EDGE ( 'NONE', *, *, #23282, .F. ) ;
#10364=CARTESIAN_POINT ( 'NONE',  ( -1.019300379054419725, -28.53917295602924042, -35.83762006677390133 ) ) ;
#10366=EDGE_CURVE ( 'NONE', #23109, #18351, #7953, .T. ) ;
#10370=ADVANCED_FACE ( 'NONE', ( #16716 ), #21, .T. ) ;
#10377=( LENGTH_UNIT ( ) NAMED_UNIT ( * ) SI_UNIT ( .MILLI., .METRE. ) );
#10388=DIRECTION ( 'NONE',  ( 1.000000000000000000, -6.938893903907226837E-18, 1.734723475976806709E-18 ) ) ;
#10389=CARTESIAN_POINT ( 'NONE',  ( -20.21097721650787449, 24.14932365326977148, 17.13687097598110398 ) ) ;
#10405=FACE_OUTER_BOUND ( 'NONE', #25741, .T. ) ;
#10413=CARTESIAN_POINT ( 'NONE',  ( -1.044556982611268614, 45.76404732357880079, -1.643392503292874895 ) ) ;
#10414=CARTESIAN_POINT ( 'NONE',  ( -12.82751273423880001, 21.21958768041857724, 44.03362901246980243 ) ) ;
#10426=CARTESIAN_POINT ( 'NONE',  ( -22.23342874802667879, -29.33662284748868387, -11.82490389046302859 ) ) ;
#10431=CARTESIAN_POINT ( 'NONE',  ( -24.53237795827023859, 6.738475012720130941, -33.25734978085264260 ) ) ;
#10432=EDGE_CURVE ( 'NONE', #24805, #19774, #6619, .T. ) ;
#10450=ADVANCED_FACE ( 'NONE', ( #15645 ), #2777, .T. ) ;
#10453=ORIENTED_EDGE ( 'NONE', *, *, #16319, .T. ) ;
#10455=ADVANCED_FACE ( 'NONE', ( #27165 ), #14375, .F. ) ;
#10456=VERTEX_POINT ( 'NONE', #22297 ) ;
#10460=VERTEX_POINT ( 'NONE', #4729 ) ;
#10466=CARTESIAN_POINT ( 'NONE',  ( -1.049819825607589685, 13.66706894614437928, -43.71263398674757639 ) ) ;
#10469=CARTESIAN_POINT ( 'NONE',  ( -20.20700224038492721, -28.44216453106542986, -8.199606986804219844 ) ) ;
#10476=EDGE_CURVE ( 'NONE', #16572, #194, #5711, .T. ) ;
#10481=CARTESIAN_POINT ( 'NONE',  ( -1.044557008772714068, -44.03203053429562885, 12.57891310333395118 ) ) ;
#10485=EDGE_CURVE ( 'NONE', #2734, #26638, #533, .T. ) ;
#10486=CARTESIAN_POINT ( 'NONE',  ( -4.473127245936431073, -47.80062405537792358, 12.17046501147566318 ) ) ;
#10495=CARTESIAN_POINT ( 'NONE',  ( -1.113548883309550153, -35.91246368318222437, -28.52482525634933097 ) ) ;
#10508=CARTESIAN_POINT ( 'NONE',  ( -1.044556982611270612, 28.22896456560720679, 36.05793013899066324 ) ) ;
#10510=B_SPLINE_CURVE_WITH_KNOTS ( 'NONE', 3,
 ( #11988, #18302, #2931, #20908, #9413, #1197 ),
 .UNSPECIFIED., .F., .F.,
 ( 4, 2, 4 ),
 ( 4.114075111014854645E-16, 0.003576372551511222079, 0.007152745103022032161 ),
 .UNSPECIFIED. ) ;
#10530=ORIENTED_EDGE ( 'NONE', *, *, #10601, .T. ) ;
#10532=ORIENTED_EDGE ( 'NONE', *, *, #1189, .F. ) ;
#10542=DIRECTION ( 'NONE',  ( -0.7071067818211355105, 4.902845705138443504E-18, 0.7071067805519596350 ) ) ;
#10550=VERTEX_POINT ( 'NONE', #2411 ) ;
#10551=( BOUNDED_SURFACE ( )  B_SPLINE_SURFACE ( 3, 1, ( 
 ( #16344, #14173 ),
 ( #14321, #20944 ),
 ( #14468, #23141 ),
 ( #1650, #1231 ) ),
 .UNSPECIFIED., .F., .F., .F. ) 
 B_SPLINE_SURFACE_WITH_KNOTS ( ( 4, 4 ),
 ( 2, 2 ),
 ( 0.000000000000000000, 1.000000000000000000 ),
 ( 0.000000000000000000, 1.000000000000000000 ),
 .UNSPECIFIED. ) 
 GEOMETRIC_REPRESENTATION_ITEM ( )  RATIONAL_B_SPLINE_SURFACE ( (
 ( 1.000000000000000000, 1.000000000000000000),
 ( 0.9593753223639863714, 0.9995975284513187731),
 ( 0.9593753223639863714, 0.9995975284513187731),
 ( 1.000000000000000000, 1.000000000000000000) ) ) 
 REPRESENTATION_ITEM ( '' )  SURFACE ( )  );
#10555=VERTEX_POINT ( 'NONE', #11922 ) ;
#10556=ORIENTED_EDGE ( 'NONE', *, *, #21882, .F. ) ;
#10560=CARTESIAN_POINT ( 'NONE',  ( -24.53239521893645048, 29.54733954334105661, -16.68574937150984638 ) ) ;
#10563=EDGE_CURVE ( 'NONE', #3225, #10550, #10847, .T. ) ;
#10564=CARTESIAN_POINT ( 'NONE',  ( 180.4657679828686980, -20.00000000000000000, 3.130582043300658722E-16 ) ) ;
#10575=CARTESIAN_POINT ( 'NONE',  ( -55.24198130335446422, 0.001391250620105636670, -0.009190321388309047670 ) ) ;
#10576=CARTESIAN_POINT ( 'NONE',  ( -55.25297051322618813, 0.01306918787467630481, -0.007247191603131783282 ) ) ;
#10580=CARTESIAN_POINT ( 'NONE',  ( -20.21097721712959583, -17.67178718142840665, 23.76068428613700334 ) ) ;
#10584=CARTESIAN_POINT ( 'NONE',  ( -1.031422197589716205, 15.60268798220638509, -43.06660437151315080 ) ) ;
#10586=ORIENTED_EDGE ( 'NONE', *, *, #6932, .F. ) ;
#10587=( BOUNDED_SURFACE ( )  B_SPLINE_SURFACE ( 3, 1, ( 
 ( #8870, #12605 ),
 ( #17209, #19228 ),
 ( #13166, #12880 ),
 ( #28003, #17629 ) ),
 .UNSPECIFIED., .F., .F., .F. ) 
 B_SPLINE_SURFACE_WITH_KNOTS ( ( 4, 4 ),
 ( 2, 2 ),
 ( 0.000000000000000000, 1.000000000000000000 ),
 ( 0.000000000000000000, 1.000000000000000000 ),
 .UNSPECIFIED. ) 
 GEOMETRIC_REPRESENTATION_ITEM ( )  RATIONAL_B_SPLINE_SURFACE ( (
 ( 1.000000000000000000, 1.000000000000000000),
 ( 0.7789835883360576307, 0.9689951854195403280),
 ( 0.7789835883360576307, 0.9689951854195403280),
 ( 1.000000000000000000, 1.000000000000000000) ) ) 
 REPRESENTATION_ITEM ( '' )  SURFACE ( )  );
#10591=AXIS2_PLACEMENT_3D ( 'NONE', #14782, #2228, #17223 ) ;
#10596=EDGE_CURVE ( 'NONE', #8511, #21937, #24574, .T. ) ;
#10599=CARTESIAN_POINT ( 'NONE',  ( -1.048996300304495310, 13.42280206896976757, -43.78665266739842110 ) ) ;
#10601=EDGE_CURVE ( 'NONE', #4557, #13961, #3957, .T. ) ;
#10604=CARTESIAN_POINT ( 'NONE',  ( -20.20612091757426043, 24.59769958242388910, -16.46550228026404028 ) ) ;
#10609=LINE ( 'NONE', #19377, #27734 ) ;
#10615=VERTEX_POINT ( 'NONE', #984 ) ;
#10616=CARTESIAN_POINT ( 'NONE',  ( -1.583189561560255143, 2.490696082059864924, -46.33203782964461936 ) ) ;
#10618=CARTESIAN_POINT ( 'NONE',  ( -55.24271866751342941, 0.004256484107795918508, -0.008488649505343059953 ) ) ;
#10619=CARTESIAN_POINT ( 'NONE',  ( -22.23226125620929139, -31.55376588768476509, 2.179935373562780221 ) ) ;
#10624=CARTESIAN_POINT ( 'NONE',  ( -25.21435515916043357, -15.02493970636125198, 31.17620025257602379 ) ) ;
#10629=( BOUNDED_SURFACE ( )  B_SPLINE_SURFACE ( 3, 1, ( 
 ( #18355, #22714 ),
 ( #9595, #27138 ),
 ( #7164, #16207 ),
 ( #22856, #15569 ) ),
 .UNSPECIFIED., .F., .F., .F. ) 
 B_SPLINE_SURFACE_WITH_KNOTS ( ( 4, 4 ),
 ( 2, 2 ),
 ( 0.000000000000000000, 1.000000000000000000 ),
 ( 0.000000000000000000, 1.000000000000000000 ),
 .UNSPECIFIED. ) 
 GEOMETRIC_REPRESENTATION_ITEM ( )  RATIONAL_B_SPLINE_SURFACE ( (
 ( 1.000000000000000000, 1.000000000000000000),
 ( 0.7789835883360578528, 0.9689951854195403280),
 ( 0.7789835883360578528, 0.9689951854195403280),
 ( 1.000000000000000000, 1.000000000000000000) ) ) 
 REPRESENTATION_ITEM ( '' )  SURFACE ( )  );
#10633=EDGE_CURVE ( 'NONE', #27511, #4864, #1410, .T. ) ;
#10634=VERTEX_POINT ( 'NONE', #25736 ) ;
#10636=CARTESIAN_POINT ( 'NONE',  ( -1.045287976400362417, 37.92705037016796155, 25.66401692419947977 ) ) ;
#10638=EDGE_CURVE ( 'NONE', #18596, #25142, #18008, .T. ) ;
#10642=CARTESIAN_POINT ( 'NONE',  ( -22.23226125620943705, 16.78323347921918796, -26.80886670319641851 ) ) ;
#10649=CARTESIAN_POINT ( 'NONE',  ( -20.24419206586954090, -10.37009329716784656, -27.76448493191440292 ) ) ;
#10651=AXIS2_PLACEMENT_3D ( 'NONE', #12113, #1172, #24793 ) ;
#10652=EDGE_LOOP ( 'NONE', ( #10051, #16919, #9749, #14817 ) ) ;
#10660=CARTESIAN_POINT ( 'NONE',  ( -55.25719721206881729, -0.008651607285660899843, 0.007063345920781139223 ) ) ;
#10667=B_SPLINE_CURVE_WITH_KNOTS ( 'NONE', 3,
 ( #13609, #515, #25138, #27278, #7156, #5408, #7291 ),
 .UNSPECIFIED., .F., .F.,
 ( 4, 3, 4 ),
 ( 0.000000000000000000, 0.006568092053401818758, 0.02506242213020845946 ),
 .UNSPECIFIED. ) ;
#10676=CARTESIAN_POINT ( 'NONE',  ( -22.23226125620944771, -16.78323347921898900, 26.80886670319655707 ) ) ;
#10677=CARTESIAN_POINT ( 'NONE',  ( -25.21435515916025594, 1.749597353048488237E-16, -4.373993382621220594E-17 ) ) ;
#10690=CARTESIAN_POINT ( 'NONE',  ( -1.050230347699842248, -0.2550051351976088121, -45.79907861674080749 ) ) ;
#10692=CARTESIAN_POINT ( 'NONE',  ( -55.24390624410018802, -0.01027195578987734684, 0.001811362924359352471 ) ) ;
#10700=CARTESIAN_POINT ( 'NONE',  ( -1.050229599974477068, 45.79907399707867199, 0.2556477501661113538 ) ) ;
#10702=VERTEX_POINT ( 'NONE', #17354 ) ;
#10707=CARTESIAN_POINT ( 'NONE',  ( -25.21435515916043002, 30.48034229288640162, -16.39063784838753790 ) ) ;
#10709=EDGE_CURVE ( 'NONE', #9246, #14330, #16579, .T. ) ;
#10717=CARTESIAN_POINT ( 'NONE',  ( -15.02187109954795119, 6.234056423739480657, -45.93032478317444856 ) ) ;
#10719=ORIENTED_EDGE ( 'NONE', *, *, #15354, .F. ) ;
#10723=FACE_OUTER_BOUND ( 'NONE', #19887, .T. ) ;
#10732=CARTESIAN_POINT ( 'NONE',  ( -1.048996300304505747, -37.49570739463903379, -26.29666317565288480 ) ) ;
#10733=ORIENTED_EDGE ( 'NONE', *, *, #15184, .F. ) ;
#10734=ORIENTED_EDGE ( 'NONE', *, *, #20336, .T. ) ;
#10736=EDGE_CURVE ( 'NONE', #15797, #22192, #19787, .T. ) ;
#10737=ORIENTED_EDGE ( 'NONE', *, *, #28165, .T. ) ;
#10741=EDGE_CURVE ( 'NONE', #26085, #18255, #18882, .T. ) ;
#10747=CARTESIAN_POINT ( 'NONE',  ( -22.23342874802668234, -11.82490389046295043, 29.33662284748872651 ) ) ;
#10756=CARTESIAN_POINT ( 'NONE',  ( -25.21435515916025594, 1.749597353048488237E-16, -4.373993382621220594E-17 ) ) ;
#10767=CARTESIAN_POINT ( 'NONE',  ( -1.019300379054419947, -2.023851374322355845, 45.76814864815092676 ) ) ;
#10777=DIRECTION ( 'NONE',  ( -0.7637818620346800147, -0.6201872550346679835, -0.1788995134688763367 ) ) ;
#10778=VERTEX_POINT ( 'NONE', #659 ) ;
#10779=CARTESIAN_POINT ( 'NONE',  ( -1.044557008772710516, -36.05793264791363129, -28.22896138707358205 ) ) ;
#10783=FACE_OUTER_BOUND ( 'NONE', #8550, .T. ) ;
#10787=CARTESIAN_POINT ( 'NONE',  ( -2.265401668238148591, 2.645701981445804929, -46.93990709177545995 ) ) ;
#10791=CARTESIAN_POINT ( 'NONE',  ( -55.24271866751342941, 0.009369360294296127586, 0.001545935011630553526 ) ) ;
#10793=ORIENTED_EDGE ( 'NONE', *, *, #6410, .F. ) ;
#10794=EDGE_LOOP ( 'NONE', ( #18183, #25979, #7295, #10004 ) ) ;
#10802=ORIENTED_EDGE ( 'NONE', *, *, #8880, .F. ) ;
#10806=EDGE_CURVE ( 'NONE', #21774, #11861, #21182, .T. ) ;
#10809=( BOUNDED_SURFACE ( )  B_SPLINE_SURFACE ( 3, 1, ( 
 ( #10692, #28226 ),
 ( #8528, #17290 ),
 ( #6365, #15117 ),
 ( #13116, #8804 ) ),
 .UNSPECIFIED., .F., .F., .F. ) 
 B_SPLINE_SURFACE_WITH_KNOTS ( ( 4, 4 ),
 ( 2, 2 ),
 ( 0.000000000000000000, 1.000000000000000000 ),
 ( 0.000000000000000000, 1.000000000000000000 ),
 .UNSPECIFIED. ) 
 GEOMETRIC_REPRESENTATION_ITEM ( )  RATIONAL_B_SPLINE_SURFACE ( (
 ( 1.000000000000000000, 1.000000000000000000),
 ( 0.9934239774497837239, 0.8357310067453919133),
 ( 0.9934239774497837239, 0.8357310067453919133),
 ( 1.000000000000000000, 1.000000000000000000) ) ) 
 REPRESENTATION_ITEM ( '' )  SURFACE ( )  );
#10815=B_SPLINE_CURVE_WITH_KNOTS ( 'NONE', 3,
 ( #20883, #5332, #13966, #12108, #5480, #22921, #16127, #9961 ),
 .UNSPECIFIED., .F., .F.,
 ( 4, 2, 2, 4 ),
 ( 0.000000000000000000, 0.002761524886576651946, 0.005523049773153303893, 0.01104609954630660952 ),
 .UNSPECIFIED. ) ;
#10816=EDGE_CURVE ( 'NONE', #26927, #12310, #18426, .T. ) ;
#10818=ORIENTED_EDGE ( 'NONE', *, *, #6948, .F. ) ;
#10819=CARTESIAN_POINT ( 'NONE',  ( -20.57838717382308147, -10.78122205917020437, -27.96569011373082603 ) ) ;
#10821=CARTESIAN_POINT ( 'NONE',  ( -55.24271866751342941, 0.009388511352198142604, 0.001425019990782173561 ) ) ;
#10826=CARTESIAN_POINT ( 'NONE',  ( -1.046936909428682450, -43.93225665392624535, -12.93351869073256388 ) ) ;
#10827=CARTESIAN_POINT ( 'NONE',  ( -25.21435515916043357, 6.169479169075458458, -34.05351380035335751 ) ) ;
#10834=CARTESIAN_POINT ( 'NONE',  ( -20.20700224038492010, -10.08426345511570332, 27.82980252387829623 ) ) ;
#10836=CARTESIAN_POINT ( 'NONE',  ( -23.79223135445719706, -16.82181692922836547, -28.60983116549958538 ) ) ;
#10847=B_SPLINE_CURVE_WITH_KNOTS ( 'NONE', 3,
 ( #3559, #5744, #23174, #16377, #10213, #18973 ),
 .UNSPECIFIED., .F., .F.,
 ( 4, 2, 4 ),
 ( 4.679414566804424472E-16, 0.003576372551511269784, 0.007152745103022071192 ),
 .UNSPECIFIED. ) ;
#10851=CARTESIAN_POINT ( 'NONE',  ( -8.786685647604890903, -23.24040270374424466, -48.22796981442760256 ) ) ;
#10855=CARTESIAN_POINT ( 'NONE',  ( -10.86508079875801691, 6.877801422380844798, -50.67624451685624365 ) ) ;
#10860=CARTESIAN_POINT ( 'NONE',  ( -55.24198130335446422, -0.008252882783649790471, 0.004276389980776089048 ) ) ;
#10861=CARTESIAN_POINT ( 'NONE',  ( -6.588769196390771299, 11.07780292579764847, 50.13301368233286581 ) ) ;
#10862=CARTESIAN_POINT ( 'NONE',  ( -1.113548883309555482, -42.96943836789115778, -16.03115934825511957 ) ) ;
#10863=CARTESIAN_POINT ( 'NONE',  ( -23.79223135445719350, -28.60983116549952143, 16.82181692922848626 ) ) ;
#10865=CARTESIAN_POINT ( 'NONE',  ( -7.078251931573400491, 34.59014398252916322, -38.93060825814240644 ) ) ;
#10871=EDGE_CURVE ( 'NONE', #26876, #7314, #18789, .T. ) ;
#10872=CARTESIAN_POINT ( 'NONE',  ( -8.786685647604890903, -9.545808661480982948, -52.67761315067281913 ) ) ;
#10874=CARTESIAN_POINT ( 'NONE',  ( -23.77929240705206837, -32.66578242509734054, 15.74261278740706338 ) ) ;
#10878=EDGE_CURVE ( 'NONE', #1317, #8855, #15660, .T. ) ;
#10882=CARTESIAN_POINT ( 'NONE',  ( -4.473127245936434626, -41.70021447285072469, -26.34600523034523434 ) ) ;
#10885=B_SPLINE_CURVE_WITH_KNOTS ( 'NONE', 3,
 ( #26815, #8986, #4657, #13424, #22224, #7549, #25539, #7989, #5512, #18904 ),
 .UNSPECIFIED., .F., .F.,
 ( 4, 2, 2, 2, 4 ),
 ( 2.976713740813343128E-16, 0.0003346187017559132675, 0.0006692374035115289214, 0.001003856105267144630, 0.001338474807022760121 ),
 .UNSPECIFIED. ) ;
#10893=CARTESIAN_POINT ( 'NONE',  ( -1.031422197589716205, 45.78027046666444733, -1.530725436377611715 ) ) ;
#10904=ORIENTED_EDGE ( 'NONE', *, *, #20434, .T. ) ;
#10906=FACE_OUTER_BOUND ( 'NONE', #22104, .T. ) ;
#10915=DIRECTION ( 'NONE',  ( -1.000000000000000000, 6.938893903907226837E-18, -1.734723475976806709E-18 ) ) ;
#10919=CARTESIAN_POINT ( 'NONE',  ( -2.904412668506655582, 2.864640348250632851, -47.56768199507435213 ) ) ;
#10929=CARTESIAN_POINT ( 'NONE',  ( -8.786685647604896232, 9.545808661481343549, 52.67761315067276229 ) ) ;
#10939=FACE_OUTER_BOUND ( 'NONE', #1070, .T. ) ;
#10942=CARTESIAN_POINT ( 'NONE',  ( -25.21435515916025594, 34.29329011225976132, 4.655591116594488099 ) ) ;
#10945=VERTEX_POINT ( 'NONE', #942 ) ;
#10947=CARTESIAN_POINT ( 'NONE',  ( -21.41427618760458884, 11.22988868156184772, -28.68857606049970244 ) ) ;
#10950=AXIS2_PLACEMENT_3D ( 'NONE', #7959, #28062, #21163 ) ;
#10951=EDGE_CURVE ( 'NONE', #10065, #23186, #25806, .T. ) ;
#10961=CARTESIAN_POINT ( 'NONE',  ( -8.786685647604885574, 6.096987947571466530E-17, -1.524246986892866633E-17 ) ) ;
#10962=CARTESIAN_POINT ( 'NONE',  ( -5.986830583229481029, 26.01297580803325360, -43.56094206392965873 ) ) ;
#10971=CIRCLE ( 'NONE', #28406, 20.00000000000000000 ) ;
#10973=ORIENTED_EDGE ( 'NONE', *, *, #28160, .F. ) ;
#10975=ORIENTED_EDGE ( 'NONE', *, *, #8707, .F. ) ;
#10976=CARTESIAN_POINT ( 'NONE',  ( -8.786685647604892679, -53.04920435127177569, 7.199674155859498548 ) ) ;
#10978=ORIENTED_EDGE ( 'NONE', *, *, #27825, .F. ) ;
#10979=EDGE_LOOP ( 'NONE', ( #23553, #13398, #6553, #18440 ) ) ;
#10983=ADVANCED_FACE ( 'NONE', ( #4225 ), #2598, .F. ) ;
#10984=EDGE_CURVE ( 'NONE', #26085, #13800, #13264, .T. ) ;
#10986=CARTESIAN_POINT ( 'NONE',  ( -1.463510566862831208, -46.14841196428341874, -2.430838777910016901 ) ) ;
#10990=CARTESIAN_POINT ( 'NONE',  ( -1.463510566862832984, 43.13857742234528558, 16.57250862017374970 ) ) ;
#10998=CARTESIAN_POINT ( 'NONE',  ( -55.25297051322618813, 0.01019003092403517226, 0.01093108995494820879 ) ) ;
#11006=CARTESIAN_POINT ( 'NONE',  ( -20.21097721650786738, -17.13687097598118925, 24.14932365326971464 ) ) ;
#11007=CARTESIAN_POINT ( 'NONE',  ( -1.050229599974477734, -26.71319688967661676, -37.20249516760164710 ) ) ;
#11024=CARTESIAN_POINT ( 'NONE',  ( -1.048172774974287291, 13.17853518375297739, -43.86067135048624266 ) ) ;
#11033=CARTESIAN_POINT ( 'NONE',  ( -12.94347594948485103, 23.08810053288751263, 42.93165645342833869 ) ) ;
#11041=CARTESIAN_POINT ( 'NONE',  ( -4.473127245936431073, 26.34600523034598396, 41.70021447285024863 ) ) ;
#11043=CARTESIAN_POINT ( 'NONE',  ( -1.259920593601974392, 45.95412615877143026, 2.243284667987943681 ) ) ;
#11049=ADVANCED_FACE ( 'NONE', ( #10723 ), #24133, .F. ) ;
#11050=ORIENTED_EDGE ( 'NONE', *, *, #26238, .T. ) ;
#11057=ORIENTED_EDGE ( 'NONE', *, *, #7388, .F. ) ;
#11058=CARTESIAN_POINT ( 'NONE',  ( -55.24198130335446422, 0.009190321388310579431, -0.001391250620101621869 ) ) ;
#11062=ORIENTED_EDGE ( 'NONE', *, *, #375, .T. ) ;
#11065=CARTESIAN_POINT ( 'NONE',  ( -20.37983603106074071, 28.74620395171562492, -7.753708011498657626 ) ) ;
#11066=CARTESIAN_POINT ( 'NONE',  ( -20.57838717382308147, -7.715628353033886278, -28.96176188950215646 ) ) ;
#11067=AXIS2_PLACEMENT_3D ( 'NONE', #8905, #12921, #2251 ) ;
#11072=CARTESIAN_POINT ( 'NONE',  ( -55.24198130335446422, 0.009190321388309335635, 0.001391250620105184774 ) ) ;
#11074=STYLED_ITEM('',(#28528),#17192);
#11076=FACE_OUTER_BOUND ( 'NONE', #11253, .T. ) ;
#11081=CARTESIAN_POINT ( 'NONE',  ( -55.25719721206881729, -0.004044147484877910065, -0.01041086141212526316 ) ) ;
#11085=ORIENTED_EDGE ( 'NONE', *, *, #11835, .T. ) ;
#11096=CARTESIAN_POINT ( 'NONE',  ( -1.113548883309547044, -12.28732181966548609, -44.18588492042589166 ) ) ;
#11102=CARTESIAN_POINT ( 'NONE',  ( -1.619063947482197729, -2.489035965910479486, -46.30105812165547974 ) ) ;
#11104=CARTESIAN_POINT ( 'NONE',  ( -20.38016308990358638, 18.69911008768368532, 23.16952666206563549 ) ) ;
#11126=CARTESIAN_POINT ( 'NONE',  ( -1.113548883309553927, -45.82026503946952545, -1.968251867498708174 ) ) ;
#11129=CARTESIAN_POINT ( 'NONE',  ( -23.77929240705206482, 31.93650644494365309, 17.17389748746929001 ) ) ;
#11133=CARTESIAN_POINT ( 'NONE',  ( -18.41936578851717599, 5.707900577128148356, -42.05131332928112187 ) ) ;
#11135=ORIENTED_EDGE ( 'NONE', *, *, #14150, .F. ) ;
#11136=EDGE_LOOP ( 'NONE', ( #25562, #2467, #9496, #18122 ) ) ;
#11138=FACE_OUTER_BOUND ( 'NONE', #17601, .T. ) ;
#11140=CARTESIAN_POINT ( 'NONE',  ( -20.20898968516257810, -0.6607166829021660082, -29.59696826051172280 ) ) ;
#11141=CARTESIAN_POINT ( 'NONE',  ( -8.786685647604887350, 53.04920435127183254, 7.199674155859139724 ) ) ;
#11147=CARTESIAN_POINT ( 'NONE',  ( -1.045287976400362417, -28.14015102489855735, -36.12803364096578207 ) ) ;
#11149=B_SPLINE_CURVE_WITH_KNOTS ( 'NONE', 3,
 ( #25230, #27222, #1190, #22798, #753, #22942, #7248, #3481 ),
 .UNSPECIFIED., .F., .F.,
 ( 4, 2, 2, 4 ),
 ( 2.211348276820754320E-16, 0.002761568181852866368, 0.005523136363705511559, 0.01104627272741080107 ),
 .UNSPECIFIED. ) ;
#11153=CONICAL_SURFACE ( 'NONE', #7489, 34.60786435723138510, 0.8559913436420825139 ) ;
#11159=EDGE_CURVE ( 'NONE', #565, #19578, #10885, .T. ) ;
#11164=AXIS2_PLACEMENT_3D ( 'NONE', #20567, #20989, #24908 ) ;
#11167=CARTESIAN_POINT ( 'NONE',  ( -20.20700224038492721, -16.58740185276692358, 24.51628800869065827 ) ) ;
#11175=CARTESIAN_POINT ( 'NONE',  ( -25.21435515916043713, 4.655591116594827383, 34.29329011225949841 ) ) ;
#11176=CARTESIAN_POINT ( 'NONE',  ( -20.20700224038492721, -28.44216453106531617, 8.199606986804630182 ) ) ;
#11178=CARTESIAN_POINT ( 'NONE',  ( -16.86833981943427929, 5.948101187262172296, 43.82216161736197790 ) ) ;
#11191=CARTESIAN_POINT ( 'NONE',  ( -55.25297051322618813, 0.001818774723749745246, 0.01483298743814625079 ) ) ;
#11192=CARTESIAN_POINT ( 'NONE',  ( -9.156249394959706578, 9.022661520478530761, 53.74753343182691623 ) ) ;
#11197=ORIENTED_EDGE ( 'NONE', *, *, #15354, .T. ) ;
#11200=CARTESIAN_POINT ( 'NONE',  ( -1.046936909428695328, 43.14407378092994350, -15.35929614323679893 ) ) ;
#11202=ORIENTED_EDGE ( 'NONE', *, *, #14433, .T. ) ;
#11207=CARTESIAN_POINT ( 'NONE',  ( -1.045287976400379737, -37.92705037016725100, 25.66401692420055269 ) ) ;
#11208=CARTESIAN_POINT ( 'NONE',  ( -55.24271866751342941, -0.004256484107795216812, 0.008488649505342837909 ) ) ;
#11214=FACE_BOUND ( 'NONE', #20491, .T. ) ;
#11220=CARTESIAN_POINT ( 'NONE',  ( -15.02187109954785171, 45.93032478317463330, 6.234056423739666286 ) ) ;
#11222=CARTESIAN_POINT ( 'NONE',  ( -9.156249394959713683, 25.18996226954615736, -48.32878616081018208 ) ) ;
#11223=ORIENTED_EDGE ( 'NONE', *, *, #25339, .T. ) ;
#11228=DIRECTION ( 'NONE',  ( -0.7637818620346800147, 0.6201872550346668733, 0.1788995134688804445 ) ) ;
#11230=CARTESIAN_POINT ( 'NONE',  ( -4.780792508754318604, 18.84172549606871883, -45.80716263181242454 ) ) ;
#11234=CARTESIAN_POINT ( 'NONE',  ( -1.463510566862832762, -11.94877850058534285, -44.64091840826485935 ) ) ;
#11242=CARTESIAN_POINT ( 'NONE',  ( -1.323439229708126774, -12.01475235539415642, 44.47813215539056131 ) ) ;
#11244=EDGE_CURVE ( 'NONE', #18571, #13110, #8828, .T. ) ;
#11248=CARTESIAN_POINT ( 'NONE',  ( -20.21097721650787093, -8.835581399094968091, 28.26295598655181607 ) ) ;
#11250=DIRECTION ( 'NONE',  ( 1.000000000000000000, -6.938893903907226837E-18, 1.734723475976806709E-18 ) ) ;
#11253=EDGE_LOOP ( 'NONE', ( #27997, #10363, #12319, #8538 ) ) ;
#11256=CARTESIAN_POINT ( 'NONE',  ( -55.24390624410018802, 0.01032895241567037548, -0.001451500391950801341 ) ) ;
#11258=EDGE_LOOP ( 'NONE', ( #19293, #7159, #22934, #1440 ) ) ;
#11270=DIRECTION ( 'NONE',  ( 0.000000000000000000, 5.223019709707975211E-21, -1.000000000000000000 ) ) ;
#11273=EDGE_CURVE ( 'NONE', #17203, #3442, #920, .T. ) ;
#11274=CARTESIAN_POINT ( 'NONE',  ( -1.155031165708890306, 12.20332162035463419, -44.25214473648917135 ) ) ;
#11292=EDGE_LOOP ( 'NONE', ( #7907, #14739, #5520, #14556 ) ) ;
#11294=ORIENTED_EDGE ( 'NONE', *, *, #1361, .F. ) ;
#11297=CARTESIAN_POINT ( 'NONE',  ( -1.048994561756802169, 36.59609844253166244, 27.53485040342854262 ) ) ;
#11306=ADVANCED_FACE ( 'NONE', ( #12828 ), #9427, .F. ) ;
#11315=CARTESIAN_POINT ( 'NONE',  ( -8.786685647604890903, -53.04920435127188938, -7.199674155858766689 ) ) ;
#11317=B_SPLINE_CURVE_WITH_KNOTS ( 'NONE', 3,
 ( #17165, #2168, #5962, #12562, #19189, #8258, #17017, #25815, #3929, #25955 ),
 .UNSPECIFIED., .F., .F.,
 ( 4, 2, 2, 2, 4 ),
 ( 8.299636676276019848E-18, 0.0003346267210630991806, 0.0006692534421261901213, 0.001003880163189280845, 0.001338506884252371786 ),
 .UNSPECIFIED. ) ;
#11321=CARTESIAN_POINT ( 'NONE',  ( -20.47566338032515887, -28.85746366088576664, -7.708089572830313152 ) ) ;
#11326=VERTEX_POINT ( 'NONE', #1751 ) ;
#11331=DIRECTION ( 'NONE',  ( -0.7563875759206389882, -0.3556158456312901173, 0.5490129373055266937 ) ) ;
#11332=CARTESIAN_POINT ( 'NONE',  ( -1.019300379054419947, -42.90269154183439326, -16.06793277091975369 ) ) ;
#11333=CARTESIAN_POINT ( 'NONE',  ( -1.045287976400365970, 15.59869763335068171, -43.05558670614252037 ) ) ;
#11338=CARTESIAN_POINT ( 'NONE',  ( -55.24340739397742794, 0.005344433640974572026, -0.008612749836242874699 ) ) ;
#11339=CARTESIAN_POINT ( 'NONE',  ( -28.41354790283022069, 5.969609727608339966, 22.41474081377994310 ) ) ;
#11340=VERTEX_POINT ( 'NONE', #1891 ) ;
#11347=CARTESIAN_POINT ( 'NONE',  ( -55.24198130335446422, -0.006527480770975599769, 0.006617369590168732142 ) ) ;
#11350=CARTESIAN_POINT ( 'NONE',  ( -20.37983603106073716, 1.508851015062576462, -29.73529213200292176 ) ) ;
#11357=CARTESIAN_POINT ( 'NONE',  ( -8.786685647604894456, 7.199674155859698388, 53.04920435127174017 ) ) ;
#11364=VERTEX_POINT ( 'NONE', #28228 ) ;
#11366=CARTESIAN_POINT ( 'NONE',  ( -4.473127245936434626, -31.51789735524219438, -37.94261489385706909 ) ) ;
#11367=CARTESIAN_POINT ( 'NONE',  ( -20.57838717382308147, 16.28767523336121315, -25.16001208503110931 ) ) ;
#11368=VERTEX_POINT ( 'NONE', #5014 ) ;
#11370=EDGE_CURVE ( 'NONE', #17492, #22027, #3261, .T. ) ;
#11375=ORIENTED_EDGE ( 'NONE', *, *, #12823, .T. ) ;
#11376=LINE ( 'NONE', #22179, #1035 ) ;
#11379=EDGE_CURVE ( 'NONE', #1317, #26336, #18246, .T. ) ;
#11401=CARTESIAN_POINT ( 'NONE',  ( -1.019300379054419725, 2.023851374323315078, 45.76814864815086992 ) ) ;
#11402=EDGE_CURVE ( 'NONE', #8934, #13041, #5094, .T. ) ;
#11403=DIRECTION ( 'NONE',  ( 0.7637818620346800147, -0.6451161201712182214, -0.02150485345384170119 ) ) ;
#11406=CARTESIAN_POINT ( 'NONE',  ( -1.259920593601965066, 43.01175804832032412, 16.33409644610508238 ) ) ;
#11411=CARTESIAN_POINT ( 'NONE',  ( -4.473127245936434626, -3.196405119334147837, -49.22197550883366546 ) ) ;
#11412=CLOSED_SHELL ( 'NONE', ( #18988, #4481, #4909, #9196, #2652, #27083, #25487, #8066, #17953, #17198, #17275, #23689, #27729, #12067, #9591, #19062, #18859, #10450, #10370, #7670, #18160, #24519, #16206, #18188, #13240, #7595, #27199, #24444, #26818, #17475, #17991, #20549, #26673, #1970, #380, #9863, #2969, #10983, #1750, #9814, #25632, #14070, #10455, #19655, #4821, #23045, #17000, #21549, #64, #880, #19747, #14747, #4545, #658, #25886, #19303, #23205, #5831, #27220, #4215, #7564, #9404, #4823, #14977, #15102, #13904, #4117, #8261, #22647, #18017, #16997, #3584, #2066, #912, #8820, #6314, #17096, #3160, #11805, #4170, #20902, #23332, #8877, #11468, #16792, #21605, #15542, #7240, #21670, #25227, #11639, #24322, #1938, #2527, #21353, #13980, #17707, #6414, #20926, #14366, #12116, #23716, #1694, #11306, #16211, #19393, #16780, #8974, #17462, #14974, #20759, #16652, #19260, #4254, #11049, #6613, #13337, #23003, #5791, #20830, #2833, #17549, #9101, #22870, #26372, #19946, #17205, #5217, #15452, #5530, #25054, #2227 ) ) ;
#11416=LINE ( 'NONE', #4938, #18846 ) ;
#11429=( BOUNDED_SURFACE ( )  B_SPLINE_SURFACE ( 3, 1, ( 
 ( #26634, #6945 ),
 ( #15694, #14109 ),
 ( #25080, #18433 ),
 ( #3185, #22928 ) ),
 .UNSPECIFIED., .F., .F., .F. ) 
 B_SPLINE_SURFACE_WITH_KNOTS ( ( 4, 4 ),
 ( 2, 2 ),
 ( 0.000000000000000000, 1.000000000000000000 ),
 ( 0.000000000000000000, 1.000000000000000000 ),
 .UNSPECIFIED. ) 
 GEOMETRIC_REPRESENTATION_ITEM ( )  RATIONAL_B_SPLINE_SURFACE ( (
 ( 1.000000000000000000, 1.000000000000000000),
 ( 0.9593753223639863714, 0.9995975284513187731),
 ( 0.9593753223639863714, 0.9995975284513187731),
 ( 1.000000000000000000, 1.000000000000000000) ) ) 
 REPRESENTATION_ITEM ( '' )  SURFACE ( )  );
#11430=ORIENTED_EDGE ( 'NONE', *, *, #20632, .F. ) ;
#11440=LINE ( 'NONE', #11728, #10154 ) ;
#11451=CARTESIAN_POINT ( 'NONE',  ( -7.711401346138374358, 47.70038152767087780, -21.83927363365046048 ) ) ;
#11462=ORIENTED_EDGE ( 'NONE', *, *, #14371, .T. ) ;
#11468=ADVANCED_FACE ( 'NONE', ( #6659 ), #1513, .F. ) ;
#11485=VERTEX_POINT ( 'NONE', #16835 ) ;
#11489=CARTESIAN_POINT ( 'NONE',  ( -24.53237795827032031, 14.09663893005633284, 30.86653739599985968 ) ) ;
#11495=VERTEX_POINT ( 'NONE', #5602 ) ;
#11502=ORIENTED_EDGE ( 'NONE', *, *, #1689, .T. ) ;
#11504=( BOUNDED_SURFACE ( )  B_SPLINE_SURFACE ( 3, 1, ( 
 ( #18805, #12322 ),
 ( #1383, #10192 ),
 ( #18953, #27733 ),
 ( #25583, #8038 ) ),
 .UNSPECIFIED., .F., .F., .F. ) 
 B_SPLINE_SURFACE_WITH_KNOTS ( ( 4, 4 ),
 ( 2, 2 ),
 ( 0.000000000000000000, 1.000000000000000000 ),
 ( 0.000000000000000000, 1.000000000000000000 ),
 .UNSPECIFIED. ) 
 GEOMETRIC_REPRESENTATION_ITEM ( )  RATIONAL_B_SPLINE_SURFACE ( (
 ( 1.000000000000000000, 1.000000000000000000),
 ( 0.7789835883360576307, 0.9689951854195403280),
 ( 0.7789835883360576307, 0.9689951854195403280),
 ( 1.000000000000000000, 1.000000000000000000) ) ) 
 REPRESENTATION_ITEM ( '' )  SURFACE ( )  );
#11505=DIRECTION ( 'NONE',  ( 0.7637818620346801257, -0.5092696688508668856, -0.3965875333584823470 ) ) ;
#11512=ORIENTED_EDGE ( 'NONE', *, *, #15184, .T. ) ;
#11515=CARTESIAN_POINT ( 'NONE',  ( -55.24390624410018802, -0.009209468562450790971, 0.004896917417127758312 ) ) ;
#11520=CARTESIAN_POINT ( 'NONE',  ( -1.583189561560252701, -16.68617981233673220, 43.29471907393757846 ) ) ;
#11525=CARTESIAN_POINT ( 'NONE',  ( -2.904412668506658246, -40.16685646686189415, 25.64203923793618145 ) ) ;
#11531=CONICAL_SURFACE ( 'NONE', #17943, 34.60786435723138510, 0.8559913436420825139 ) ;
#11544=CARTESIAN_POINT ( 'NONE',  ( -9.156249394959713683, -48.78605533024723684, 24.29252099376542517 ) ) ;
#11553=CARTESIAN_POINT ( 'NONE',  ( -7.711401346138397450, -47.70038152767074990, 21.83927363365083707 ) ) ;
#11554=FACE_OUTER_BOUND ( 'NONE', #5583, .T. ) ;
#11556=CONICAL_SURFACE ( 'NONE', #7923, 34.60786435723138510, 0.8559913436420825139 ) ;
#11558=CARTESIAN_POINT ( 'NONE',  ( -55.24390624410018802, -0.004572280736701530256, -0.009374879212970928244 ) ) ;
#11563=CARTESIAN_POINT ( 'NONE',  ( -1.113427685306992876, 16.03057832159213092, 42.96952363574816758 ) ) ;
#11564=ORIENTED_EDGE ( 'NONE', *, *, #27027, .F. ) ;
#11567=CARTESIAN_POINT ( 'NONE',  ( -20.20612092514784308, -29.57813644637189299, 1.137292630518367265 ) ) ;
#11571=CARTESIAN_POINT ( 'NONE',  ( -25.21435515916043713, -4.655591116594118617, 34.29329011225960500 ) ) ;
#11576=ORIENTED_EDGE ( 'NONE', *, *, #7985, .F. ) ;
#11578=VECTOR ( 'NONE', #19682, 1000.000000000000114 ) ;
#11580=EDGE_CURVE ( 'NONE', #20671, #11368, #22927, .T. ) ;
#11584=CARTESIAN_POINT ( 'NONE',  ( -1.583189561560255143, -25.21827308671260326, -38.94740041318284796 ) ) ;
#11586=CARTESIAN_POINT ( 'NONE',  ( -20.57838717382308147, -16.28767523336102130, 25.16001208503123365 ) ) ;
#11587=CARTESIAN_POINT ( 'NONE',  ( -1.049819825607587465, 26.50610175068268859, -37.34982882986852815 ) ) ;
#11601=VECTOR ( 'NONE', #26084, 999.9999999999998863 ) ;
#11603=CARTESIAN_POINT ( 'NONE',  ( -55.24390624410018802, -0.009209468562450790971, 0.004896917417127758312 ) ) ;
#11612=CARTESIAN_POINT ( 'NONE',  ( -20.47566262905009538, -27.87687924095555658, -10.72601569609885708 ) ) ;
#11613=ORIENTED_EDGE ( 'NONE', *, *, #4787, .F. ) ;
#11617=SHAPE_REPRESENTATION_RELATIONSHIP ( 'NONE' , 'NONE' ,  #22271, #2743 ) ;
#11619=CARTESIAN_POINT ( 'NONE',  ( -20.20700224038492721, 0.9908225410478516126, -29.58392382092673145 ) ) ;
#11620=VECTOR ( 'NONE', #23344, 1000.000000000000114 ) ;
#11627=VERTEX_POINT ( 'NONE', #28433 ) ;
#11631=CARTESIAN_POINT ( 'NONE',  ( -16.86833981943424376, -19.19877306373879122, -39.83928801320582380 ) ) ;
#11633=CARTESIAN_POINT ( 'NONE',  ( -20.57838717382308147, -18.89542499756482741, 23.26537097894125594 ) ) ;
#11635=CARTESIAN_POINT ( 'NONE',  ( -55.24198130335446422, -0.008310594958152726572, 0.004163123460802491127 ) ) ;
#11639=ADVANCED_FACE ( 'NONE', ( #24284 ), #27658, .F. ) ;
#11650=VECTOR ( 'NONE', #6320, 999.9999999999998863 ) ;
#11651=VECTOR ( 'NONE', #10100, 1000.000000000000000 ) ;
#11657=VERTEX_POINT ( 'NONE', #93 ) ;
#11658=VERTEX_POINT ( 'NONE', #12901 ) ;
#11660=CARTESIAN_POINT ( 'NONE',  ( -20.20612092514784308, 16.46550332780526915, -24.59769888281538996 ) ) ;
#11675=DIRECTION ( 'NONE',  ( 0.7563875759206389882, -0.03500244528122105347, 0.6531865459554679898 ) ) ;
#11681=CARTESIAN_POINT ( 'NONE',  ( -1.619063947482197729, -35.99532424477401094, -29.22875152547743838 ) ) ;
#11690=( BOUNDED_SURFACE ( )  B_SPLINE_SURFACE ( 3, 1, ( 
 ( #3619, #27937 ),
 ( #12395, #27371 ),
 ( #25664, #14696 ),
 ( #16440, #25223 ) ),
 .UNSPECIFIED., .F., .F., .F. ) 
 B_SPLINE_SURFACE_WITH_KNOTS ( ( 4, 4 ),
 ( 2, 2 ),
 ( 0.000000000000000000, 1.000000000000000000 ),
 ( 0.000000000000000000, 1.000000000000000000 ),
 .UNSPECIFIED. ) 
 GEOMETRIC_REPRESENTATION_ITEM ( )  RATIONAL_B_SPLINE_SURFACE ( (
 ( 1.000000000000000000, 1.000000000000000000),
 ( 0.7789835883360578528, 0.9689951854195403280),
 ( 0.7789835883360578528, 0.9689951854195403280),
 ( 1.000000000000000000, 1.000000000000000000) ) ) 
 REPRESENTATION_ITEM ( '' )  SURFACE ( )  );
#11692=ORIENTED_EDGE ( 'NONE', *, *, #4648, .F. ) ;
#11697=CARTESIAN_POINT ( 'NONE',  ( -55.24390624410018802, 0.007503127514282199352, -0.007245494385991655198 ) ) ;
#11701=CARTESIAN_POINT ( 'NONE',  ( -1.619063947482197729, 2.489035965910801895, 46.30105812165545842 ) ) ;
#11705=EDGE_CURVE ( 'NONE', #12310, #384, #14630, .T. ) ;
#11706=CARTESIAN_POINT ( 'NONE',  ( -16.86833981943425442, 20.94590537750608661, -38.94907963570727816 ) ) ;
#11708=CARTESIAN_POINT ( 'NONE',  ( -1.619063947482201282, 11.94059994246159384, -44.80407745103787676 ) ) ;
#11709=EDGE_CURVE ( 'NONE', #22192, #26713, #10233, .T. ) ;
#11710=CARTESIAN_POINT ( 'NONE',  ( -23.79248802219731118, -28.61009539422396131, -16.82188324679470881 ) ) ;
#11718=DIRECTION ( 'NONE',  ( 0.000000000000000000, 5.223019709707975211E-21, -1.000000000000000000 ) ) ;
#11722=( BOUNDED_SURFACE ( )  B_SPLINE_SURFACE ( 3, 1, ( 
 ( #19844, #26323 ),
 ( #11072, #6479 ),
 ( #271, #8501 ),
 ( #2268, #17539 ) ),
 .UNSPECIFIED., .F., .F., .F. ) 
 B_SPLINE_SURFACE_WITH_KNOTS ( ( 4, 4 ),
 ( 2, 2 ),
 ( 0.000000000000000000, 1.000000000000000000 ),
 ( 0.000000000000000000, 1.000000000000000000 ),
 .UNSPECIFIED. ) 
 GEOMETRIC_REPRESENTATION_ITEM ( )  RATIONAL_B_SPLINE_SURFACE ( (
 ( 1.000000000000000000, 1.000000000000000000),
 ( 0.9593753223639863714, 0.9995975284513187731),
 ( 0.9593753223639863714, 0.9995975284513187731),
 ( 1.000000000000000000, 1.000000000000000000) ) ) 
 REPRESENTATION_ITEM ( '' )  SURFACE ( )  );
#11725=CARTESIAN_POINT ( 'NONE',  ( -1.031422197589711987, 12.69107518035501414, -44.01264471863851213 ) ) ;
#11728=CARTESIAN_POINT ( 'NONE',  ( -28.41354790283022069, 19.47297445639567925, 12.60397206714810814 ) ) ;
#11739=ORIENTED_EDGE ( 'NONE', *, *, #8930, .F. ) ;
#11740=ORIENTED_EDGE ( 'NONE', *, *, #26954, .F. ) ;
#11745=CARTESIAN_POINT ( 'NONE',  ( -2.265401668238148591, -46.93990709177548837, -2.645701981445641504 ) ) ;
#11753=ORIENTED_EDGE ( 'NONE', *, *, #27078, .T. ) ;
#11754=CARTESIAN_POINT ( 'NONE',  ( -7.078251931573400491, -47.71415099571819951, -20.86696228105206075 ) ) ;
#11765=B_SPLINE_CURVE_WITH_KNOTS ( 'NONE', 3,
 ( #1267, #18389, #22892, #27173, #1136, #25178 ),
 .UNSPECIFIED., .F., .F.,
 ( 4, 2, 4 ),
 ( 0.000000000000000000, 0.0004335184443140220763, 0.0008670368886280441527 ),
 .UNSPECIFIED. ) ;
#11770=DIRECTION ( 'NONE',  ( 0.000000000000000000, -1.000000000000000000, 0.000000000000000000 ) ) ;
#11771=CARTESIAN_POINT ( 'NONE',  ( -1.619063947482201282, 16.67502769180561728, -43.26576862488438735 ) ) ;
#11783=CARTESIAN_POINT ( 'NONE',  ( -25.21435515916025594, 1.749597353048488237E-16, -4.373993382621220594E-17 ) ) ;
#11785=CARTESIAN_POINT ( 'NONE',  ( -12.82751273423877869, -48.43568301531143305, 6.573887447703340214 ) ) ;
#11789=CARTESIAN_POINT ( 'NONE',  ( -55.24340739397742084, 0.01010924026184365637, 0.0007387096945736542795 ) ) ;
#11793=PLANE ( 'NONE',  #25345 ) ;
#11795=CARTESIAN_POINT ( 'NONE',  ( -25.21435515916025594, 1.749597353048488237E-16, -4.373993382621220594E-17 ) ) ;
#11801=ORIENTED_EDGE ( 'NONE', *, *, #19981, .T. ) ;
#11805=ADVANCED_FACE ( 'NONE', ( #20811 ), #15884, .F. ) ;
#11806=CARTESIAN_POINT ( 'NONE',  ( -55.24390624410018802, 0.004572280736702236288, 0.009374879212970765180 ) ) ;
#11808=DIRECTION ( 'NONE',  ( 0.000000000000000000, 5.223019709708190374E-21, -1.000000000000000000 ) ) ;
#11810=ORIENTED_EDGE ( 'NONE', *, *, #12158, .F. ) ;
#11818=CARTESIAN_POINT ( 'NONE',  ( -1.049819825607596124, -36.75053263699369666, 27.33096219556280815 ) ) ;
#11826=CARTESIAN_POINT ( 'NONE',  ( -10.86508079875781618, -36.95527278096552237, -35.35100740321762913 ) ) ;
#11829=CARTESIAN_POINT ( 'NONE',  ( -55.24198130335446422, -0.009190321388308575826, -0.001391250620105316613 ) ) ;
#11830=VERTEX_POINT ( 'NONE', #1785 ) ;
#11834=VERTEX_POINT ( 'NONE', #1649 ) ;
#11835=EDGE_CURVE ( 'NONE', #27304, #25524, #27329, .T. ) ;
#11841=CARTESIAN_POINT ( 'NONE',  ( -8.786685647604890903, 37.00619870957935120, -38.68584556812312059 ) ) ;
#11848=CARTESIAN_POINT ( 'NONE',  ( -55.24728320129491266, 0.0006547948648751116246, -0.01453410071985669280 ) ) ;
#11852=CARTESIAN_POINT ( 'NONE',  ( -1.056502255334264895, -0.5104472526223093887, -45.80535052436396626 ) ) ;
#11855=ORIENTED_EDGE ( 'NONE', *, *, #4913, .T. ) ;
#11859=CARTESIAN_POINT ( 'NONE',  ( -1.048172774974298616, 27.73787987941060607, 36.44231470008685392 ) ) ;
#11861=VERTEX_POINT ( 'NONE', #12586 ) ;
#11864=EDGE_CURVE ( 'NONE', #15398, #20457, #18401, .T. ) ;
#11867=B_SPLINE_CURVE_WITH_KNOTS ( 'NONE', 3,
 ( #1844, #6201, #10649, #8084, #19416, #8487 ),
 .UNSPECIFIED., .F., .F.,
 ( 4, 2, 4 ),
 ( 1.734723475976807094E-18, 0.0004335184443140250579, 0.0008670368886280483810 ),
 .UNSPECIFIED. ) ;
#11868=DIRECTION ( 'NONE',  ( -1.000000000000000000, 6.938893903907226837E-18, -1.734723475976806709E-18 ) ) ;
#11877=VERTEX_POINT ( 'NONE', #12726 ) ;
#11890=CARTESIAN_POINT ( 'NONE',  ( -9.156249394959706578, -48.78605533024757079, -24.29252099376471818 ) ) ;
#11895=CARTESIAN_POINT ( 'NONE',  ( -1.045287976400365970, 45.76855895860946077, 1.530335034933974381 ) ) ;
#11897=B_SPLINE_CURVE_WITH_KNOTS ( 'NONE', 3,
 ( #5441, #3560, #25313, #12341, #21406, #7625, #27594 ),
 .UNSPECIFIED., .F., .F.,
 ( 4, 3, 4 ),
 ( 1.734723475976807094E-18, 0.009512539173626401862, 0.02506242213020843518 ),
 .UNSPECIFIED. ) ;
#11905=CARTESIAN_POINT ( 'NONE',  ( -1.539760825549686407, -38.84664866728793697, -25.17088484262129455 ) ) ;
#11910=CARTESIAN_POINT ( 'NONE',  ( -1.048171036023512803, -15.11933492062798656, 43.23005599774316465 ) ) ;
#11911=CARTESIAN_POINT ( 'NONE',  ( -7.078251931573400491, -44.92740138729146082, 26.33626633876272649 ) ) ;
#11922=CARTESIAN_POINT ( 'NONE',  ( 14.74894986621300319, -5.136656239696338858E-17, 37.50000000000001421 ) ) ;
#11925=CARTESIAN_POINT ( 'NONE',  ( -1.031422197589711987, -36.13727897780105991, 28.14735071801782595 ) ) ;
#11926=ORIENTED_EDGE ( 'NONE', *, *, #676, .T. ) ;
#11927=CARTESIAN_POINT ( 'NONE',  ( -23.79248802219729697, -24.83956736572394064, 22.01156985585195258 ) ) ;
#11941=EDGE_CURVE ( 'NONE', #13547, #14894, #7887, .T. ) ;
#11944=CARTESIAN_POINT ( 'NONE',  ( -20.20700224038492010, 16.58740185276710832, -24.51628800869052682 ) ) ;
#11953=CARTESIAN_POINT ( 'NONE',  ( -1.048171036023512803, -43.23005599774311492, -15.11933492062811801 ) ) ;
#11955=CARTESIAN_POINT ( 'NONE',  ( -20.24399999263415140, 27.76448601145554562, 10.36954246768216059 ) ) ;
#11972=EDGE_CURVE ( 'NONE', #20933, #19163, #22114, .T. ) ;
#11976=VECTOR ( 'NONE', #13908, 1000.000000000000114 ) ;
#11977=CARTESIAN_POINT ( 'NONE',  ( -1.048994561756796839, 43.31369460697995777, 14.87838255483211469 ) ) ;
#11979=( BOUNDED_SURFACE ( )  B_SPLINE_SURFACE ( 3, 1, ( 
 ( #11256, #6806 ),
 ( #9243, #24366 ),
 ( #6953, #20026 ),
 ( #4629, #13549 ) ),
 .UNSPECIFIED., .F., .F., .F. ) 
 B_SPLINE_SURFACE_WITH_KNOTS ( ( 4, 4 ),
 ( 2, 2 ),
 ( 0.000000000000000000, 1.000000000000000000 ),
 ( 0.000000000000000000, 1.000000000000000000 ),
 .UNSPECIFIED. ) 
 GEOMETRIC_REPRESENTATION_ITEM ( )  RATIONAL_B_SPLINE_SURFACE ( (
 ( 1.000000000000000000, 1.000000000000000000),
 ( 0.7789835883360576307, 0.9689951854195403280),
 ( 0.7789835883360576307, 0.9689951854195403280),
 ( 1.000000000000000000, 1.000000000000000000) ) ) 
 REPRESENTATION_ITEM ( '' )  SURFACE ( )  );
#11988=CARTESIAN_POINT ( 'NONE',  ( -25.21435515916043713, -4.655591116594118617, 34.29329011225960500 ) ) ;
#11989=EDGE_CURVE ( 'NONE', #23103, #9163, #20950, .T. ) ;
#11990=AXIS2_PLACEMENT_3D ( 'NONE', #26822, #20344, #11718 ) ;
#12001=AXIS2_PLACEMENT_3D ( 'NONE', #23590, #27881, #9914 ) ;
#12013=AXIS2_PLACEMENT_3D ( 'NONE', #17814, #15652, #9059 ) ;
#12018=CARTESIAN_POINT ( 'NONE',  ( -1.539760825549678636, 25.17088484262142956, -38.84664866728784460 ) ) ;
#12029=CARTESIAN_POINT ( 'NONE',  ( -1.044557008772710294, 25.56990300677035677, 37.98985164565299755 ) ) ;
#12034=ORIENTED_EDGE ( 'NONE', *, *, #8172, .T. ) ;
#12049=LINE ( 'NONE', #20820, #15209 ) ;
#12055=ORIENTED_EDGE ( 'NONE', *, *, #14405, .T. ) ;
#12059=CARTESIAN_POINT ( 'NONE',  ( -1.583189561560252701, -38.94740041318275559, 25.21827308671274182 ) ) ;
#12062=CIRCLE ( 'NONE', #22656, 53.53553390275978785 ) ;
#12066=CARTESIAN_POINT ( 'NONE',  ( -1.031422197589711987, -12.69107518035471394, 44.01264471863858319 ) ) ;
#12067=ADVANCED_FACE ( 'NONE', ( #27391 ), #11531, .T. ) ;
#12070=CARTESIAN_POINT ( 'NONE',  ( -20.20612092514785019, 27.77903665678167400, -10.22177639105870384 ) ) ;
#12094=CARTESIAN_POINT ( 'NONE',  ( -25.21435515916043713, -30.48034229288627017, 16.39063784838775462 ) ) ;
#12095=B_SPLINE_CURVE_WITH_KNOTS ( 'NONE', 3,
 ( #1683, #3437, #8060, #21122, #11178, #22113, #26560 ),
 .UNSPECIFIED., .F., .F.,
 ( 4, 3, 4 ),
 ( 0.000000000000000000, 0.006568092053401763247, 0.02506242213020846987 ),
 .UNSPECIFIED. ) ;
#12099=CARTESIAN_POINT ( 'NONE',  ( -4.178947244162634966, 37.51424432987651159, -31.41809272265936315 ) ) ;
#12102=ORIENTED_EDGE ( 'NONE', *, *, #14718, .F. ) ;
#12105=EDGE_CURVE ( 'NONE', #21619, #20671, #13833, .T. ) ;
#12107=CARTESIAN_POINT ( 'NONE',  ( -1.045287976400383290, 12.68782741917383738, 44.00138577190627842 ) ) ;
#12108=CARTESIAN_POINT ( 'NONE',  ( -6.574463467970654840, 5.014313797967739461, 51.07975593197901532 ) ) ;
#12113=CARTESIAN_POINT ( 'NONE',  ( -8.786685647604885574, 6.096987947571466530E-17, -1.524246986892866633E-17 ) ) ;
#12116=ADVANCED_FACE ( 'NONE', ( #7998 ), #18660, .F. ) ;
#12123=ORIENTED_EDGE ( 'NONE', *, *, #10563, .T. ) ;
#12126=VERTEX_POINT ( 'NONE', #20772 ) ;
#12127=CARTESIAN_POINT ( 'NONE',  ( -25.21435515916025594, 1.749597353048488237E-16, -4.373993382621220594E-17 ) ) ;
#12133=EDGE_CURVE ( 'NONE', #5543, #5967, #13399, .T. ) ;
#12135=B_SPLINE_CURVE_WITH_KNOTS ( 'NONE', 3,
 ( #14861, #12830, #10836, #3633, #16891, #25542 ),
 .UNSPECIFIED., .F., .F.,
 ( 4, 2, 4 ),
 ( 3.709064347514218400E-16, 0.003576372551511170905, 0.007152745103021971446 ),
 .UNSPECIFIED. ) ;
#12140=DIRECTION ( 'NONE',  ( 0.7637818620346801257, 0.02150485345384395286, -0.6451161201712182214 ) ) ;
#12141=CARTESIAN_POINT ( 'NONE',  ( -8.786685647604896232, 23.24040270374459993, 48.22796981442743913 ) ) ;
#12145=DIRECTION ( 'NONE',  ( 1.000000000000000000, -6.938893903907226837E-18, 1.734723475976806709E-18 ) ) ;
#12147=CARTESIAN_POINT ( 'NONE',  ( -1.619063947482197729, 16.67502769180622835, 43.26576862488415287 ) ) ;
#12158=EDGE_CURVE ( 'NONE', #18255, #711, #24377, .T. ) ;
#12169=CARTESIAN_POINT ( 'NONE',  ( -2.265401668238145483, -39.53028715828216377, 25.45016726748356817 ) ) ;
#12172=CARTESIAN_POINT ( 'NONE',  ( -6.574463467970648622, -20.55340846381166742, -47.03022655117394635 ) ) ;
#12190=( BOUNDED_SURFACE ( )  B_SPLINE_SURFACE ( 3, 1, ( 
 ( #225, #6428 ),
 ( #15325, #13307 ),
 ( #15043, #19516 ),
 ( #2513, #22256 ) ),
 .UNSPECIFIED., .F., .F., .F. ) 
 B_SPLINE_SURFACE_WITH_KNOTS ( ( 4, 4 ),
 ( 2, 2 ),
 ( 0.000000000000000000, 1.000000000000000000 ),
 ( 0.000000000000000000, 1.000000000000000000 ),
 .UNSPECIFIED. ) 
 GEOMETRIC_REPRESENTATION_ITEM ( )  RATIONAL_B_SPLINE_SURFACE ( (
 ( 1.000000000000000000, 1.000000000000000000),
 ( 0.9934239774497837239, 0.8357310067453919133),
 ( 0.9934239774497837239, 0.8357310067453919133),
 ( 1.000000000000000000, 1.000000000000000000) ) ) 
 REPRESENTATION_ITEM ( '' )  SURFACE ( )  );
#12191=CARTESIAN_POINT ( 'NONE',  ( -55.24390624410018802, -0.009374879212966679906, -0.004572280736703028189 ) ) ;
#12200=CARTESIAN_POINT ( 'NONE',  ( -1.048171036023507252, 43.86077206077069235, -13.17819047681618372 ) ) ;
#12207=DIRECTION ( 'NONE',  ( 0.000000000000000000, 5.223019709708233256E-21, -1.000000000000000000 ) ) ;
#12208=CARTESIAN_POINT ( 'NONE',  ( -20.20700224038492721, 27.82980252387819675, -10.08426345511598932 ) ) ;
#12211=CARTESIAN_POINT ( 'NONE',  ( -1.031422197589716205, -28.14735071801769095, -36.13727897780117360 ) ) ;
#12214=CARTESIAN_POINT ( 'NONE',  ( -1.323830074806768398, -43.04593525292981582, -16.42382241777520946 ) ) ;
#12221=ORIENTED_EDGE ( 'NONE', *, *, #18702, .T. ) ;
#12226=CARTESIAN_POINT ( 'NONE',  ( -1.049819825607602342, 36.75053263699390271, -27.33096219556254169 ) ) ;
#12230=EDGE_CURVE ( 'NONE', #4452, #6648, #11317, .T. ) ;
#12233=( BOUNDED_SURFACE ( )  B_SPLINE_SURFACE ( 3, 1, ( 
 ( #14491, #16665 ),
 ( #5734, #10048 ),
 ( #5430, #20833 ),
 ( #28006, #10199 ) ),
 .UNSPECIFIED., .F., .F., .F. ) 
 B_SPLINE_SURFACE_WITH_KNOTS ( ( 4, 4 ),
 ( 2, 2 ),
 ( 0.000000000000000000, 1.000000000000000000 ),
 ( 0.000000000000000000, 1.000000000000000000 ),
 .UNSPECIFIED. ) 
 GEOMETRIC_REPRESENTATION_ITEM ( )  RATIONAL_B_SPLINE_SURFACE ( (
 ( 1.000000000000000000, 1.000000000000000000),
 ( 0.9934239774497837239, 0.8357310067453919133),
 ( 0.9934239774497837239, 0.8357310067453919133),
 ( 1.000000000000000000, 1.000000000000000000) ) ) 
 REPRESENTATION_ITEM ( '' )  SURFACE ( )  );
#12234=EDGE_CURVE ( 'NONE', #11877, #3600, #9290, .T. ) ;
#12238=B_SPLINE_CURVE_WITH_KNOTS ( 'NONE', 3,
 ( #21574, #1710, #21298, #4016, #10244, #27912, #1580, #25636, #10508, #14672 ),
 .UNSPECIFIED., .F., .F.,
 ( 4, 2, 2, 2, 4 ),
 ( 0.000000000000000000, 0.0003346267210630921333, 0.0006692534421261842666, 0.001003880163189276292, 0.001338506884252368533 ),
 .UNSPECIFIED. ) ;
#12244=CARTESIAN_POINT ( 'NONE',  ( -1.044556982611281493, 43.01635920718349126, -15.70482750345250267 ) ) ;
#12251=CARTESIAN_POINT ( 'NONE',  ( -21.81686047589426636, -27.83628745321466624, -26.62923599424956933 ) ) ;
#12255=CIRCLE ( 'NONE', #9928, 44.74884827092600403 ) ;
#12276=CARTESIAN_POINT ( 'NONE',  ( -1.583189561560252701, 44.83405390829673109, -11.94859433442916874 ) ) ;
#12283=VERTEX_POINT ( 'NONE', #26784 ) ;
#12286=ORIENTED_EDGE ( 'NONE', *, *, #13025, .T. ) ;
#12287=EDGE_LOOP ( 'NONE', ( #2501, #25475, #10734, #17432 ) ) ;
#12288=ORIENTED_EDGE ( 'NONE', *, *, #3123, .T. ) ;
#12291=CARTESIAN_POINT ( 'NONE',  ( -55.24390624410018802, 0.004896917417131886954, -0.009209468562452662738 ) ) ;
#12298=ORIENTED_EDGE ( 'NONE', *, *, #99, .F. ) ;
#12304=B_SPLINE_CURVE_WITH_KNOTS ( 'NONE', 3,
 ( #13819, #21440, #3744, #3595, #28053, #27635, #12514, #8492, #1850, #19008 ),
 .UNSPECIFIED., .F., .F.,
 ( 4, 2, 2, 2, 4 ),
 ( 1.301042606982605321E-18, 0.0003346267210630944101, 0.0006692534421261875192, 0.001003880163189280628, 0.001338506884252373737 ),
 .UNSPECIFIED. ) ;
#12306=ORIENTED_EDGE ( 'NONE', *, *, #15511, .T. ) ;
#12308=CARTESIAN_POINT ( 'NONE',  ( -55.24390624410018802, 0.007245494385991800047, -0.007503127514277958821 ) ) ;
#12309=FACE_OUTER_BOUND ( 'NONE', #26059, .T. ) ;
#12310=VERTEX_POINT ( 'NONE', #20310 ) ;
#12314=ORIENTED_EDGE ( 'NONE', *, *, #10736, .F. ) ;
#12316=EDGE_CURVE ( 'NONE', #15270, #20885, #23377, .T. ) ;
#12319=ORIENTED_EDGE ( 'NONE', *, *, #3934, .T. ) ;
#12322=CARTESIAN_POINT ( 'NONE',  ( -1.583189561560253589, 46.33203782964461936, -2.490696082060032790 ) ) ;
#12323=FACE_OUTER_BOUND ( 'NONE', #2096, .T. ) ;
#12325=CARTESIAN_POINT ( 'NONE',  ( -25.21435515916025594, 1.749597353048488237E-16, -4.373993382621220594E-17 ) ) ;
#12326=CARTESIAN_POINT ( 'NONE',  ( -20.20700224038492721, 27.82980252387819675, -10.08426345511598932 ) ) ;
#12330=CARTESIAN_POINT ( 'NONE',  ( -1.464342487929859660, -46.14921266389556820, 2.431462367721817230 ) ) ;
#12331=CARTESIAN_POINT ( 'NONE',  ( -1.045287976400383290, 28.14015102489806708, -36.12803364096618708 ) ) ;
#12332=ORIENTED_EDGE ( 'NONE', *, *, #27976, .T. ) ;
#12338=LINE ( 'NONE', #6170, #20806 ) ;
#12341=CARTESIAN_POINT ( 'NONE',  ( -15.02187109954785527, 32.04062513125116141, -33.49412687891580021 ) ) ;
#12344=CARTESIAN_POINT ( 'NONE',  ( -1.155001620486255209, -44.25209926692301110, 12.20337535396725492 ) ) ;
#12355=FACE_OUTER_BOUND ( 'NONE', #6492, .T. ) ;
#12363=CARTESIAN_POINT ( 'NONE',  ( -1.619063947482197729, -35.99532424477401094, -29.22875152547743838 ) ) ;
#12377=CARTESIAN_POINT ( 'NONE',  ( -25.21435515916025594, 1.749597353048488237E-16, -4.373993382621220594E-17 ) ) ;
#12389=CARTESIAN_POINT ( 'NONE',  ( -8.786685647604885574, 6.617461520090397715E-15, -53.53553390275978785 ) ) ;
#12395=CARTESIAN_POINT ( 'NONE',  ( -55.25297051322618813, 0.01093108995494865114, -0.01019003092403491552 ) ) ;
#12400=CARTESIAN_POINT ( 'NONE',  ( -1.031422197589711764, 12.69107518035563587, 44.01264471863832739 ) ) ;
#12402=CARTESIAN_POINT ( 'NONE',  ( -23.77929240705206482, 35.68044874544704470, 6.464423883190010933 ) ) ;
#12412=VERTEX_POINT ( 'NONE', #7966 ) ;
#12414=CARTESIAN_POINT ( 'NONE',  ( -1.583189561560255143, -16.68617981233672509, 43.29471907393757846 ) ) ;
#12416=CARTESIAN_POINT ( 'NONE',  ( -1.048171036023513247, 26.08692787913922473, 37.64178826568577563 ) ) ;
#12422=ORIENTED_EDGE ( 'NONE', *, *, #10816, .F. ) ;
#12423=LINE ( 'NONE', #27835, #25782 ) ;
#12427=CARTESIAN_POINT ( 'NONE',  ( -20.47566338032508426, 1.586617869344308041, 29.82700953060495408 ) ) ;
#12437=CARTESIAN_POINT ( 'NONE',  ( -1.045287976400365970, -25.66401692419961833, 37.92705037016786918 ) ) ;
#12441=CARTESIAN_POINT ( 'NONE',  ( -5.986830583229483693, -19.95149887249887399, -46.64941882410793283 ) ) ;
#12442=CARTESIAN_POINT ( 'NONE',  ( -20.20700224038492721, 10.08426345511588984, -27.82980252387822517 ) ) ;
#12444=VERTEX_POINT ( 'NONE', #27361 ) ;
#12445=CARTESIAN_POINT ( 'NONE',  ( -2.265401668238146815, -25.45016726748341540, -39.53028715828224904 ) ) ;
#12450=ORIENTED_EDGE ( 'NONE', *, *, #27691, .T. ) ;
#12454=ORIENTED_EDGE ( 'NONE', *, *, #7172, .F. ) ;
#12467=VERTEX_POINT ( 'NONE', #28067 ) ;
#12480=CARTESIAN_POINT ( 'NONE',  ( -20.38016308990359349, 27.81387210821422329, -10.62413300760995583 ) ) ;
#12483=CARTESIAN_POINT ( 'NONE',  ( -25.21435515916043713, -23.92354251275954979, -25.00736669481013053 ) ) ;
#12492=CARTESIAN_POINT ( 'NONE',  ( -6.588769196390762417, 44.25609997968906839, -26.02756986588556742 ) ) ;
#12500=( NAMED_UNIT ( * ) SI_UNIT ( $, .STERADIAN. ) SOLID_ANGLE_UNIT ( ) );
#12503=CARTESIAN_POINT ( 'NONE',  ( -25.21435515916043713, -15.02493970636168896, -31.17620025257581062 ) ) ;
#12514=CARTESIAN_POINT ( 'NONE',  ( -1.113427685306989767, -42.96952363574823863, 16.03057832159198171 ) ) ;
#12520=CARTESIAN_POINT ( 'NONE',  ( -1.031422197589716205, -45.78027046666446154, -1.530725436377304183 ) ) ;
#12535=ORIENTED_EDGE ( 'NONE', *, *, #9978, .T. ) ;
#12536=B_SPLINE_CURVE_WITH_KNOTS ( 'NONE', 3,
 ( #28199, #4165, #13933, #11927, #7195, #22746 ),
 .UNSPECIFIED., .F., .F.,
 ( 4, 2, 4 ),
 ( 1.512296865354101973E-16, 0.003570751334075637860, 0.007141502668151123931 ),
 .UNSPECIFIED. ) ;
#12547=LINE ( 'NONE', #23663, #8831 ) ;
#12562=CARTESIAN_POINT ( 'NONE',  ( -1.323439229708135434, 38.58845475799802927, 25.17120723334049970 ) ) ;
#12566=EDGE_CURVE ( 'NONE', #194, #17492, #22660, .T. ) ;
#12569=CARTESIAN_POINT ( 'NONE',  ( -1.048172774974290622, 43.86067135048637766, 13.17853518375252442 ) ) ;
#12572=B_SPLINE_CURVE_WITH_KNOTS ( 'NONE', 3,
 ( #15211, #12778, #15071, #6323, #2249, #28178, #24164 ),
 .UNSPECIFIED., .F., .F.,
 ( 4, 3, 4 ),
 ( 0.000000000000000000, 0.006568092053401826565, 0.02506242213020857396 ),
 .UNSPECIFIED. ) ;
#12573=LINE ( 'NONE', #10564, #7991 ) ;
#12578=ORIENTED_EDGE ( 'NONE', *, *, #10432, .F. ) ;
#12580=CARTESIAN_POINT ( 'NONE',  ( -15.02187109954782507, -32.04062513125090561, 33.49412687891607021 ) ) ;
#12581=CARTESIAN_POINT ( 'NONE',  ( -25.21435515916043713, -34.05351380035328646, 6.169479169075816394 ) ) ;
#12584=VERTEX_POINT ( 'NONE', #4591 ) ;
#12586=CARTESIAN_POINT ( 'NONE',  ( -25.21435515916043713, 4.655591116594827383, 34.29329011225949841 ) ) ;
#12587=CARTESIAN_POINT ( 'NONE',  ( -1.239374126674604337, 28.97829083655439675, -35.79060836339822060 ) ) ;
#12590=B_SPLINE_CURVE_WITH_KNOTS ( 'NONE', 3,
 ( #7807, #1300, #21016, #22780, #5333, #16719, #1024, #27352, #8093, #18427, #27203, #3325, #9964 ),
 .UNSPECIFIED., .F., .F.,
 ( 4, 3, 3, 3, 4 ),
 ( 1.105886215935214523E-17, 0.0007657099931970556828, 0.001531419946797917854, 0.002296279302920152532, 0.003061450627205755497 ),
 .UNSPECIFIED. ) ;
#12598=DIRECTION ( 'NONE',  ( 0.000000000000000000, 5.223019709707975211E-21, -1.000000000000000000 ) ) ;
#12601=CARTESIAN_POINT ( 'NONE',  ( -1.619063947482197729, -29.22875152547730337, 35.99532424477411041 ) ) ;
#12605=CARTESIAN_POINT ( 'NONE',  ( -1.583189561560253589, 2.490696082060518624, 46.33203782964458384 ) ) ;
#12610=LINE ( 'NONE', #8720, #8410 ) ;
#12611=DIRECTION ( 'NONE',  ( -0.7563875759206388771, 0.6531865459554675457, -0.03500244528123232224 ) ) ;
#12623=CARTESIAN_POINT ( 'NONE',  ( -1.031422197589711764, 1.530725436377463389, -45.78027046666443312 ) ) ;
#12635=CARTESIAN_POINT ( 'NONE',  ( -28.41354790283022069, 21.64275480268748453, -8.345538364877153725 ) ) ;
#12650=CARTESIAN_POINT ( 'NONE',  ( -2.911734481061421853, 36.84482841982651280, -30.23325065583374638 ) ) ;
#12670=ORIENTED_EDGE ( 'NONE', *, *, #13321, .T. ) ;
#12680=CARTESIAN_POINT ( 'NONE',  ( -20.24419206586952669, 10.37009329716804196, 27.76448493191432476 ) ) ;
#12681=B_SPLINE_CURVE_WITH_KNOTS ( 'NONE', 3,
 ( #16113, #18130, #9510, #22768, #17975, #20291, #20145 ),
 .UNSPECIFIED., .F., .F.,
 ( 4, 3, 4 ),
 ( 1.201851678989727385E-17, 0.009512539173626329003, 0.02506242213020845599 ),
 .UNSPECIFIED. ) ;
#12687=CARTESIAN_POINT ( 'NONE',  ( -1.031422197589711987, -1.530725436377782467, -45.78027046666441890 ) ) ;
#12694=CARTESIAN_POINT ( 'NONE',  ( -55.25297051322618813, -0.002853887643043501524, -0.01466904165775538733 ) ) ;
#12702=EDGE_LOOP ( 'NONE', ( #21422, #13709, #16130, #12298 ) ) ;
#12703=ORIENTED_EDGE ( 'NONE', *, *, #3654, .F. ) ;
#12706=CARTESIAN_POINT ( 'NONE',  ( -55.24271866751342941, 0.001545935011631005204, -0.009369360294295841357 ) ) ;
#12719=CARTESIAN_POINT ( 'NONE',  ( -1.031422197589716205, -15.60268798220608844, 43.06660437151324317 ) ) ;
#12720=CARTESIAN_POINT ( 'NONE',  ( -1.031422197589716205, 44.01264471863849082, -12.69107518035517046 ) ) ;
#12726=CARTESIAN_POINT ( 'NONE',  ( -1.619063947482197729, 44.80407745103800465, 11.94059994246113021 ) ) ;
#12731=B_SPLINE_CURVE_WITH_KNOTS ( 'NONE', 3,
 ( #5693, #23262, #16187, #3513 ),
 .UNSPECIFIED., .F., .F.,
 ( 4, 4 ),
 ( 1.877672896018868361E-16, 0.001982023823822947652 ),
 .UNSPECIFIED. ) ;
#12735=VERTEX_POINT ( 'NONE', #6554 ) ;
#12756=DIRECTION ( 'NONE',  ( 1.000000000000000000, -6.938893903907226837E-18, 1.734723475976806709E-18 ) ) ;
#12761=CARTESIAN_POINT ( 'NONE',  ( -55.24300891470648622, 0.003362556190415182372, -0.009225237711098200136 ) ) ;
#12762=FACE_OUTER_BOUND ( 'NONE', #20509, .T. ) ;
#12766=CARTESIAN_POINT ( 'NONE',  ( -55.24728320129491266, 0.003868537197317429340, 0.01402509393918536899 ) ) ;
#12767=( BOUNDED_SURFACE ( )  B_SPLINE_SURFACE ( 3, 1, ( 
 ( #18572, #720 ),
 ( #27189, #24644 ),
 ( #24490, #16267 ),
 ( #22620, #4897 ) ),
 .UNSPECIFIED., .F., .F., .F. ) 
 B_SPLINE_SURFACE_WITH_KNOTS ( ( 4, 4 ),
 ( 2, 2 ),
 ( 0.000000000000000000, 1.000000000000000000 ),
 ( 0.000000000000000000, 1.000000000000000000 ),
 .UNSPECIFIED. ) 
 GEOMETRIC_REPRESENTATION_ITEM ( )  RATIONAL_B_SPLINE_SURFACE ( (
 ( 1.000000000000000000, 1.000000000000000000),
 ( 0.9934239774497838349, 0.8357310067453913582),
 ( 0.9934239774497838349, 0.8357310067453913582),
 ( 1.000000000000000000, 1.000000000000000000) ) ) 
 REPRESENTATION_ITEM ( '' )  SURFACE ( )  );
#12778=CARTESIAN_POINT ( 'NONE',  ( -23.77929240705205771, -26.20227034809537514, 25.06639637888449457 ) ) ;
#12780=CARTESIAN_POINT ( 'NONE',  ( -2.911734481061404534, -2.802366807346520439, -47.57875121082949477 ) ) ;
#12792=CARTESIAN_POINT ( 'NONE',  ( -20.57838717382308147, -28.96176188950213870, 7.715628353033985753 ) ) ;
#12802=B_SPLINE_CURVE_WITH_KNOTS ( 'NONE', 3,
 ( #26803, #17592, #7113, #4492, #2325, #4931, #13700 ),
 .UNSPECIFIED., .F., .F.,
 ( 4, 3, 4 ),
 ( 0.000000000000000000, 0.006568092053401789268, 0.02506242213020845946 ),
 .UNSPECIFIED. ) ;
#12808=EDGE_CURVE ( 'NONE', #4550, #27179, #7212, .T. ) ;
#12810=EDGE_LOOP ( 'NONE', ( #22760, #14889, #76, #15724 ) ) ;
#12815=ORIENTED_EDGE ( 'NONE', *, *, #20807, .T. ) ;
#12823=EDGE_CURVE ( 'NONE', #5123, #19834, #4101, .T. ) ;
#12825=DIRECTION ( 'NONE',  ( 0.7637818620346801257, 0.6201872550346656521, -0.1788995134688848854 ) ) ;
#12828=FACE_OUTER_BOUND ( 'NONE', #739, .T. ) ;
#12830=CARTESIAN_POINT ( 'NONE',  ( -24.53239521893647179, -16.68574937150994231, -29.54733954334103174 ) ) ;
#12834=CARTESIAN_POINT ( 'NONE',  ( -1.050231094221210970, 45.79908322896420003, -0.2545420581350661404 ) ) ;
#12847=EDGE_CURVE ( 'NONE', #8562, #13021, #26754, .T. ) ;
#12850=EDGE_CURVE ( 'NONE', #26713, #27831, #12049, .T. ) ;
#12859=CARTESIAN_POINT ( 'NONE',  ( -1.583189561560252701, 29.24830400313166123, -36.01941156322796900 ) ) ;
#12861=CARTESIAN_POINT ( 'NONE',  ( -1.048996300304493312, -27.53442103413720332, -36.59642367107734628 ) ) ;
#12865=CARTESIAN_POINT ( 'NONE',  ( -1.045287976400362417, -15.59869763335038506, 43.05558670614261985 ) ) ;
#12866=CARTESIAN_POINT ( 'NONE',  ( -28.41354790283022069, -12.60397206714846341, -19.47297445639544833 ) ) ;
#12868=CARTESIAN_POINT ( 'NONE',  ( -8.786685647604890903, -9.545808661480235102, 52.67761315067295413 ) ) ;
#12869=ORIENTED_EDGE ( 'NONE', *, *, #13312, .F. ) ;
#12871=CARTESIAN_POINT ( 'NONE',  ( -1.323830074806771284, 2.318057800980712457, -46.01435746200690602 ) ) ;
#12872=CIRCLE ( 'NONE', #1853, 34.60786435723138510 ) ;
#12873=CARTESIAN_POINT ( 'NONE',  ( -23.79223135445719350, -13.25822371132274924, 30.42557260166825017 ) ) ;
#12880=CARTESIAN_POINT ( 'NONE',  ( -7.078251931573406708, 5.101176922831390570, 51.82710018979469879 ) ) ;
#12882=EDGE_CURVE ( 'NONE', #18351, #10615, #28425, .T. ) ;
#12889=ORIENTED_EDGE ( 'NONE', *, *, #18734, .T. ) ;
#12894=CARTESIAN_POINT ( 'NONE',  ( -10.86508079875782329, 24.22249093393363850, 45.04061326950845512 ) ) ;
#12899=CARTESIAN_POINT ( 'NONE',  ( -55.24340739397742794, -0.006539691034608149933, -0.007744344507854676943 ) ) ;
#12901=CARTESIAN_POINT ( 'NONE',  ( -1.045287976400362417, 25.66401692420069125, 37.92705037016716574 ) ) ;
#12903=CARTESIAN_POINT ( 'NONE',  ( -7.711401346138401891, 35.51061203065580685, 38.61705198405327621 ) ) ;
#12907=VECTOR ( 'NONE', #13914, 999.9999999999998863 ) ;
#12916=DIRECTION ( 'NONE',  ( 0.000000000000000000, 5.223019709707975211E-21, -1.000000000000000000 ) ) ;
#12920=CARTESIAN_POINT ( 'NONE',  ( -1.031422197589711764, -43.06660437151319343, -15.60268798220621100 ) ) ;
#12921=DIRECTION ( 'NONE',  ( 1.000000000000000000, -6.938893903907226837E-18, 1.734723475976806709E-18 ) ) ;
#12930=ORIENTED_EDGE ( 'NONE', *, *, #14999, .F. ) ;
#12931=CIRCLE ( 'NONE', #23989, 20.00000000000000000 ) ;
#12935=CARTESIAN_POINT ( 'NONE',  ( -20.20700224038492721, 28.44216453106536946, -8.199606986804427677 ) ) ;
#12938=FACE_OUTER_BOUND ( 'NONE', #9025, .T. ) ;
#12945=DIRECTION ( 'NONE',  ( 0.000000000000000000, 5.223019709708116647E-21, -1.000000000000000000 ) ) ;
#12955=VECTOR ( 'NONE', #27228, 999.9999999999998863 ) ;
#12959=EDGE_CURVE ( 'NONE', #1293, #17227, #14012, .T. ) ;
#12965=CARTESIAN_POINT ( 'NONE',  ( -22.23226125620929139, 30.68305173820436593, 7.677408153693709991 ) ) ;
#12969=CARTESIAN_POINT ( 'NONE',  ( -1.045287976400362417, -12.68782741917263657, 44.00138577190661948 ) ) ;
#12971=CARTESIAN_POINT ( 'NONE',  ( -1.056502255334265339, 36.75727364034771938, 27.33667001641128991 ) ) ;
#12972=CARTESIAN_POINT ( 'NONE',  ( -1.259972190295308714, -35.85909728507027694, 28.82609802125297449 ) ) ;
#12975=CARTESIAN_POINT ( 'NONE',  ( -20.57838717382308147, -10.78122205916981358, 27.96569011373096814 ) ) ;
#12985=B_SPLINE_CURVE_WITH_KNOTS ( 'NONE', 3,
 ( #21544, #10481, #23598, #19118, #12344, #25740, #10216, #18977, #21409, #8057 ),
 .UNSPECIFIED., .F., .F.,
 ( 4, 2, 2, 2, 4 ),
 ( 2.847672227753435151E-16, 0.0003346187017559057865, 0.0006692374035115268615, 0.001003856105267147665, 0.001338474807022768795 ),
 .UNSPECIFIED. ) ;
#12993=CARTESIAN_POINT ( 'NONE',  ( -20.57838717382308502, 25.16001208503106668, -16.28767523336130196 ) ) ;
#12997=DIRECTION ( 'NONE',  ( -1.000000000000000000, 6.938893903907226837E-18, -1.734723475976806709E-18 ) ) ;
#13001=B_SPLINE_CURVE_WITH_KNOTS ( 'NONE', 3,
 ( #11176, #24425, #13606, #231 ),
 .UNSPECIFIED., .F., .F.,
 ( 4, 4 ),
 ( 1.904170172768910460E-16, 0.001982023823822945917 ),
 .UNSPECIFIED. ) ;
#13007=CARTESIAN_POINT ( 'NONE',  ( -12.94347594948482083, -33.69581619287849605, 35.22469990145643948 ) ) ;
#13010=CARTESIAN_POINT ( 'NONE',  ( -1.044557008772712070, -43.01636061108997922, -15.70482370518800153 ) ) ;
#13013=FACE_OUTER_BOUND ( 'NONE', #4380, .T. ) ;
#13017=ORIENTED_EDGE ( 'NONE', *, *, #4573, .F. ) ;
#13021=VERTEX_POINT ( 'NONE', #24810 ) ;
#13024=AXIS2_PLACEMENT_3D ( 'NONE', #21906, #11250, #6946 ) ;
#13025=EDGE_CURVE ( 'NONE', #11340, #8983, #25712, .T. ) ;
#13030=CARTESIAN_POINT ( 'NONE',  ( -8.786685647604887350, 53.04920435127183254, -7.199674155859138835 ) ) ;
#13035=DIRECTION ( 'NONE',  ( 0.000000000000000000, 5.223019709707975211E-21, -1.000000000000000000 ) ) ;
#13041=VERTEX_POINT ( 'NONE', #3200 ) ;
#13044=FACE_OUTER_BOUND ( 'NONE', #22158, .T. ) ;
#13048=VERTEX_POINT ( 'NONE', #465 ) ;
#13052=CARTESIAN_POINT ( 'NONE',  ( -20.57838717382308147, -29.92853265176830746, 1.611677988432673070 ) ) ;
#13072=CARTESIAN_POINT ( 'NONE',  ( -8.259864102781634188, -6.590267880897305197, -52.60025989855206063 ) ) ;
#13074=CARTESIAN_POINT ( 'NONE',  ( -20.90916690077964901, -18.74041620980142753, 34.84883504600970383 ) ) ;
#13077=CARTESIAN_POINT ( 'NONE',  ( -18.41936578851709072, 38.22933728004715448, 18.42310649277586876 ) ) ;
#13081=CARTESIAN_POINT ( 'NONE',  ( -23.77929240705206837, 32.66578242509746133, -15.74261278740683778 ) ) ;
#13088=CARTESIAN_POINT ( 'NONE',  ( -28.13707043255157103, -22.00298671236735615, 6.342158660427235972 ) ) ;
#13091=FACE_OUTER_BOUND ( 'NONE', #8233, .T. ) ;
#13101=B_SPLINE_CURVE_WITH_KNOTS ( 'NONE', 3,
 ( #12437, #1088, #27415, #23546, #16913, #23128, #2029, #27555, #21227, #3809, #19594, #9876, #8661 ),
 .UNSPECIFIED., .F., .F.,
 ( 4, 3, 3, 3, 4 ),
 ( 9.813077866773594792E-18, 0.0007657099931970698858, 0.001531419946797932816, 0.002296279302920152098, 0.003061450627205747257 ),
 .UNSPECIFIED. ) ;
#13106=ORIENTED_EDGE ( 'NONE', *, *, #11709, .F. ) ;
#13110=VERTEX_POINT ( 'NONE', #1188 ) ;
#13114=CARTESIAN_POINT ( 'NONE',  ( -8.259864102781673267, 25.58601832199082793, -46.42816643551579148 ) ) ;
#13116=CARTESIAN_POINT ( 'NONE',  ( -55.24271866751342941, -0.009388511352197387999, -0.001425019990782294558 ) ) ;
#13124=ORIENTED_EDGE ( 'NONE', *, *, #7499, .F. ) ;
#13127=VERTEX_POINT ( 'NONE', #14698 ) ;
#13132=CARTESIAN_POINT ( 'NONE',  ( -20.20700224038492010, -18.19058640100240254, -23.35150625415651859 ) ) ;
#13133=CARTESIAN_POINT ( 'NONE',  ( -20.24399999263414429, -16.36687688782875938, -24.70869149526196651 ) ) ;
#13136=CARTESIAN_POINT ( 'NONE',  ( -1.048172774974291066, 1.020161070261757841, 45.78636862970791555 ) ) ;
#13148=CARTESIAN_POINT ( 'NONE',  ( -24.53239521893647890, -29.54733954334097135, 16.68574937151005599 ) ) ;
#13149=ORIENTED_EDGE ( 'NONE', *, *, #10806, .F. ) ;
#13150=CARTESIAN_POINT ( 'NONE',  ( -4.473127245936431073, 31.51789735524192793, -37.94261489385728936 ) ) ;
#13151=CARTESIAN_POINT ( 'NONE',  ( -1.619063947482197729, -25.20140673341345305, 38.92136151114934961 ) ) ;
#13166=CARTESIAN_POINT ( 'NONE',  ( -55.25297051322618813, 0.01483298743815085648, 0.001818774723749092123 ) ) ;
#13169=CARTESIAN_POINT ( 'NONE',  ( -20.47566262905010248, 25.06314747784837138, -16.24827521404660047 ) ) ;
#13173=CARTESIAN_POINT ( 'NONE',  ( -1.049817751779876129, -43.71287583013717182, 13.66628317065032583 ) ) ;
#13180=CARTESIAN_POINT ( 'NONE',  ( -4.178947244162567465, -37.51424432987625579, 31.41809272265961539 ) ) ;
#13193=CARTESIAN_POINT ( 'NONE',  ( -1.239374126674604337, 44.48112152129363750, 11.92219841463783503 ) ) ;
#13194=CARTESIAN_POINT ( 'NONE',  ( 14.74894986621300319, 4.490279961725991446E-15, -37.50000000000001421 ) ) ;
#13200=CARTESIAN_POINT ( 'NONE',  ( -25.21435515916044423, -16.39063784838720395, 30.48034229288656505 ) ) ;
#13203=CARTESIAN_POINT ( 'NONE',  ( -25.21435515916043357, 31.17620025257608418, 15.02493970636113474 ) ) ;
#13220=EDGE_CURVE ( 'NONE', #27068, #6724, #19569, .T. ) ;
#13228=ORIENTED_EDGE ( 'NONE', *, *, #5717, .T. ) ;
#13233=B_SPLINE_CURVE_WITH_KNOTS ( 'NONE', 3,
 ( #8740, #15777, #24588, #4848, #11321, #20090 ),
 .UNSPECIFIED., .F., .F.,
 ( 4, 2, 4 ),
 ( 1.734723475976807094E-18, 0.0004335184443140234316, 0.0008670368886280451284 ),
 .UNSPECIFIED. ) ;
#13240=ADVANCED_FACE ( 'NONE', ( #17835 ), #23986, .F. ) ;
#13241=CARTESIAN_POINT ( 'NONE',  ( -1.239374126674604337, -2.406737988131443906, -45.98822239537607715 ) ) ;
#13248=CARTESIAN_POINT ( 'NONE',  ( -25.21435515916025594, 1.749597353048488237E-16, -4.373993382621220594E-17 ) ) ;
#13249=CARTESIAN_POINT ( 'NONE',  ( -20.20612092514785019, -24.59769888281546102, -16.46550332780518033 ) ) ;
#13250=CARTESIAN_POINT ( 'NONE',  ( -55.24390624410018802, 0.001451500391951047672, 0.01032895241566990016 ) ) ;
#13254=VERTEX_POINT ( 'NONE', #19864 ) ;
#13259=ORIENTED_EDGE ( 'NONE', *, *, #10984, .T. ) ;
#13260=B_SPLINE_CURVE_WITH_KNOTS ( 'NONE', 3,
 ( #26839, #5395, #16626, #21611, #7424, #16331, #23400, #14307, #25420, #1083, #9723, #27550, #1218 ),
 .UNSPECIFIED., .F., .F.,
 ( 4, 3, 3, 3, 4 ),
 ( 6.938893903907227607E-18, 0.0007657099931970527554, 0.001531419946797919806, 0.002296279302920157302, 0.003061450627205762002 ),
 .UNSPECIFIED. ) ;
#13262=EDGE_LOOP ( 'NONE', ( #673, #8050, #8106, #1182 ) ) ;
#13264=B_SPLINE_CURVE_WITH_KNOTS ( 'NONE', 3,
 ( #25705, #4087, #17187, #6265, #6395, #27853, #12581 ),
 .UNSPECIFIED., .F., .F.,
 ( 4, 3, 4 ),
 ( 9.299800619644450092E-17, 0.009512539173626386249, 0.02506242213020836232 ),
 .UNSPECIFIED. ) ;
#13268=CARTESIAN_POINT ( 'NONE',  ( -1.019300379054419947, 25.26451264419699783, 38.21680004809136477 ) ) ;
#13271=CARTESIAN_POINT ( 'NONE',  ( -1.050230347699841582, 0.2550051351977194458, 45.79907861674081460 ) ) ;
#13276=CARTESIAN_POINT ( 'NONE',  ( -8.786685647604890903, 7.199674155858966529, -53.04920435127184675 ) ) ;
#13281=CARTESIAN_POINT ( 'NONE',  ( -55.25719721206881729, 0.01041086141212315547, 0.004044147484874825726 ) ) ;
#13284=CARTESIAN_POINT ( 'NONE',  ( -7.078251931573400491, 38.93060825814280435, 34.59014398252872269 ) ) ;
#13286=ORIENTED_EDGE ( 'NONE', *, *, #14850, .T. ) ;
#13293=EDGE_LOOP ( 'NONE', ( #20547, #3824, #9829, #26694 ) ) ;
#13294=CARTESIAN_POINT ( 'NONE',  ( -1.044557008772713402, -15.70482370518787718, 43.01636061109000053 ) ) ;
#13302=CARTESIAN_POINT ( 'NONE',  ( -28.13707043255157103, -7.802116958608856123, 21.52861750560947129 ) ) ;
#13303=CARTESIAN_POINT ( 'NONE',  ( -22.23342874802668234, 2.180636882146512079, -31.55488258420089664 ) ) ;
#13304=CARTESIAN_POINT ( 'NONE',  ( -1.239374126674604337, -25.08410696974269527, -38.61989855450929809 ) ) ;
#13306=CARTESIAN_POINT ( 'NONE',  ( -24.53239521893647890, -24.99972072650158950, -22.94500969220225883 ) ) ;
#13307=CARTESIAN_POINT ( 'NONE',  ( -1.239374126674604337, -11.92219841463861130, -44.48112152129341013 ) ) ;
#13312=EDGE_CURVE ( 'NONE', #12584, #13547, #23722, .T. ) ;
#13318=CARTESIAN_POINT ( 'NONE',  ( -7.733045908741333463, 45.70676731105722723, -25.81515396910878479 ) ) ;
#13321=EDGE_CURVE ( 'NONE', #25057, #6789, #12681, .T. ) ;
#13325=ORIENTED_EDGE ( 'NONE', *, *, #15862, .T. ) ;
#13327=( GEOMETRIC_REPRESENTATION_CONTEXT ( 3 ) GLOBAL_UNCERTAINTY_ASSIGNED_CONTEXT ( ( #5061 ) ) GLOBAL_UNIT_ASSIGNED_CONTEXT ( ( #10377, #1284, #12500 ) ) REPRESENTATION_CONTEXT ( 'NONE', 'WORKASPACE' ) );
#13332=FACE_OUTER_BOUND ( 'NONE', #1903, .T. ) ;
#13337=ADVANCED_FACE ( 'NONE', ( #5028 ), #12767, .F. ) ;
#13350=CARTESIAN_POINT ( 'NONE',  ( -28.13707043255157103, -7.802116958609158992, -21.52861750560936471 ) ) ;
#13354=LINE ( 'NONE', #13088, #17833 ) ;
#13361=CARTESIAN_POINT ( 'NONE',  ( -18.41936578851706230, 42.05131332928132082, 5.707900577128324215 ) ) ;
#13366=AXIS2_PLACEMENT_3D ( 'NONE', #23738, #9306, #6721 ) ;
#13367=AXIS2_PLACEMENT_3D ( 'NONE', #6572, #17775, #26273 ) ;
#13368=CARTESIAN_POINT ( 'NONE',  ( -20.57838717382308147, 10.78122205917000365, -27.96569011373090063 ) ) ;
#13379=CARTESIAN_POINT ( 'NONE',  ( -55.24728320129491266, 0.005114031043468944375, -0.01362040845703405695 ) ) ;
#13382=B_SPLINE_CURVE_WITH_KNOTS ( 'NONE', 3,
 ( #17517, #15068, #2109, #4141, #21426, #23466 ),
 .UNSPECIFIED., .F., .F.,
 ( 4, 2, 4 ),
 ( 4.055692965608002806E-16, 0.003576372551511211671, 0.007152745103022018283 ),
 .UNSPECIFIED. ) ;
#13393=EDGE_LOOP ( 'NONE', ( #10802, #2673, #21318, #20348 ) ) ;
#13398=ORIENTED_EDGE ( 'NONE', *, *, #3939, .F. ) ;
#13399=B_SPLINE_CURVE_WITH_KNOTS ( 'NONE', 3,
 ( #14443, #10296, #19054, #16170, #24972, #5232 ),
 .UNSPECIFIED., .F., .F.,
 ( 4, 2, 4 ),
 ( 4.906538933386797396E-18, 0.0004335151646191543395, 0.0008670303292383036917 ),
 .UNSPECIFIED. ) ;
#13403=CARTESIAN_POINT ( 'NONE',  ( -20.20700224038492721, 29.58392382092673500, -0.9908225410479557516 ) ) ;
#13415=CARTESIAN_POINT ( 'NONE',  ( -25.21435515916025594, 1.749597353048488237E-16, -4.373993382621220594E-17 ) ) ;
#13416=CARTESIAN_POINT ( 'NONE',  ( -1.049819078601898381, 0.5100232645225435402, 45.79653735114490587 ) ) ;
#13418=CARTESIAN_POINT ( 'NONE',  ( -4.178947244162633190, -45.38689110596704523, 18.28784278438497068 ) ) ;
#13424=CARTESIAN_POINT ( 'NONE',  ( -1.113548883309550375, 35.91246368318242332, 28.52482525634906096 ) ) ;
#13429=CARTESIAN_POINT ( 'NONE',  ( -7.733045908741331687, -5.980865481987790666, 52.15131830128831325 ) ) ;
#13430=ORIENTED_EDGE ( 'NONE', *, *, #23080, .T. ) ;
#13435=EDGE_LOOP ( 'NONE', ( #27774, #11576, #16644, #13149 ) ) ;
#13436=CARTESIAN_POINT ( 'NONE',  ( -28.13707043255157103, 6.342158660427315020, 22.00298671236732773 ) ) ;
#13437=VECTOR ( 'NONE', #22360, 1000.000000000000114 ) ;
#13439=ORIENTED_EDGE ( 'NONE', *, *, #20477, .T. ) ;
#13441=VECTOR ( 'NONE', #4151, 1000.000000000000000 ) ;
#13446=DIRECTION ( 'NONE',  ( -0.7071067818211355105, 9.150583771627656306E-17, -0.7071067805519596350 ) ) ;
#13449=CARTESIAN_POINT ( 'NONE',  ( -12.94347594948481373, -23.08810053288719999, -42.93165645342850212 ) ) ;
#13451=CARTESIAN_POINT ( 'NONE',  ( -1.058473599757826511, -38.06357893967446415, -25.48501014712384816 ) ) ;
#13453=FACE_OUTER_BOUND ( 'NONE', #8914, .T. ) ;
#13458=CARTESIAN_POINT ( 'NONE',  ( -1.046935749539993799, 27.93995161054695231, -36.28605774377773230 ) ) ;
#13462=CARTESIAN_POINT ( 'NONE',  ( -5.986830583229478364, 19.95149887249920440, 46.64941882410778362 ) ) ;
#13467=CARTESIAN_POINT ( 'NONE',  ( -23.79223135445719350, 16.82181692922858929, 28.60983116549946814 ) ) ;
#13472=AXIS2_PLACEMENT_3D ( 'NONE', #21167, #25784, #6077 ) ;
#13473=( BOUNDED_SURFACE ( )  B_SPLINE_SURFACE ( 3, 1, ( 
 ( #21097, #18806 ),
 ( #21250, #5866 ),
 ( #3690, #19098 ),
 ( #27295, #27871 ) ),
 .UNSPECIFIED., .F., .F., .F. ) 
 B_SPLINE_SURFACE_WITH_KNOTS ( ( 4, 4 ),
 ( 2, 2 ),
 ( 0.000000000000000000, 1.000000000000000000 ),
 ( 0.000000000000000000, 1.000000000000000000 ),
 .UNSPECIFIED. ) 
 GEOMETRIC_REPRESENTATION_ITEM ( )  RATIONAL_B_SPLINE_SURFACE ( (
 ( 1.000000000000000000, 1.000000000000000000),
 ( 0.7789835883360576307, 0.9689951854195403280),
 ( 0.7789835883360576307, 0.9689951854195403280),
 ( 1.000000000000000000, 1.000000000000000000) ) ) 
 REPRESENTATION_ITEM ( '' )  SURFACE ( )  );
#13476=CARTESIAN_POINT ( 'NONE',  ( -1.619063947482197729, 46.30105812165548684, 2.489035965910320503 ) ) ;
#13478=PRODUCT_DEFINITION_FORMATION_WITH_SPECIFIED_SOURCE ( 'ANY', '', #2083, .NOT_KNOWN. ) ;
#13490=CARTESIAN_POINT ( 'NONE',  ( -55.24300891470648622, 0.009439835024157980023, -0.002702093572889658051 ) ) ;
#13501=CARTESIAN_POINT ( 'NONE',  ( -1.031422197589716205, 37.93675465142474224, -25.67058493451456513 ) ) ;
#13503=CARTESIAN_POINT ( 'NONE',  ( -20.20700224038492365, -8.199606986804534259, -28.44216453106533748 ) ) ;
#13514=EDGE_CURVE ( 'NONE', #18375, #1898, #4788, .T. ) ;
#13515=ORIENTED_EDGE ( 'NONE', *, *, #7165, .F. ) ;
#13518=CARTESIAN_POINT ( 'NONE',  ( -2.911734481061402757, -12.03743348210748998, 46.11606034418773703 ) ) ;
#13522=EDGE_LOOP ( 'NONE', ( #25163, #7318, #22994, #9362 ) ) ;
#13527=ORIENTED_EDGE ( 'NONE', *, *, #19555, .T. ) ;
#13536=DIRECTION ( 'NONE',  ( 1.000000000000000000, -6.938893903907226837E-18, 1.734723475976806709E-18 ) ) ;
#13537=CARTESIAN_POINT ( 'NONE',  ( -19.53423201713129842, 1.355459634611817431E-16, -3.388649086529543578E-17 ) ) ;
#13538=CARTESIAN_POINT ( 'NONE',  ( -20.47566338032516597, 18.81547714195514232, 23.19796701701855213 ) ) ;
#13547=VERTEX_POINT ( 'NONE', #8615 ) ;
#13549=CARTESIAN_POINT ( 'NONE',  ( -9.156249394959713683, -25.18996226954579498, 48.32878616081037393 ) ) ;
#13554=CARTESIAN_POINT ( 'NONE',  ( -1.048994561756786625, 37.49601524795411223, -26.29622118251694829 ) ) ;
#13557=CARTESIAN_POINT ( 'NONE',  ( -20.24419206586952313, -18.44224248888889051, -23.20105925399719382 ) ) ;
#13560=LINE ( 'NONE', #17737, #13437 ) ;
#13561=CARTESIAN_POINT ( 'NONE',  ( -23.79223135445719706, 32.40779366744838796, -7.157574570129257907 ) ) ;
#13572=LINE ( 'NONE', #6514, #15215 ) ;
#13574=CARTESIAN_POINT ( 'NONE',  ( -5.986830583229486358, -33.39046620690942291, -38.20088153919488860 ) ) ;
#13579=CARTESIAN_POINT ( 'NONE',  ( -20.38016308990358993, -29.73560196176845238, 1.509191766064522655 ) ) ;
#13582=LINE ( 'NONE', #27363, #20799 ) ;
#13594=CARTESIAN_POINT ( 'NONE',  ( -8.786685647604890903, 52.67761315067286176, -9.545808661480789326 ) ) ;
#13595=CARTESIAN_POINT ( 'NONE',  ( -1.048171036023513913, 27.73816396939564299, -36.44209502233717046 ) ) ;
#13598=ORIENTED_EDGE ( 'NONE', *, *, #16415, .T. ) ;
#13603=CARTESIAN_POINT ( 'NONE',  ( -7.711401346138175406, -45.70592430511711513, -25.75361633141480766 ) ) ;
#13606=CARTESIAN_POINT ( 'NONE',  ( -20.21097721650787449, -28.05863614620931656, 9.464413208035370673 ) ) ;
#13607=( BOUNDED_SURFACE ( )  B_SPLINE_SURFACE ( 3, 1, ( 
 ( #23396, #1077 ),
 ( #3650, #19066 ),
 ( #28107, #25961 ),
 ( #19612, #10308 ) ),
 .UNSPECIFIED., .F., .F., .F. ) 
 B_SPLINE_SURFACE_WITH_KNOTS ( ( 4, 4 ),
 ( 2, 2 ),
 ( 0.000000000000000000, 1.000000000000000000 ),
 ( 0.000000000000000000, 1.000000000000000000 ),
 .UNSPECIFIED. ) 
 GEOMETRIC_REPRESENTATION_ITEM ( )  RATIONAL_B_SPLINE_SURFACE ( (
 ( 1.000000000000000000, 1.000000000000000000),
 ( 0.9593753223639863714, 0.9995975284513187731),
 ( 0.9593753223639863714, 0.9995975284513187731),
 ( 1.000000000000000000, 1.000000000000000000) ) ) 
 REPRESENTATION_ITEM ( '' )  SURFACE ( )  );
#13609=CARTESIAN_POINT ( 'NONE',  ( -25.21435515916042647, 25.00736669481023355, -23.92354251275945742 ) ) ;
#13626=CARTESIAN_POINT ( 'NONE',  ( -55.25297051322618813, -0.01354497706059463319, 0.006313402748432140991 ) ) ;
#13641=CARTESIAN_POINT ( 'NONE',  ( -1.463510566862823437, -38.76366072687759612, 25.15876608740857989 ) ) ;
#13649=( BOUNDED_SURFACE ( )  B_SPLINE_SURFACE ( 3, 1, ( 
 ( #24114, #28397 ),
 ( #19765, #10865 ),
 ( #26249, #13150 ),
 ( #19627, #12859 ) ),
 .UNSPECIFIED., .F., .F., .F. ) 
 B_SPLINE_SURFACE_WITH_KNOTS ( ( 4, 4 ),
 ( 2, 2 ),
 ( 0.000000000000000000, 1.000000000000000000 ),
 ( 0.000000000000000000, 1.000000000000000000 ),
 .UNSPECIFIED. ) 
 GEOMETRIC_REPRESENTATION_ITEM ( )  RATIONAL_B_SPLINE_SURFACE ( (
 ( 1.000000000000000000, 1.000000000000000000),
 ( 0.7789835883360578528, 0.9689951854195403280),
 ( 0.7789835883360578528, 0.9689951854195403280),
 ( 1.000000000000000000, 1.000000000000000000) ) ) 
 REPRESENTATION_ITEM ( '' )  SURFACE ( )  );
#13653=CARTESIAN_POINT ( 'NONE',  ( -1.045287976400383290, 36.12803364096649972, 28.14015102489766917 ) ) ;
#13662=CARTESIAN_POINT ( 'NONE',  ( -20.21097721650787093, 28.26295598655185515, 8.835581399094868615 ) ) ;
#13663=CARTESIAN_POINT ( 'NONE',  ( -20.24419206586952313, 16.36655224501367911, -24.70913649113835930 ) ) ;
#13664=CARTESIAN_POINT ( 'NONE',  ( 14.74894986621300319, -1.023413983156987147E-16, 2.558534957892467869E-17 ) ) ;
#13669=ORIENTED_EDGE ( 'NONE', *, *, #21702, .F. ) ;
#13670=ORIENTED_EDGE ( 'NONE', *, *, #19181, .T. ) ;
#13678=EDGE_CURVE ( 'NONE', #4666, #23146, #19862, .T. ) ;
#13680=CARTESIAN_POINT ( 'NONE',  ( -20.20700224038492010, -8.199606986804138131, 28.44216453106544762 ) ) ;
#13688=( BOUNDED_SURFACE ( )  B_SPLINE_SURFACE ( 3, 1, ( 
 ( #21331, #19172 ),
 ( #14304, #25939 ),
 ( #3918, #21470 ),
 ( #1742, #16186 ) ),
 .UNSPECIFIED., .F., .F., .F. ) 
 B_SPLINE_SURFACE_WITH_KNOTS ( ( 4, 4 ),
 ( 2, 2 ),
 ( 0.000000000000000000, 1.000000000000000000 ),
 ( 0.000000000000000000, 1.000000000000000000 ),
 .UNSPECIFIED. ) 
 GEOMETRIC_REPRESENTATION_ITEM ( )  RATIONAL_B_SPLINE_SURFACE ( (
 ( 1.000000000000000000, 1.000000000000000000),
 ( 0.9934239774497838349, 0.8357310067453913582),
 ( 0.9934239774497838349, 0.8357310067453913582),
 ( 1.000000000000000000, 1.000000000000000000) ) ) 
 REPRESENTATION_ITEM ( '' )  SURFACE ( )  );
#13691=DIRECTION ( 'NONE',  ( 5.541455922705463698E-20, -5.223019709708320524E-21, 1.000000000000000000 ) ) ;
#13699=CARTESIAN_POINT ( 'NONE',  ( -1.583189561560255143, 25.21827308671289103, 38.94740041318266321 ) ) ;
#13700=CARTESIAN_POINT ( 'NONE',  ( -8.786685647604890903, -9.545808661480235102, 52.67761315067295413 ) ) ;
#13703=EDGE_CURVE ( 'NONE', #1901, #6478, #15725, .T. ) ;
#13709=ORIENTED_EDGE ( 'NONE', *, *, #9725, .T. ) ;
#13729=EDGE_CURVE ( 'NONE', #14557, #4557, #9957, .T. ) ;
#13730=DIRECTION ( 'NONE',  ( 0.000000000000000000, -5.223019709708190374E-21, 1.000000000000000000 ) ) ;
#13732=CARTESIAN_POINT ( 'NONE',  ( -1.583189561560256253, -25.21827308671203838, 38.94740041318321744 ) ) ;
#13744=CARTESIAN_POINT ( 'NONE',  ( -6.574463467970635300, 47.03022655117400319, -20.55340846381147202 ) ) ;
#13748=CARTESIAN_POINT ( 'NONE',  ( -20.57838717382308147, 16.28767523336157552, 25.16001208503087838 ) ) ;
#13752=EDGE_LOOP ( 'NONE', ( #24630, #21052, #14600, #15352 ) ) ;
#13755=ORIENTED_EDGE ( 'NONE', *, *, #27256, .T. ) ;
#13762=( NAMED_UNIT ( * ) SI_UNIT ( $, .STERADIAN. ) SOLID_ANGLE_UNIT ( ) );
#13773=CARTESIAN_POINT ( 'NONE',  ( -1.583189561560255143, -44.83405390829663872, 11.94859433442949381 ) ) ;
#13776=VERTEX_POINT ( 'NONE', #8577 ) ;
#13777=ORIENTED_EDGE ( 'NONE', *, *, #6348, .F. ) ;
#13798=B_SPLINE_CURVE_WITH_KNOTS ( 'NONE', 3,
 ( #14896, #25285, #10178, #5557, #17617, #17468, #24257, #24400, #8856, #26256 ),
 .UNSPECIFIED., .F., .F.,
 ( 4, 2, 2, 2, 4 ),
 ( 5.898697549827394244E-18, 0.0003346267210630972291, 0.0006692534421261884950, 0.001003880163189279761, 0.001338506884252371135 ),
 .UNSPECIFIED. ) ;
#13800=VERTEX_POINT ( 'NONE', #19369 ) ;
#13811=CARTESIAN_POINT ( 'NONE',  ( -8.786685647604890903, 23.24040270374391426, -48.22796981442777309 ) ) ;
#13816=( BOUNDED_SURFACE ( )  B_SPLINE_SURFACE ( 3, 1, ( 
 ( #16417, #22917 ),
 ( #2740, #25202 ),
 ( #5476, #14236 ),
 ( #23058, #11520 ) ),
 .UNSPECIFIED., .F., .F., .F. ) 
 B_SPLINE_SURFACE_WITH_KNOTS ( ( 4, 4 ),
 ( 2, 2 ),
 ( 0.000000000000000000, 1.000000000000000000 ),
 ( 0.000000000000000000, 1.000000000000000000 ),
 .UNSPECIFIED. ) 
 GEOMETRIC_REPRESENTATION_ITEM ( )  RATIONAL_B_SPLINE_SURFACE ( (
 ( 1.000000000000000000, 1.000000000000000000),
 ( 0.7789835883360578528, 0.9689951854195403280),
 ( 0.7789835883360578528, 0.9689951854195403280),
 ( 1.000000000000000000, 1.000000000000000000) ) ) 
 REPRESENTATION_ITEM ( '' )  SURFACE ( )  );
#13819=CARTESIAN_POINT ( 'NONE',  ( -1.619063947482197729, -43.26576862488421682, 16.67502769180607203 ) ) ;
#13824=CARTESIAN_POINT ( 'NONE',  ( -28.41354790283022069, -1.249099604786914286, 23.16239616762932130 ) ) ;
#13828=CARTESIAN_POINT ( 'NONE',  ( -4.162674018437131807, -37.46098494546610880, -31.44946543094281921 ) ) ;
#13829=CARTESIAN_POINT ( 'NONE',  ( -20.57838717382308147, -1.611677988432568709, -29.92853265176830746 ) ) ;
#13833=CIRCLE ( 'NONE', #4643, 53.53553390275978785 ) ;
#13834=EDGE_LOOP ( 'NONE', ( #10719, #15666, #27745, #23465 ) ) ;
#13835=CONICAL_SURFACE ( 'NONE', #19359, 34.60786435723138510, 0.8559913436420825139 ) ;
#13847=LINE ( 'NONE', #20900, #25 ) ;
#13848=CARTESIAN_POINT ( 'NONE',  ( -1.044556982611280160, 1.643392503293353180, 45.76404732357876526 ) ) ;
#13854=CARTESIAN_POINT ( 'NONE',  ( -55.24390624410018802, -0.007503127514281482044, 0.007245494385991411469 ) ) ;
#13875=EDGE_CURVE ( 'NONE', #1901, #16572, #17630, .T. ) ;
#13880=CARTESIAN_POINT ( 'NONE',  ( -23.79223135445718995, -32.40779366744830270, 7.157574570129486169 ) ) ;
#13887=ORIENTED_EDGE ( 'NONE', *, *, #25109, .F. ) ;
#13901=CARTESIAN_POINT ( 'NONE',  ( -55.24390624410018802, -0.009374879212970498032, 0.004572280736701721943 ) ) ;
#13904=ADVANCED_FACE ( 'NONE', ( #3972 ), #16648, .F. ) ;
#13905=B_SPLINE_CURVE_WITH_KNOTS ( 'NONE', 3,
 ( #3436, #13010, #18689, #10862, #21799, #19624, #12214, #28394, #17457, #26665 ),
 .UNSPECIFIED., .F., .F.,
 ( 4, 2, 2, 2, 4 ),
 ( 2.845980932296679661E-16, 0.0003346187017559042144, 0.0006692374035115238257, 0.001003856105267143329, 0.001338474807022762940 ),
 .UNSPECIFIED. ) ;
#13908=DIRECTION ( 'NONE',  ( -0.7637818620346800147, 0.5345501402766299481, 0.3617919495470734992 ) ) ;
#13914=DIRECTION ( 'NONE',  ( -0.7563875759206388771, -0.6531865459554678788, 0.03500244528122777032 ) ) ;
#13916=CYLINDRICAL_SURFACE ( 'NONE', #17103, 20.00000000000000000 ) ;
#13917=CARTESIAN_POINT ( 'NONE',  ( -1.113548883309557924, 16.03115934825529010, -42.96943836789110094 ) ) ;
#13925=ORIENTED_EDGE ( 'NONE', *, *, #11709, .T. ) ;
#13928=CARTESIAN_POINT ( 'NONE',  ( -25.21435515916043713, -34.29329011225952684, 4.655591116594705703 ) ) ;
#13931=CARTESIAN_POINT ( 'NONE',  ( -1.058197053496163109, -28.32422455455050425, 36.00048521498983689 ) ) ;
#13933=CARTESIAN_POINT ( 'NONE',  ( -22.23226125620943705, -24.24619897613461461, 20.31044300692198945 ) ) ;
#13934=CARTESIAN_POINT ( 'NONE',  ( -8.786685647604855376, -7.199674155859337787, -53.04920435127184675 ) ) ;
#13940=CARTESIAN_POINT ( 'NONE',  ( -1.031422197589711987, -28.14735071801769095, -36.13727897780115939 ) ) ;
#13946=ORIENTED_EDGE ( 'NONE', *, *, #7419, .F. ) ;
#13957=CARTESIAN_POINT ( 'NONE',  ( -55.24340739397742794, -0.009386184976284812215, 0.003826481709800012669 ) ) ;
#13961=VERTEX_POINT ( 'NONE', #2660 ) ;
#13962=CARTESIAN_POINT ( 'NONE',  ( -55.24300891470648622, 0.008142823778062486390, -0.005486913146696510354 ) ) ;
#13963=CARTESIAN_POINT ( 'NONE',  ( -1.048996300304502194, -36.59642367107725391, 27.53442103413733122 ) ) ;
#13966=CARTESIAN_POINT ( 'NONE',  ( -7.711401346138401891, 6.030154970217631138, 52.11446537925907307 ) ) ;
#13968=CARTESIAN_POINT ( 'NONE',  ( -1.019300379054419725, 42.90269154183429379, -16.06793277092006988 ) ) ;
#13980=ADVANCED_FACE ( 'NONE', ( #16038 ), #26544, .F. ) ;
#13986=CARTESIAN_POINT ( 'NONE',  ( -55.25297051322618813, 0.002853887643044372355, 0.01466904165775517396 ) ) ;
#14004=CARTESIAN_POINT ( 'NONE',  ( -1.239374126674604337, 16.50008610789298302, -42.99367564261284258 ) ) ;
#14012=B_SPLINE_CURVE_WITH_KNOTS ( 'NONE', 3,
 ( #13132, #15132, #13557, #316, #17589, #26510 ),
 .UNSPECIFIED., .F., .F.,
 ( 4, 2, 4 ),
 ( 0.000000000000000000, 0.0004335184443140231063, 0.0008670368886280462126 ),
 .UNSPECIFIED. ) ;
#14013=CARTESIAN_POINT ( 'NONE',  ( -55.24271866751342941, -0.006757859501009785483, 0.006671293903667892267 ) ) ;
#14015=CARTESIAN_POINT ( 'NONE',  ( 14.74894986621300319, -1.023413983156987147E-16, 2.558534957892467869E-17 ) ) ;
#14022=CARTESIAN_POINT ( 'NONE',  ( -23.79248802219723302, 33.03370827286732947, -3.207402715357277057 ) ) ;
#14027=ORIENTED_EDGE ( 'NONE', *, *, #18156, .F. ) ;
#14049=CARTESIAN_POINT ( 'NONE',  ( -24.53237795827032741, 29.54731592868594348, 16.68575684089460864 ) ) ;
#14063=ORIENTED_EDGE ( 'NONE', *, *, #16381, .T. ) ;
#14065=DIRECTION ( 'NONE',  ( 1.000000000000000000, -6.938893903907226837E-18, 1.734723475976806709E-18 ) ) ;
#14070=ADVANCED_FACE ( 'NONE', ( #14158 ), #13688, .F. ) ;
#14071=CARTESIAN_POINT ( 'NONE',  ( -1.048172774974293064, -43.23017713506512649, 15.11899685083868761 ) ) ;
#14076=CARTESIAN_POINT ( 'NONE',  ( -8.786685647604890903, -37.00619870957905277, 38.68584556812340480 ) ) ;
#14080=CARTESIAN_POINT ( 'NONE',  ( -7.078251931573400491, 5.101176922830666705, -51.82710018979476274 ) ) ;
#14081=B_SPLINE_CURVE_WITH_KNOTS ( 'NONE', 3,
 ( #28327, #17532, #8624, #16373, #11631, #4867, #23017 ),
 .UNSPECIFIED., .F., .F.,
 ( 4, 3, 4 ),
 ( 0.000000000000000000, 0.006568092053401776258, 0.02506242213020846987 ),
 .UNSPECIFIED. ) ;
#14089=EDGE_CURVE ( 'NONE', #6415, #11326, #4063, .T. ) ;
#14095=EDGE_CURVE ( 'NONE', #26061, #5381, #9215, .T. ) ;
#14108=B_SPLINE_CURVE_WITH_KNOTS ( 'NONE', 3,
 ( #7254, #6822, #24683, #15720, #9112, #4934, #22366, #15426 ),
 .UNSPECIFIED., .F., .F.,
 ( 4, 2, 2, 4 ),
 ( 2.194186273941487942E-16, 0.002761568181852859863, 0.005523136363705500283, 0.01104627272741079066 ),
 .UNSPECIFIED. ) ;
#14109=CARTESIAN_POINT ( 'NONE',  ( -1.056502255334265339, -0.5104472526216820016, 45.80535052436398047 ) ) ;
#14111=CARTESIAN_POINT ( 'NONE',  ( -1.031422197589716205, 43.06660437151330711, 15.60268798220593389 ) ) ;
#14119=EDGE_CURVE ( 'NONE', #6842, #4463, #609, .T. ) ;
#14120=CARTESIAN_POINT ( 'NONE',  ( -4.780792508754312387, -18.84172549606840619, 45.80716263181253822 ) ) ;
#14123=ORIENTED_EDGE ( 'NONE', *, *, #22838, .F. ) ;
#14138=CARTESIAN_POINT ( 'NONE',  ( -55.24300891470648622, 0.002702093572889911754, 0.009439835024157509913 ) ) ;
#14141=CARTESIAN_POINT ( 'NONE',  ( -55.24271866751342941, -0.001545935011626541761, -0.009369360294294543784 ) ) ;
#14150=EDGE_CURVE ( 'NONE', #8163, #20232, #7860, .T. ) ;
#14156=CARTESIAN_POINT ( 'NONE',  ( -1.113427685306999759, -1.967672929087495470, -45.82016658690750432 ) ) ;
#14158=FACE_OUTER_BOUND ( 'NONE', #6622, .T. ) ;
#14166=CARTESIAN_POINT ( 'NONE',  ( -1.113548883309539272, 25.34012683631610940, 38.22628252420783213 ) ) ;
#14167=CARTESIAN_POINT ( 'NONE',  ( -1.619063947482201282, -16.67502769180592992, -43.26576862488428077 ) ) ;
#14168=CARTESIAN_POINT ( 'NONE',  ( -5.986830583229461489, 46.64941882410799678, -19.95149887249867859 ) ) ;
#14170=ORIENTED_EDGE ( 'NONE', *, *, #1602, .F. ) ;
#14173=CARTESIAN_POINT ( 'NONE',  ( -1.031422197589716205, 25.67058493451498080, 37.93675465142445091 ) ) ;
#14174=CARTESIAN_POINT ( 'NONE',  ( -25.21435515916043713, -6.169479169075696490, -34.05351380035330777 ) ) ;
#14192=FACE_OUTER_BOUND ( 'NONE', #28465, .T. ) ;
#14193=CARTESIAN_POINT ( 'NONE',  ( -20.20700224038492721, -27.82980252387826781, -10.08426345511578504 ) ) ;
#14211=CARTESIAN_POINT ( 'NONE',  ( -20.57838717382308147, -25.16001208503117326, -16.28767523336112433 ) ) ;
#14216=CARTESIAN_POINT ( 'NONE',  ( -1.259920593601969729, 12.06711544331625596, 44.39818421957802741 ) ) ;
#14220=B_SPLINE_CURVE_WITH_KNOTS ( 'NONE', 3,
 ( #28153, #6025, #10210, #27884, #8589, #14780, #16944, #3557 ),
 .UNSPECIFIED., .F., .F.,
 ( 4, 2, 2, 4 ),
 ( 2.225109362706117716E-16, 0.002761568181852862899, 0.005523136363705503753, 0.01104627272741078893 ),
 .UNSPECIFIED. ) ;
#14236=CARTESIAN_POINT ( 'NONE',  ( -4.473127245936431073, -18.25038884639838699, 45.82513704981563052 ) ) ;
#14237=CARTESIAN_POINT ( 'NONE',  ( -55.24300891470650754, 0.008142823778062566187, 0.005486913146700293786 ) ) ;
#14241=CARTESIAN_POINT ( 'NONE',  ( 180.4657679828686980, 20.00000000000000000, 2.762351802624772237E-15 ) ) ;
#14253=B_SPLINE_CURVE_WITH_KNOTS ( 'NONE', 3,
 ( #23013, #26875, #18536, #7317, #3279, #9910, #22876 ),
 .UNSPECIFIED., .F., .F.,
 ( 4, 3, 4 ),
 ( 0.000000000000000000, 0.006568092053401830901, 0.02506242213020847681 ),
 .UNSPECIFIED. ) ;
#14258=VECTOR ( 'NONE', #25775, 1000.000000000000114 ) ;
#14259=VECTOR ( 'NONE', #3447, 1000.000000000000000 ) ;
#14265=CARTESIAN_POINT ( 'NONE',  ( -25.21435515916025594, 1.749597353048488237E-16, -4.373993382621220594E-17 ) ) ;
#14266=CARTESIAN_POINT ( 'NONE',  ( -1.583189561560256253, 46.33203782964461936, -2.490696082060027017 ) ) ;
#14267=DIRECTION ( 'NONE',  ( 5.541455922705463698E-20, -5.223019709708320524E-21, 1.000000000000000000 ) ) ;
#14274=CARTESIAN_POINT ( 'NONE',  ( -22.23226125620944060, -26.80886670319648246, -16.78323347921907427 ) ) ;
#14279=LINE ( 'NONE', #7841, #14972 ) ;
#14283=CARTESIAN_POINT ( 'NONE',  ( -28.41354790283022069, 19.47297445639550162, -12.60397206714839413 ) ) ;
#14287=CARTESIAN_POINT ( 'NONE',  ( -1.049819825607599455, 27.33096219556293249, 36.75053263699358297 ) ) ;
#14289=EDGE_CURVE ( 'NONE', #3600, #26826, #14802, .T. ) ;
#14298=CARTESIAN_POINT ( 'NONE',  ( -1.019300379054419947, 44.15350047934399669, -12.21833869579480236 ) ) ;
#14301=CARTESIAN_POINT ( 'NONE',  ( -1.464342487929859660, -2.431462367721655138, -46.14921266389555399 ) ) ;
#14304=CARTESIAN_POINT ( 'NONE',  ( -55.24300891470650754, -0.009812809446892518245, 0.0003472257464213444889 ) ) ;
#14306=CARTESIAN_POINT ( 'NONE',  ( -1.045287976400362417, -44.00138577190658395, -12.68782741917276446 ) ) ;
#14307=CARTESIAN_POINT ( 'NONE',  ( -1.050229599974470185, -13.90955673306158147, -43.63650726458059381 ) ) ;
#14308=DIRECTION ( 'NONE',  ( 0.000000000000000000, 5.223019709708233256E-21, -1.000000000000000000 ) ) ;
#14310=EDGE_LOOP ( 'NONE', ( #28017, #254, #18417, #19932 ) ) ;
#14321=CARTESIAN_POINT ( 'NONE',  ( -55.24198130335446422, -0.006617369590168513567, -0.006527480770976002225 ) ) ;
#14323=CARTESIAN_POINT ( 'NONE',  ( -55.24728320129491266, 0.008013189884950885564, -0.01214321324516771938 ) ) ;
#14326=CARTESIAN_POINT ( 'NONE',  ( -2.911734481061388990, -46.11606034418772282, -12.03743348210763031 ) ) ;
#14330=VERTEX_POINT ( 'NONE', #9164 ) ;
#14332=VERTEX_POINT ( 'NONE', #17654 ) ;
#14336=CARTESIAN_POINT ( 'NONE',  ( -55.24390624410018802, -0.001451500391950358120, -0.01032895241567008057 ) ) ;
#14337=CARTESIAN_POINT ( 'NONE',  ( -25.21435515916043357, -25.00736669481038987, -23.92354251275926558 ) ) ;
#14339=CARTESIAN_POINT ( 'NONE',  ( -20.20700224038492010, -0.9908225410480588913, -29.58392382092672435 ) ) ;
#14341=VERTEX_POINT ( 'NONE', #19670 ) ;
#14342=CIRCLE ( 'NONE', #4237, 53.53553390275978785 ) ;
#14346=CARTESIAN_POINT ( 'NONE',  ( -1.044557008772713624, 28.22896138707370994, -36.05793264791354602 ) ) ;
#14350=ORIENTED_EDGE ( 'NONE', *, *, #9809, .T. ) ;
#14354=CARTESIAN_POINT ( 'NONE',  ( -1.045287976400365970, -43.05558670614224326, 15.59869763335140469 ) ) ;
#14356=ORIENTED_EDGE ( 'NONE', *, *, #9233, .T. ) ;
#14366=ADVANCED_FACE ( 'NONE', ( #6737 ), #5976, .F. ) ;
#14369=CARTESIAN_POINT ( 'NONE',  ( -55.24390624410018802, 0.007245494385991918876, 0.007503127514281743120 ) ) ;
#14371=EDGE_CURVE ( 'NONE', #11877, #13127, #26571, .T. ) ;
#14374=AXIS2_PLACEMENT_3D ( 'NONE', #4123, #8456, #17353 ) ;
#14375=( BOUNDED_SURFACE ( )  B_SPLINE_SURFACE ( 3, 1, ( 
 ( #11208, #13501 ),
 ( #11347, #24615 ),
 ( #11635, #19983 ),
 ( #551, #18102 ) ),
 .UNSPECIFIED., .F., .F., .F. ) 
 B_SPLINE_SURFACE_WITH_KNOTS ( ( 4, 4 ),
 ( 2, 2 ),
 ( 0.000000000000000000, 1.000000000000000000 ),
 ( 0.000000000000000000, 1.000000000000000000 ),
 .UNSPECIFIED. ) 
 GEOMETRIC_REPRESENTATION_ITEM ( )  RATIONAL_B_SPLINE_SURFACE ( (
 ( 1.000000000000000000, 1.000000000000000000),
 ( 0.9593753223639863714, 0.9995975284513187731),
 ( 0.9593753223639863714, 0.9995975284513187731),
 ( 1.000000000000000000, 1.000000000000000000) ) ) 
 REPRESENTATION_ITEM ( '' )  SURFACE ( )  );
#14377=CARTESIAN_POINT ( 'NONE',  ( -1.050230346682696103, 37.05264119692688496, -26.91946103437118509 ) ) ;
#14382=CARTESIAN_POINT ( 'NONE',  ( -21.81686047589431965, -33.92779429964186733, 18.24499610240074432 ) ) ;
#14383=CARTESIAN_POINT ( 'NONE',  ( -1.045287976400351981, -15.59869763335126436, -43.05558670614231431 ) ) ;
#14402=FACE_OUTER_BOUND ( 'NONE', #7155, .T. ) ;
#14403=AXIS2_PLACEMENT_3D ( 'NONE', #1550, #17748, #14505 ) ;
#14405=EDGE_CURVE ( 'NONE', #6724, #14674, #1826, .T. ) ;
#14408=ORIENTED_EDGE ( 'NONE', *, *, #28081, .T. ) ;
#14410=LINE ( 'NONE', #13436, #24562 ) ;
#14421=CARTESIAN_POINT ( 'NONE',  ( -20.21097721650788159, -23.76068422213743503, 17.67178726257384014 ) ) ;
#14423=CARTESIAN_POINT ( 'NONE',  ( -20.90916690077963835, -38.93431874629077782, -7.054312691028836291 ) ) ;
#14427=CARTESIAN_POINT ( 'NONE',  ( -20.38016308990357217, 24.94368798801375675, 16.25718651464953624 ) ) ;
#14428=EDGE_CURVE ( 'NONE', #10456, #1639, #25147, .T. ) ;
#14433=EDGE_CURVE ( 'NONE', #17046, #21703, #9891, .T. ) ;
#14434=DIRECTION ( 'NONE',  ( -0.7563875759206388771, 0.2351350468682910366, 0.6104009704506918599 ) ) ;
#14441=CARTESIAN_POINT ( 'NONE',  ( -1.619063947482197729, -25.20140673341401438, -38.92136151114898723 ) ) ;
#14443=CARTESIAN_POINT ( 'NONE',  ( -20.57838717382308147, 23.26537097894132344, 18.89542499756474569 ) ) ;
#14459=CARTESIAN_POINT ( 'NONE',  ( -1.619063947482197729, -38.92136151114888776, 25.20140673341416360 ) ) ;
#14468=CARTESIAN_POINT ( 'NONE',  ( -55.24198130335446422, -0.004163123460802295971, -0.008310594958153156783 ) ) ;
#14470=CARTESIAN_POINT ( 'NONE',  ( -55.24728320129491266, -0.01453410071985621575, -0.0006547948648749734972 ) ) ;
#14484=CARTESIAN_POINT ( 'NONE',  ( -1.045287976400383290, -44.00138577190632816, 12.68782741917368106 ) ) ;
#14485=FACE_OUTER_BOUND ( 'NONE', #13522, .T. ) ;
#14491=CARTESIAN_POINT ( 'NONE',  ( -55.24390624410018802, -0.001451500391952595045, 0.01032895241566660592 ) ) ;
#14492=CARTESIAN_POINT ( 'NONE',  ( -1.050231094221206973, 43.47885872350356351, -14.39477892760314326 ) ) ;
#14505=DIRECTION ( 'NONE',  ( 0.000000000000000000, 5.223019709707975211E-21, -1.000000000000000000 ) ) ;
#14509=CARTESIAN_POINT ( 'NONE',  ( -1.239374126674604337, 2.406737988131122830, -45.98822239537607004 ) ) ;
#14516=CARTESIAN_POINT ( 'NONE',  ( -21.81686047589426991, -16.72402253294291796, 34.70276904128906637 ) ) ;
#14522=ORIENTED_EDGE ( 'NONE', *, *, #26439, .T. ) ;
#14531=CARTESIAN_POINT ( 'NONE',  ( -8.786685647604885574, 6.096987947571466530E-17, -1.524246986892866633E-17 ) ) ;
#14536=( BOUNDED_SURFACE ( )  B_SPLINE_SURFACE ( 3, 1, ( 
 ( #2091, #21963 ),
 ( #15467, #8881 ),
 ( #17638, #2225 ),
 ( #6433, #10893 ) ),
 .UNSPECIFIED., .F., .F., .F. ) 
 B_SPLINE_SURFACE_WITH_KNOTS ( ( 4, 4 ),
 ( 2, 2 ),
 ( 0.000000000000000000, 1.000000000000000000 ),
 ( 0.000000000000000000, 1.000000000000000000 ),
 .UNSPECIFIED. ) 
 GEOMETRIC_REPRESENTATION_ITEM ( )  RATIONAL_B_SPLINE_SURFACE ( (
 ( 1.000000000000000000, 1.000000000000000000),
 ( 0.9593753223639863714, 0.9995975284513187731),
 ( 0.9593753223639863714, 0.9995975284513187731),
 ( 1.000000000000000000, 1.000000000000000000) ) ) 
 REPRESENTATION_ITEM ( '' )  SURFACE ( )  );
#14539=CARTESIAN_POINT ( 'NONE',  ( -55.24390624410018802, 0.007245494385991918876, 0.007503127514281743120 ) ) ;
#14546=CARTESIAN_POINT ( 'NONE',  ( -20.20700224038492010, 24.51628800869071867, 16.58740185276683832 ) ) ;
#14551=( BOUNDED_SURFACE ( )  B_SPLINE_SURFACE ( 3, 1, ( 
 ( #26636, #14111 ),
 ( #11829, #4775 ),
 ( #20597, #22930 ),
 ( #18435, #20307 ) ),
 .UNSPECIFIED., .F., .F., .F. ) 
 B_SPLINE_SURFACE_WITH_KNOTS ( ( 4, 4 ),
 ( 2, 2 ),
 ( 0.000000000000000000, 1.000000000000000000 ),
 ( 0.000000000000000000, 1.000000000000000000 ),
 .UNSPECIFIED. ) 
 GEOMETRIC_REPRESENTATION_ITEM ( )  RATIONAL_B_SPLINE_SURFACE ( (
 ( 1.000000000000000000, 1.000000000000000000),
 ( 0.9593753223639863714, 0.9995975284513187731),
 ( 0.9593753223639863714, 0.9995975284513187731),
 ( 1.000000000000000000, 1.000000000000000000) ) ) 
 REPRESENTATION_ITEM ( '' )  SURFACE ( )  );
#14553=VERTEX_POINT ( 'NONE', #12868 ) ;
#14556=ORIENTED_EDGE ( 'NONE', *, *, #27256, .F. ) ;
#14557=VERTEX_POINT ( 'NONE', #10037 ) ;
#14558=ORIENTED_EDGE ( 'NONE', *, *, #15988, .T. ) ;
#14568=CARTESIAN_POINT ( 'NONE',  ( -1.113427685306993542, 45.82016658690751854, -1.967672929087340261 ) ) ;
#14590=CARTESIAN_POINT ( 'NONE',  ( -20.57838717382308147, 7.715628353033680220, -28.96176188950220975 ) ) ;
#14592=FACE_OUTER_BOUND ( 'NONE', #13293, .T. ) ;
#14594=FACE_OUTER_BOUND ( 'NONE', #26767, .T. ) ;
#14596=CARTESIAN_POINT ( 'NONE',  ( -24.53237795827004319, 33.71192251888839309, -3.868415699415555853 ) ) ;
#14600=ORIENTED_EDGE ( 'NONE', *, *, #14979, .T. ) ;
#14604=DIRECTION ( 'NONE',  ( 0.000000000000000000, 5.223019709707975211E-21, -1.000000000000000000 ) ) ;
#14606=DIRECTION ( 'NONE',  ( -1.000000000000000000, 6.938893903907226837E-18, -1.734723475976806709E-18 ) ) ;
#14608=DIRECTION ( 'NONE',  ( -1.000000000000000000, 6.938893903907226837E-18, -1.734723475976806709E-18 ) ) ;
#14630=B_SPLINE_CURVE_WITH_KNOTS ( 'NONE', 3,
 ( #11315, #16057, #26561, #9313, #20378, #4698, #5121 ),
 .UNSPECIFIED., .F., .F.,
 ( 4, 3, 4 ),
 ( 9.269414991073849107E-17, 0.009512539173626381045, 0.02506242213020854620 ),
 .UNSPECIFIED. ) ;
#14634=CARTESIAN_POINT ( 'NONE',  ( -20.24419206586951603, -1.282847120831435594, -29.61012937815439372 ) ) ;
#14636=ORIENTED_EDGE ( 'NONE', *, *, #19981, .F. ) ;
#14642=VERTEX_POINT ( 'NONE', #24123 ) ;
#14644=CARTESIAN_POINT ( 'NONE',  ( -1.155001620486257208, -28.62773628245643209, 35.88346938217584636 ) ) ;
#14650=CARTESIAN_POINT ( 'NONE',  ( -1.619063947482194177, 29.22875152547808852, 35.99532424477347092 ) ) ;
#14656=ORIENTED_EDGE ( 'NONE', *, *, #7800, .F. ) ;
#14661=EDGE_CURVE ( 'NONE', #1690, #15158, #8862, .T. ) ;
#14672=CARTESIAN_POINT ( 'NONE',  ( -1.045287976400365970, 28.14015102489882736, 36.12803364096558312 ) ) ;
#14674=VERTEX_POINT ( 'NONE', #26543 ) ;
#14680=CARTESIAN_POINT ( 'NONE',  ( -20.21097721712959228, 23.76068428613707439, 17.67178718142832494 ) ) ;
#14696=CARTESIAN_POINT ( 'NONE',  ( -4.473127245936431073, -26.34600523034567487, -41.70021447285044047 ) ) ;
#14698=CARTESIAN_POINT ( 'NONE',  ( -20.57838717382308147, 28.96176188950229502, 7.715628353033378239 ) ) ;
#14700=ORIENTED_EDGE ( 'NONE', *, *, #24872, .T. ) ;
#14704=CARTESIAN_POINT ( 'NONE',  ( -1.045287976400362417, -44.00138577190658395, -12.68782741917276446 ) ) ;
#14712=EDGE_LOOP ( 'NONE', ( #12578, #18404, #18847, #13515 ) ) ;
#14718=EDGE_CURVE ( 'NONE', #12310, #5017, #18396, .T. ) ;
#14724=FACE_OUTER_BOUND ( 'NONE', #13393, .T. ) ;
#14729=VECTOR ( 'NONE', #10915, 1000.000000000000000 ) ;
#14730=CARTESIAN_POINT ( 'NONE',  ( -8.786685647604855376, -7.199674155859337787, -53.04920435127184675 ) ) ;
#14736=CARTESIAN_POINT ( 'NONE',  ( -20.57838717382308147, -16.28767523336102130, 25.16001208503123365 ) ) ;
#14739=ORIENTED_EDGE ( 'NONE', *, *, #23080, .F. ) ;
#14740=VERTEX_POINT ( 'NONE', #22386 ) ;
#14747=ADVANCED_FACE ( 'NONE', ( #20204 ), #17880, .F. ) ;
#14749=CARTESIAN_POINT ( 'NONE',  ( 180.4657679828686980, -1.252232817320263489E-15, 3.130582043300658722E-16 ) ) ;
#14754=EDGE_CURVE ( 'NONE', #15797, #26004, #6008, .T. ) ;
#14756=CYLINDRICAL_SURFACE ( 'NONE', #6191, 37.50000000000001421 ) ;
#14778=CARTESIAN_POINT ( 'NONE',  ( -12.82751273423881599, 8.715310691360238948, -48.09651489336683738 ) ) ;
#14780=CARTESIAN_POINT ( 'NONE',  ( -6.588769196390765970, -50.13301368233292976, 11.07780292579747083 ) ) ;
#14782=CARTESIAN_POINT ( 'NONE',  ( -25.21435515916025594, 1.749597353048488237E-16, -4.373993382621220594E-17 ) ) ;
#14784=ORIENTED_EDGE ( 'NONE', *, *, #7280, .T. ) ;
#14788=ORIENTED_EDGE ( 'NONE', *, *, #22131, .T. ) ;
#14789=CARTESIAN_POINT ( 'NONE',  ( -1.056502255334264895, 14.64009593116162478, 43.40574022158757828 ) ) ;
#14791=FACE_OUTER_BOUND ( 'NONE', #21811, .T. ) ;
#14794=CARTESIAN_POINT ( 'NONE',  ( -7.078251931573400491, -38.93060825814254144, -34.59014398252902112 ) ) ;
#14800=DIRECTION ( 'NONE',  ( -0.7563875759206388771, -0.6104009704506927481, 0.2351350468682887607 ) ) ;
#14802=LINE ( 'NONE', #21701, #7850 ) ;
#14804=CARTESIAN_POINT ( 'NONE',  ( -28.41354790283022069, -18.00456980371910376, -14.62505768302794529 ) ) ;
#14817=ORIENTED_EDGE ( 'NONE', *, *, #22531, .F. ) ;
#14827=CYLINDRICAL_SURFACE ( 'NONE', #26708, 20.00000000000000000 ) ;
#14834=ORIENTED_EDGE ( 'NONE', *, *, #23282, .T. ) ;
#14836=CARTESIAN_POINT ( 'NONE',  ( -8.786685647604890903, -9.545808661480235102, 52.67761315067295413 ) ) ;
#14838=ORIENTED_EDGE ( 'NONE', *, *, #20722, .F. ) ;
#14839=ORIENTED_EDGE ( 'NONE', *, *, #23556, .T. ) ;
#14846=CIRCLE ( 'NONE', #9820, 20.00000000000000000 ) ;
#14850=EDGE_CURVE ( 'NONE', #3600, #19910, #21195, .T. ) ;
#14861=CARTESIAN_POINT ( 'NONE',  ( -25.21435515916043357, -16.39063784838764093, -30.48034229288631991 ) ) ;
#14868=CONICAL_SURFACE ( 'NONE', #5680, 34.60786435723138510, 0.8559913436420825139 ) ;
#14872=CARTESIAN_POINT ( 'NONE',  ( -55.24340739397742084, 0.003826481709804142178, -0.009386184976286654491 ) ) ;
#14873=CARTESIAN_POINT ( 'NONE',  ( -25.21435515916043357, 6.169479169075458458, -34.05351380035335751 ) ) ;
#14876=CARTESIAN_POINT ( 'NONE',  ( -16.86833981943427929, -5.948101187261880085, -43.82216161736206317 ) ) ;
#14885=CARTESIAN_POINT ( 'NONE',  ( -1.056502255334265339, -14.64009593116072949, 43.40574022158788381 ) ) ;
#14889=ORIENTED_EDGE ( 'NONE', *, *, #21911, .F. ) ;
#14892=CARTESIAN_POINT ( 'NONE',  ( -20.20612092514784663, 23.26073121129637045, -18.30568145913851907 ) ) ;
#14894=VERTEX_POINT ( 'NONE', #749 ) ;
#14896=CARTESIAN_POINT ( 'NONE',  ( -1.619063947482197729, -29.22875152547781852, -35.99532424477369830 ) ) ;
#14897=ORIENTED_EDGE ( 'NONE', *, *, #5648, .T. ) ;
#14910=CARTESIAN_POINT ( 'NONE',  ( -20.57838717382308502, 25.16001208503106668, -16.28767523336130196 ) ) ;
#14921=CARTESIAN_POINT ( 'NONE',  ( -22.23226125620943705, -20.31044300692189708, -24.24619897613468211 ) ) ;
#14926=CARTESIAN_POINT ( 'NONE',  ( -8.259864102781492079, -38.68084189741939127, 36.24929574824932388 ) ) ;
#14937=CARTESIAN_POINT ( 'NONE',  ( -20.57838717382308147, -18.89542499756516847, -23.26537097894098594 ) ) ;
#14941=CARTESIAN_POINT ( 'NONE',  ( -24.53237795827026346, 16.68575684089495326, -29.54731592868563439 ) ) ;
#14958=CARTESIAN_POINT ( 'NONE',  ( -8.786685647604931759, 47.14957014837394667, 25.35688121747446999 ) ) ;
#14967=B_SPLINE_CURVE_WITH_KNOTS ( 'NONE', 3,
 ( #20447, #4907, #24498, #11955, #18269, #24789 ),
 .UNSPECIFIED., .F., .F.,
 ( 4, 2, 4 ),
 ( 1.734723475976806902E-18, 0.0004335151646191491353, 0.0008670303292382965359 ),
 .UNSPECIFIED. ) ;
#14968=LINE ( 'NONE', #12389, #1504 ) ;
#14970=B_SPLINE_CURVE_WITH_KNOTS ( 'NONE', 3,
 ( #4609, #6788, #6645, #4902, #19867, #3134, #15397, #21895, #22177, #24207 ),
 .UNSPECIFIED., .F., .F.,
 ( 4, 2, 2, 2, 4 ),
 ( 8.673617379884035472E-19, 0.0003346267210630925128, 0.0006692534421261841582, 0.001003880163189275858, 0.001338506884252367449 ),
 .UNSPECIFIED. ) ;
#14972=VECTOR ( 'NONE', #5670, 999.9999999999997726 ) ;
#14974=ADVANCED_FACE ( 'NONE', ( #10405 ), #25500, .F. ) ;
#14977=ADVANCED_FACE ( 'NONE', ( #21323 ), #11690, .F. ) ;
#14978=CARTESIAN_POINT ( 'NONE',  ( -55.24300891470650754, -0.009225237711100996510, 0.003362556190412404646 ) ) ;
#14979=EDGE_CURVE ( 'NONE', #25910, #23596, #22542, .T. ) ;
#14984=CARTESIAN_POINT ( 'NONE',  ( -55.24390624410018802, -0.009374879212966679906, -0.004572280736703028189 ) ) ;
#14987=CARTESIAN_POINT ( 'NONE',  ( -22.34422965417122953, 37.30738373203627845, 6.759368364653937533 ) ) ;
#14994=CARTESIAN_POINT ( 'NONE',  ( -1.539760825549689294, 44.72358953107748647, 11.93465943778467597 ) ) ;
#14995=ORIENTED_EDGE ( 'NONE', *, *, #15957, .T. ) ;
#14996=B_SPLINE_CURVE_WITH_KNOTS ( 'NONE', 3,
 ( #25462, #5735, #12330, #23297, #21258, #19105, #3549, #18535, #27301, #5431 ),
 .UNSPECIFIED., .F., .F.,
 ( 4, 2, 2, 2, 4 ),
 ( 1.563658610346375379E-18, 0.0003346267210630944644, 0.0006692534421261873024, 0.001003880163189280195, 0.001338506884252373087 ),
 .UNSPECIFIED. ) ;
#14997=ORIENTED_EDGE ( 'NONE', *, *, #10878, .T. ) ;
#14999=EDGE_CURVE ( 'NONE', #7798, #23222, #25656, .T. ) ;
#15003=CARTESIAN_POINT ( 'NONE',  ( -55.24340739397742084, 0.009386184976286932047, 0.003826481709803695053 ) ) ;
#15012=ORIENTED_EDGE ( 'NONE', *, *, #6512, .T. ) ;
#15016=CARTESIAN_POINT ( 'NONE',  ( -7.078251931573406708, 34.59014398252973166, 38.93060825814192327 ) ) ;
#15019=CARTESIAN_POINT ( 'NONE',  ( 14.74894986621300319, -1.025372615548127706E-16, 37.50000000000001421 ) ) ;
#15026=CARTESIAN_POINT ( 'NONE',  ( -1.323830074806774615, -16.42382241777507090, 43.04593525292983003 ) ) ;
#15032=ORIENTED_EDGE ( 'NONE', *, *, #13678, .F. ) ;
#15034=CARTESIAN_POINT ( 'NONE',  ( -1.113548883309547710, 1.968251867498868934, -45.82026503946952545 ) ) ;
#15035=CARTESIAN_POINT ( 'NONE',  ( -25.21435515916043357, -15.02493970636125198, 31.17620025257602379 ) ) ;
#15038=CARTESIAN_POINT ( 'NONE',  ( -1.049817751779893227, 14.63752841325048237, -43.39729912094385611 ) ) ;
#15043=CARTESIAN_POINT ( 'NONE',  ( -55.24300891470648622, 0.007734635432133147095, 0.006048736206180498759 ) ) ;
#15052=FACE_OUTER_BOUND ( 'NONE', #19386, .T. ) ;
#15054=CARTESIAN_POINT ( 'NONE',  ( -8.786685647604706162, -38.68584556812290032, 37.00619870957955015 ) ) ;
#15068=CARTESIAN_POINT ( 'NONE',  ( -24.53239521893650377, -22.94500969220219488, 24.99972072650167476 ) ) ;
#15070=CARTESIAN_POINT ( 'NONE',  ( -55.24340739397742084, -0.005344433640972736689, -0.008612749836246649457 ) ) ;
#15071=CARTESIAN_POINT ( 'NONE',  ( -22.34422965417124018, -27.39717383755262148, 26.20925041532883881 ) ) ;
#15072=CARTESIAN_POINT ( 'NONE',  ( -55.24390624410018802, 0.009209468562451588944, -0.004896917417127890151 ) ) ;
#15083=CARTESIAN_POINT ( 'NONE',  ( -12.82751273423876270, 48.43568301531151121, -6.573887447703007147 ) ) ;
#15084=CARTESIAN_POINT ( 'NONE',  ( -20.37983603106074426, -28.74620395171555742, 7.753708011498863684 ) ) ;
#15097=EDGE_CURVE ( 'NONE', #6273, #26826, #21855, .T. ) ;
#15102=ADVANCED_FACE ( 'NONE', ( #9211 ), #24380, .F. ) ;
#15106=CARTESIAN_POINT ( 'NONE',  ( -1.239374126674604337, -35.79060836339833429, -28.97829083655425819 ) ) ;
#15110=EDGE_LOOP ( 'NONE', ( #13777, #20771, #25249, #2287 ) ) ;
#15112=CARTESIAN_POINT ( 'NONE',  ( -1.239374126674604337, 11.92219841463891861, 44.48112152129332486 ) ) ;
#15113=CARTESIAN_POINT ( 'NONE',  ( -28.41354790283022069, -18.00456980371888704, 14.62505768302820464 ) ) ;
#15117=CARTESIAN_POINT ( 'NONE',  ( -1.019300379054419947, 35.83762006677442002, 28.53917295602858673 ) ) ;
#15121=ORIENTED_EDGE ( 'NONE', *, *, #7457, .T. ) ;
#15125=CARTESIAN_POINT ( 'NONE',  ( -20.57838717382308147, -27.96569011373093971, -10.78122205916989529 ) ) ;
#15131=CARTESIAN_POINT ( 'NONE',  ( -25.21435515916025594, 1.749597353048488237E-16, -4.373993382621220594E-17 ) ) ;
#15132=CARTESIAN_POINT ( 'NONE',  ( -20.20612092514784308, -18.30568145913859368, -23.26073121129629939 ) ) ;
#15136=CARTESIAN_POINT ( 'NONE',  ( -22.34422965417127216, -5.100074259622869199, -37.57019010019544680 ) ) ;
#15140=EDGE_CURVE ( 'NONE', #11627, #22401, #6921, .T. ) ;
#15147=AXIS2_PLACEMENT_3D ( 'NONE', #12127, #20896, #1185 ) ;
#15153=CARTESIAN_POINT ( 'NONE',  ( -5.986830583229477476, 11.27873876172141365, -49.46736940480261779 ) ) ;
#15156=CARTESIAN_POINT ( 'NONE',  ( -20.47566338032527611, 23.19796701701867647, -18.81547714195482612 ) ) ;
#15158=VERTEX_POINT ( 'NONE', #22319 ) ;
#15161=ORIENTED_EDGE ( 'NONE', *, *, #7499, .T. ) ;
#15163=ORIENTED_EDGE ( 'NONE', *, *, #10638, .T. ) ;
#15174=CARTESIAN_POINT ( 'NONE',  ( -28.41354790283022069, 22.41474081378001060, -5.969609727608100158 ) ) ;
#15177=CARTESIAN_POINT ( 'NONE',  ( -20.57838717382308147, -29.92853265176832878, -1.611677988432255848 ) ) ;
#15178=DIRECTION ( 'NONE',  ( 1.000000000000000000, -6.938893903907226837E-18, 1.734723475976806709E-18 ) ) ;
#15180=ORIENTED_EDGE ( 'NONE', *, *, #947, .F. ) ;
#15181=VERTEX_POINT ( 'NONE', #23331 ) ;
#15184=EDGE_CURVE ( 'NONE', #22553, #22201, #8454, .T. ) ;
#15193=VECTOR ( 'NONE', #167, 1000.000000000000000 ) ;
#15197=CIRCLE ( 'NONE', #16599, 34.60786435723138510 ) ;
#15198=ORIENTED_EDGE ( 'NONE', *, *, #9707, .F. ) ;
#15200=CONICAL_SURFACE ( 'NONE', #4184, 34.60786435723138510, 0.8559913436420825139 ) ;
#15204=DIRECTION ( 'NONE',  ( -0.7637818620346800147, -0.3617919495470753866, 0.5345501402766286159 ) ) ;
#15209=VECTOR ( 'NONE', #23000, 1000.000000000000000 ) ;
#15210=B_SPLINE_CURVE_WITH_KNOTS ( 'NONE', 3,
 ( #2303, #19882, #170, #8959, #17716, #24506 ),
 .UNSPECIFIED., .F., .F.,
 ( 4, 2, 4 ),
 ( 1.396102177145585797E-16, 0.003570751334075631788, 0.007141502668151123931 ),
 .UNSPECIFIED. ) ;
#15211=CARTESIAN_POINT ( 'NONE',  ( -25.21435515916043713, -25.00736669481004526, 23.92354251275963861 ) ) ;
#15215=VECTOR ( 'NONE', #22039, 1000.000000000000114 ) ;
#15218=CARTESIAN_POINT ( 'NONE',  ( -1.031422197589716205, -43.06660437151298026, 15.60268798220682562 ) ) ;
#15224=CARTESIAN_POINT ( 'NONE',  ( -20.20612091757424977, 28.48192249925588371, -8.058516044219283359 ) ) ;
#15228=CARTESIAN_POINT ( 'NONE',  ( -20.21097721650786738, -9.464413208035280078, -28.05863614620935209 ) ) ;
#15238=CARTESIAN_POINT ( 'NONE',  ( -4.178947244162647401, 41.47292084251672151, 25.96944194166747621 ) ) ;
#15242=VERTEX_POINT ( 'NONE', #12363 ) ;
#15250=CARTESIAN_POINT ( 'NONE',  ( -2.265401668238146815, 29.73100299756566756, -36.42007794497261841 ) ) ;
#15251=CARTESIAN_POINT ( 'NONE',  ( -1.050230346682677007, -0.0006945978172492803249, 45.79907861045643358 ) ) ;
#15252=ORIENTED_EDGE ( 'NONE', *, *, #23285, .T. ) ;
#15264=CARTESIAN_POINT ( 'NONE',  ( -1.031422197589711987, -37.93675465142491277, -25.67058493451428802 ) ) ;
#15268=LINE ( 'NONE', #8536, #11601 ) ;
#15270=VERTEX_POINT ( 'NONE', #17240 ) ;
#15278=CARTESIAN_POINT ( 'NONE',  ( -1.045287976400365970, -45.76855895860947498, -1.530335034933654859 ) ) ;
#15283=CARTESIAN_POINT ( 'NONE',  ( -1.048996300304498419, 0.7649764263858191971, 45.79145529752468491 ) ) ;
#15288=CARTESIAN_POINT ( 'NONE',  ( -20.20612091757420359, -23.26073043121646933, -18.30568244821369817 ) ) ;
#15289=ORIENTED_EDGE ( 'NONE', *, *, #10984, .F. ) ;
#15290=ORIENTED_EDGE ( 'NONE', *, *, #26566, .F. ) ;
#15293=CARTESIAN_POINT ( 'NONE',  ( -55.25719721206881729, 0.01115102788683387629, -0.0006290797159233242576 ) ) ;
#15294=CARTESIAN_POINT ( 'NONE',  ( -4.780792508754331038, 11.68149851467529210, 48.13366140756546230 ) ) ;
#15298=ORIENTED_EDGE ( 'NONE', *, *, #8880, .T. ) ;
#15299=CARTESIAN_POINT ( 'NONE',  ( -7.711401346138389457, 10.36923727626120773, -51.42722225669425740 ) ) ;
#15302=CARTESIAN_POINT ( 'NONE',  ( -1.046936909428682672, -37.78538189376526901, -25.87632113675147849 ) ) ;
#15309=B_SPLINE_CURVE_WITH_KNOTS ( 'NONE', 3,
 ( #27011, #19982, #15642, #24318, #24892, #22148 ),
 .UNSPECIFIED., .F., .F.,
 ( 4, 2, 4 ),
 ( 0.000000000000000000, 0.003570751334075635691, 0.007141502668151271382 ),
 .UNSPECIFIED. ) ;
#15313=EDGE_CURVE ( 'NONE', #6648, #565, #28011, .T. ) ;
#15314=ORIENTED_EDGE ( 'NONE', *, *, #1816, .F. ) ;
#15317=CARTESIAN_POINT ( 'NONE',  ( -1.259972190295306715, -38.49631882650665204, -25.19627397134285474 ) ) ;
#15321=DIRECTION ( 'NONE',  ( 1.000000000000000000, -6.938893903907226837E-18, 1.734723475976806709E-18 ) ) ;
#15325=CARTESIAN_POINT ( 'NONE',  ( -55.24340739397742794, 0.008612749836243148785, 0.005344433640974122733 ) ) ;
#15337=CARTESIAN_POINT ( 'NONE',  ( -55.24390624410018802, -0.007503127514277506058, -0.007245494385991484328 ) ) ;
#15346=ORIENTED_EDGE ( 'NONE', *, *, #2253, .F. ) ;
#15352=ORIENTED_EDGE ( 'NONE', *, *, #18060, .T. ) ;
#15353=DIRECTION ( 'NONE',  ( 1.000000000000000000, -6.938893903907226837E-18, 1.734723475976806709E-18 ) ) ;
#15354=EDGE_CURVE ( 'NONE', #28309, #20148, #26630, .T. ) ;
#15360=( BOUNDED_SURFACE ( )  B_SPLINE_SURFACE ( 3, 1, ( 
 ( #12706, #1212 ),
 ( #17027, #8135 ),
 ( #14872, #3507 ),
 ( #12291, #21059 ) ),
 .UNSPECIFIED., .F., .F., .F. ) 
 B_SPLINE_SURFACE_WITH_KNOTS ( ( 4, 4 ),
 ( 2, 2 ),
 ( 0.000000000000000000, 1.000000000000000000 ),
 ( 0.000000000000000000, 1.000000000000000000 ),
 .UNSPECIFIED. ) 
 GEOMETRIC_REPRESENTATION_ITEM ( )  RATIONAL_B_SPLINE_SURFACE ( (
 ( 1.000000000000000000, 1.000000000000000000),
 ( 0.9934239774497838349, 0.8357310067453913582),
 ( 0.9934239774497838349, 0.8357310067453913582),
 ( 1.000000000000000000, 1.000000000000000000) ) ) 
 REPRESENTATION_ITEM ( '' )  SURFACE ( )  );
#15366=ORIENTED_EDGE ( 'NONE', *, *, #20949, .F. ) ;
#15368=CARTESIAN_POINT ( 'NONE',  ( -20.57838717382308502, 28.96176188950218844, -7.715628353033780584 ) ) ;
#15379=CARTESIAN_POINT ( 'NONE',  ( -25.21435515916043357, -34.29329011225959079, -4.655591116594231416 ) ) ;
#15387=EDGE_CURVE ( 'NONE', #27689, #27511, #20104, .T. ) ;
#15391=CARTESIAN_POINT ( 'NONE',  ( -1.583189561560256253, 25.21827308671232615, -38.94740041318302559 ) ) ;
#15397=CARTESIAN_POINT ( 'NONE',  ( -1.113427685306994652, -25.34053733836502431, 38.22586258295222450 ) ) ;
#15398=VERTEX_POINT ( 'NONE', #25119 ) ;
#15399=CARTESIAN_POINT ( 'NONE',  ( -55.24390624410018802, -0.001451500391950358120, -0.01032895241567008057 ) ) ;
#15400=CARTESIAN_POINT ( 'NONE',  ( -55.24340739397742084, -0.006539691034612123317, 0.007744344507854589339 ) ) ;
#15405=CARTESIAN_POINT ( 'NONE',  ( -8.786685647604890903, -47.14957014837335691, 25.35688121747554291 ) ) ;
#15410=CARTESIAN_POINT ( 'NONE',  ( -20.57838717382308502, 23.26537097894105699, -18.89542499756508320 ) ) ;
#15413=EDGE_LOOP ( 'NONE', ( #24549, #24041, #9478, #3895 ) ) ;
#15420=LINE ( 'NONE', #15868, #1861 ) ;
#15422=CARTESIAN_POINT ( 'NONE',  ( -25.21435515916043713, 30.48034229288662544, 16.39063784838709736 ) ) ;
#15424=CARTESIAN_POINT ( 'NONE',  ( -1.323830074806773727, 43.04593525292991529, 16.42382241777492524 ) ) ;
#15426=CARTESIAN_POINT ( 'NONE',  ( -8.786685647604890903, -48.22796981442785835, -23.24040270374372952 ) ) ;
#15429=ORIENTED_EDGE ( 'NONE', *, *, #21911, .T. ) ;
#15435=FACE_BOUND ( 'NONE', #20584, .T. ) ;
#15439=ORIENTED_EDGE ( 'NONE', *, *, #15313, .F. ) ;
#15446=CARTESIAN_POINT ( 'NONE',  ( -1.056502255334264895, 13.66916755949850604, -43.72121397317227576 ) ) ;
#15450=CARTESIAN_POINT ( 'NONE',  ( -12.82751273423877514, -44.03362901246993744, 21.21958768041844579 ) ) ;
#15452=ADVANCED_FACE ( 'NONE', ( #5244 ), #4956, .T. ) ;
#15453=EDGE_CURVE ( 'NONE', #21625, #9465, #22534, .T. ) ;
#15455=ORIENTED_EDGE ( 'NONE', *, *, #2602, .T. ) ;
#15467=CARTESIAN_POINT ( 'NONE',  ( -55.24198130335446422, -0.009170435128244796077, 0.001516807524704069481 ) ) ;
#15482=CARTESIAN_POINT ( 'NONE',  ( -55.25297051322618813, 0.01354497706059944184, 0.006313402748433108967 ) ) ;
#15497=VERTEX_POINT ( 'NONE', #5686 ) ;
#15502=DIRECTION ( 'NONE',  ( 0.7637818620346800147, -0.3617919495470791613, -0.5345501402766260624 ) ) ;
#15507=ORIENTED_EDGE ( 'NONE', *, *, #5946, .F. ) ;
#15511=EDGE_CURVE ( 'NONE', #10615, #23186, #26985, .T. ) ;
#15512=CARTESIAN_POINT ( 'NONE',  ( -1.056502255334264895, -37.35734037467652513, -26.51074901220491498 ) ) ;
#15516=CARTESIAN_POINT ( 'NONE',  ( -8.786685647604931759, 47.14957014837394667, 25.35688121747446999 ) ) ;
#15519=CARTESIAN_POINT ( 'NONE',  ( -55.24390624410018802, -0.01032895241566962087, 0.001451500391950532459 ) ) ;
#15523=ORIENTED_EDGE ( 'NONE', *, *, #16485, .F. ) ;
#15527=CARTESIAN_POINT ( 'NONE',  ( -55.24340739397742794, 0.01010924026184123470, -0.0007387096945706978770 ) ) ;
#15528=ORIENTED_EDGE ( 'NONE', *, *, #26987, .T. ) ;
#15530=CARTESIAN_POINT ( 'NONE',  ( -1.155001620486249214, -12.20337535396710749, -44.25209926692303952 ) ) ;
#15542=ADVANCED_FACE ( 'NONE', ( #17173 ), #6557, .F. ) ;
#15545=CARTESIAN_POINT ( 'NONE',  ( -1.019300379054419725, -38.21680004809182662, -25.26451264419630860 ) ) ;
#15548=VERTEX_POINT ( 'NONE', #18921 ) ;
#15549=CARTESIAN_POINT ( 'NONE',  ( -1.045287976400365970, 44.00138577190666922, 12.68782741917247670 ) ) ;
#15551=CARTESIAN_POINT ( 'NONE',  ( -1.048171036023513025, 45.78635789057865679, 1.020520027229292470 ) ) ;
#15553=ORIENTED_EDGE ( 'NONE', *, *, #22131, .F. ) ;
#15554=ORIENTED_EDGE ( 'NONE', *, *, #21352, .T. ) ;
#15561=CARTESIAN_POINT ( 'NONE',  ( -20.20612091757427109, -16.46550228026411844, -24.59769958242381094 ) ) ;
#15562=VECTOR ( 'NONE', #28055, 1000.000000000000000 ) ;
#15564=DIRECTION ( 'NONE',  ( 1.000000000000000000, -6.938893903907226837E-18, 1.734723475976806709E-18 ) ) ;
#15565=CARTESIAN_POINT ( 'NONE',  ( -1.539763995773681282, 43.19716353142356269, 16.63252574782999460 ) ) ;
#15569=CARTESIAN_POINT ( 'NONE',  ( -1.583189561560252701, -29.24830400313139478, 36.01941156322819637 ) ) ;
#15570=VERTEX_POINT ( 'NONE', #18462 ) ;
#15579=CARTESIAN_POINT ( 'NONE',  ( -20.20700224038492721, -29.58392382092672790, 0.9908225410481621420 ) ) ;
#15591=LINE ( 'NONE', #13302, #20725 ) ;
#15594=CARTESIAN_POINT ( 'NONE',  ( -1.583189561560255143, -29.24830400313138767, 36.01941156322820348 ) ) ;
#15596=CARTESIAN_POINT ( 'NONE',  ( -21.41427618760457463, -23.81423075802597111, -19.54551635498120277 ) ) ;
#15597=CARTESIAN_POINT ( 'NONE',  ( -20.47566262905010248, -29.82700878811085232, -1.586617686065453725 ) ) ;
#15607=ORIENTED_EDGE ( 'NONE', *, *, #21752, .F. ) ;
#15618=ORIENTED_EDGE ( 'NONE', *, *, #2253, .T. ) ;
#15623=DIRECTION ( 'NONE',  ( 1.000000000000000000, 0.000000000000000000, 0.000000000000000000 ) ) ;
#15631=EDGE_CURVE ( 'NONE', #600, #20457, #15874, .T. ) ;
#15638=ORIENTED_EDGE ( 'NONE', *, *, #11941, .T. ) ;
#15642=CARTESIAN_POINT ( 'NONE',  ( -22.23226125620929139, -2.179935373562669643, -31.55376588768476509 ) ) ;
#15644=EDGE_CURVE ( 'NONE', #3087, #8562, #16731, .T. ) ;
#15645=FACE_OUTER_BOUND ( 'NONE', #22639, .T. ) ;
#15652=DIRECTION ( 'NONE',  ( 1.000000000000000000, -6.938893903907226837E-18, 1.734723475976806709E-18 ) ) ;
#15660=B_SPLINE_CURVE_WITH_KNOTS ( 'NONE', 3,
 ( #18786, #7874, #3521, #25276, #16633, #27123 ),
 .UNSPECIFIED., .F., .F.,
 ( 4, 2, 4 ),
 ( 0.000000000000000000, 0.0004335151646191514122, 0.0008670303292383013064 ),
 .UNSPECIFIED. ) ;
#15661=VERTEX_POINT ( 'NONE', #14704 ) ;
#15663=CARTESIAN_POINT ( 'NONE',  ( -55.25297051322618813, -0.01093108995495129139, -0.01019003092403723831 ) ) ;
#15665=VERTEX_POINT ( 'NONE', #23513 ) ;
#15666=ORIENTED_EDGE ( 'NONE', *, *, #19555, .F. ) ;
#15672=CARTESIAN_POINT ( 'NONE',  ( -1.583189561560256253, -44.83405390829680215, -11.94859433442884900 ) ) ;
#15676=CARTESIAN_POINT ( 'NONE',  ( -12.94347594948482083, 21.16159467081353540, -43.91326021875521946 ) ) ;
#15683=CARTESIAN_POINT ( 'NONE',  ( -1.048171036023494596, -37.64178826568587510, 26.08692787913908617 ) ) ;
#15686=CARTESIAN_POINT ( 'NONE',  ( -1.058473599757806971, -12.47539220917832914, 44.07591602137168252 ) ) ;
#15687=CARTESIAN_POINT ( 'NONE',  ( -20.57838717382308147, 29.92853265176831812, 1.611677988432465014 ) ) ;
#15693=CARTESIAN_POINT ( 'NONE',  ( -8.786685647604890903, -47.14957014837335691, 25.35688121747554291 ) ) ;
#15694=CARTESIAN_POINT ( 'NONE',  ( -55.24198130335446422, -0.001516807524703878444, -0.009170435128245257514 ) ) ;
#15700=CARTESIAN_POINT ( 'NONE',  ( -1.113427685307007975, 44.18561238466754304, 12.28784199929889098 ) ) ;
#15705=CARTESIAN_POINT ( 'NONE',  ( -1.045287976400362417, 25.66401692419989899, -37.92705037016767733 ) ) ;
#15708=EDGE_CURVE ( 'NONE', #384, #11657, #12872, .T. ) ;
#15711=LINE ( 'NONE', #6454, #934 ) ;
#15714=EDGE_CURVE ( 'NONE', #10003, #16572, #19745, .T. ) ;
#15715=DIRECTION ( 'NONE',  ( 1.000000000000000000, -6.938893903907226837E-18, 1.734723475976806709E-18 ) ) ;
#15720=CARTESIAN_POINT ( 'NONE',  ( -4.162674018437132695, -45.34593312138897403, -18.33413805792422124 ) ) ;
#15724=ORIENTED_EDGE ( 'NONE', *, *, #8205, .F. ) ;
#15725=B_SPLINE_CURVE_WITH_KNOTS ( 'NONE', 3,
 ( #19101, #23292, #16363, #16810, #23158, #23008 ),
 .UNSPECIFIED., .F., .F.,
 ( 4, 2, 4 ),
 ( 6.505213034913026604E-19, 0.0004335151646191484848, 0.0008670303292382963191 ),
 .UNSPECIFIED. ) ;
#15732=CARTESIAN_POINT ( 'NONE',  ( -8.786685647604890903, -37.00619870957961410, -38.68584556812286479 ) ) ;
#15738=ORIENTED_EDGE ( 'NONE', *, *, #18153, .T. ) ;
#15754=CARTESIAN_POINT ( 'NONE',  ( -1.619063947482197729, 44.80407745103800465, 11.94059994246113021 ) ) ;
#15766=CARTESIAN_POINT ( 'NONE',  ( -20.57838717382308147, 16.28767523336157552, 25.16001208503087838 ) ) ;
#15776=VECTOR ( 'NONE', #26055, 1000.000000000000114 ) ;
#15777=CARTESIAN_POINT ( 'NONE',  ( -20.20612092514784663, -28.48192215759672408, -8.058517256680987728 ) ) ;
#15779=LINE ( 'NONE', #20138, #23850 ) ;
#15780=ORIENTED_EDGE ( 'NONE', *, *, #24716, .T. ) ;
#15781=DIRECTION ( 'NONE',  ( -0.7563875759206388771, -0.6320336713238522419, -0.1685564395263275950 ) ) ;
#15782=CIRCLE ( 'NONE', #5211, 34.60786435723138510 ) ;
#15784=CARTESIAN_POINT ( 'NONE',  ( -1.583189561560256253, -16.68617981233733261, -43.29471907393735819 ) ) ;
#15786=ORIENTED_EDGE ( 'NONE', *, *, #6948, .T. ) ;
#15787=FACE_OUTER_BOUND ( 'NONE', #26746, .T. ) ;
#15788=B_SPLINE_CURVE_WITH_KNOTS ( 'NONE', 3,
 ( #21189, #25946, #16886, #4051, #17155, #10690, #3921 ),
 .UNSPECIFIED., .F., .F.,
 ( 4, 3, 4 ),
 ( 1.062518129035794345E-17, 0.0007657099931970561164, 0.001530725384384652287 ),
 .UNSPECIFIED. ) ;
#15797=VERTEX_POINT ( 'NONE', #20230 ) ;
#15806=CARTESIAN_POINT ( 'NONE',  ( 14.74894986621300141, -20.00000000000000000, 1.693217769544952477E-16 ) ) ;
#15817=FACE_OUTER_BOUND ( 'NONE', #11292, .T. ) ;
#15819=ORIENTED_EDGE ( 'NONE', *, *, #10633, .F. ) ;
#15823=CARTESIAN_POINT ( 'NONE',  ( -1.056502255334265339, -13.66916755949880802, -43.72121397317219049 ) ) ;
#15838=CARTESIAN_POINT ( 'NONE',  ( -1.048994561756789734, -0.7655149579820232919, 45.79144455904142319 ) ) ;
#15840=( BOUNDED_SURFACE ( )  B_SPLINE_SURFACE ( 3, 1, ( 
 ( #541, #2846 ),
 ( #9046, #18096 ),
 ( #26874, #7463 ),
 ( #22433, #17802 ) ),
 .UNSPECIFIED., .F., .F., .F. ) 
 B_SPLINE_SURFACE_WITH_KNOTS ( ( 4, 4 ),
 ( 2, 2 ),
 ( 0.000000000000000000, 1.000000000000000000 ),
 ( 0.000000000000000000, 1.000000000000000000 ),
 .UNSPECIFIED. ) 
 GEOMETRIC_REPRESENTATION_ITEM ( )  RATIONAL_B_SPLINE_SURFACE ( (
 ( 1.000000000000000000, 1.000000000000000000),
 ( 0.9593753223639863714, 0.9995975284513187731),
 ( 0.9593753223639863714, 0.9995975284513187731),
 ( 1.000000000000000000, 1.000000000000000000) ) ) 
 REPRESENTATION_ITEM ( '' )  SURFACE ( )  );
#15846=CARTESIAN_POINT ( 'NONE',  ( -1.049819825607590351, 14.63675055554442395, 43.39756533277866879 ) ) ;
#15858=CARTESIAN_POINT ( 'NONE',  ( -1.323439229708132769, 44.47813215539063947, 12.01475235539399300 ) ) ;
#15861=ORIENTED_EDGE ( 'NONE', *, *, #2865, .F. ) ;
#15862=EDGE_CURVE ( 'NONE', #10945, #6911, #7752, .T. ) ;
#15866=CARTESIAN_POINT ( 'NONE',  ( -4.473127245936434626, -45.82513704981530367, 18.25038884639918280 ) ) ;
#15868=CARTESIAN_POINT ( 'NONE',  ( -28.13707043255157103, -22.88591869784691823, -0.7675454997506192534 ) ) ;
#15869=CARTESIAN_POINT ( 'NONE',  ( -55.24390624410018802, -0.01032895241566633357, -0.001451500391952961289 ) ) ;
#15874=LINE ( 'NONE', #24682, #4631 ) ;
#15876=CARTESIAN_POINT ( 'NONE',  ( -9.156249394959713683, -8.027840202794317648, -53.90509764945126392 ) ) ;
#15877=CARTESIAN_POINT ( 'NONE',  ( -20.57838717382308147, -23.26537097894118133, -18.89542499756491978 ) ) ;
#15882=FACE_OUTER_BOUND ( 'NONE', #10123, .T. ) ;
#15884=( BOUNDED_SURFACE ( )  B_SPLINE_SURFACE ( 3, 1, ( 
 ( #27564, #1096 ),
 ( #9885, #25434 ),
 ( #5710, #21236 ),
 ( #12308, #1517 ) ),
 .UNSPECIFIED., .F., .F., .F. ) 
 B_SPLINE_SURFACE_WITH_KNOTS ( ( 4, 4 ),
 ( 2, 2 ),
 ( 0.000000000000000000, 1.000000000000000000 ),
 ( 0.000000000000000000, 1.000000000000000000 ),
 .UNSPECIFIED. ) 
 GEOMETRIC_REPRESENTATION_ITEM ( )  RATIONAL_B_SPLINE_SURFACE ( (
 ( 1.000000000000000000, 1.000000000000000000),
 ( 0.7789835883360578528, 0.9689951854195403280),
 ( 0.7789835883360578528, 0.9689951854195403280),
 ( 1.000000000000000000, 1.000000000000000000) ) ) 
 REPRESENTATION_ITEM ( '' )  SURFACE ( )  );
#15885=CARTESIAN_POINT ( 'NONE',  ( -20.20997486282892552, -0.3303743256173646836, 29.60348406988233450 ) ) ;
#15886=EDGE_CURVE ( 'NONE', #27831, #15797, #11149, .T. ) ;
#15897=EDGE_CURVE ( 'NONE', #18596, #11834, #13847, .T. ) ;
#15899=ORIENTED_EDGE ( 'NONE', *, *, #8005, .T. ) ;
#15907=CARTESIAN_POINT ( 'NONE',  ( -20.20612091757422846, -29.57813639663779526, -1.137293889216260512 ) ) ;
#15912=CARTESIAN_POINT ( 'NONE',  ( -8.786685647604898008, 48.22796981442765940, -23.24040270374399952 ) ) ;
#15917=CARTESIAN_POINT ( 'NONE',  ( -24.53239521893651442, 16.68574937151015192, 29.54733954334095358 ) ) ;
#15922=ORIENTED_EDGE ( 'NONE', *, *, #2687, .F. ) ;
#15923=CARTESIAN_POINT ( 'NONE',  ( -8.786685647604890903, 47.14957014837354876, -25.35688121747519119 ) ) ;
#15926=ORIENTED_EDGE ( 'NONE', *, *, #4648, .T. ) ;
#15932=CARTESIAN_POINT ( 'NONE',  ( -24.53239521893653219, 24.99972072650176713, 22.94500969220215580 ) ) ;
#15938=LINE ( 'NONE', #4997, #5856 ) ;
#15941=EDGE_LOOP ( 'NONE', ( #970, #22970, #5787, #10793 ) ) ;
#15948=CARTESIAN_POINT ( 'NONE',  ( -55.24198130335446422, 0.004163123460802997666, 0.008310594958152995454 ) ) ;
#15957=EDGE_CURVE ( 'NONE', #6789, #23146, #25793, .T. ) ;
#15958=ORIENTED_EDGE ( 'NONE', *, *, #20495, .T. ) ;
#15969=CARTESIAN_POINT ( 'NONE',  ( -1.019300379054419725, -44.15350047934408195, -12.21833869579447729 ) ) ;
#15974=EDGE_CURVE ( 'NONE', #23403, #4018, #20721, .T. ) ;
#15979=CARTESIAN_POINT ( 'NONE',  ( -1.045287976400379737, -37.92705037016725100, 25.66401692420055269 ) ) ;
#15983=CARTESIAN_POINT ( 'NONE',  ( -25.21435515916025594, 1.749597353048488237E-16, -4.373993382621220594E-17 ) ) ;
#15984=EDGE_CURVE ( 'NONE', #19211, #22079, #16294, .T. ) ;
#15988=EDGE_CURVE ( 'NONE', #18758, #14894, #9790, .T. ) ;
#15992=CARTESIAN_POINT ( 'NONE',  ( -1.058473599757832062, 44.07591602137171094, 12.47539220917817815 ) ) ;
#15997=CARTESIAN_POINT ( 'NONE',  ( -1.046936909428696438, 36.28616897897453697, -27.93981068760634656 ) ) ;
#15999=CARTESIAN_POINT ( 'NONE',  ( -1.583189561560256253, 2.490696082060512406, 46.33203782964458384 ) ) ;
#16001=CARTESIAN_POINT ( 'NONE',  ( -2.904412668506652473, -17.42365698954667863, 44.35433137608958276 ) ) ;
#16005=CARTESIAN_POINT ( 'NONE',  ( -20.21097721650787804, 23.76068422213757714, -17.67178726257366606 ) ) ;
#16009=CARTESIAN_POINT ( 'NONE',  ( -5.986830583229481917, -46.64941882410784757, 19.95149887249902321 ) ) ;
#16013=CARTESIAN_POINT ( 'NONE',  ( -25.21435515916043713, -30.48034229288650820, -16.39063784838731053 ) ) ;
#16021=CARTESIAN_POINT ( 'NONE',  ( -55.24271866751342941, 0.001545935011627245191, 0.009369360294294363373 ) ) ;
#16029=CARTESIAN_POINT ( 'NONE',  ( -1.583189561560256253, 11.94859433442902130, -44.83405390829675952 ) ) ;
#16034=CARTESIAN_POINT ( 'NONE',  ( -8.786685647604896232, 52.67761315067299677, 9.545808661480061019 ) ) ;
#16035=EDGE_CURVE ( 'NONE', #23403, #11830, #8408, .T. ) ;
#16038=FACE_OUTER_BOUND ( 'NONE', #20967, .T. ) ;
#16050=CARTESIAN_POINT ( 'NONE',  ( -24.53237795827028833, 3.868415699416160258, 33.71192251888858493 ) ) ;
#16053=FACE_OUTER_BOUND ( 'NONE', #21946, .T. ) ;
#16057=CARTESIAN_POINT ( 'NONE',  ( -10.86508079875774158, -50.67624451685647102, -6.877801422380581009 ) ) ;
#16060=CARTESIAN_POINT ( 'NONE',  ( -23.79223135445718995, -7.157574570129374258, -32.40779366744832402 ) ) ;
#16062=CARTESIAN_POINT ( 'NONE',  ( -1.045287976400351981, -15.59869763335126436, -43.05558670614231431 ) ) ;
#16075=EDGE_CURVE ( 'NONE', #22524, #9224, #18366, .T. ) ;
#16078=CARTESIAN_POINT ( 'NONE',  ( -1.031422197589711764, -44.01264471863837713, 12.69107518035547777 ) ) ;
#16083=ORIENTED_EDGE ( 'NONE', *, *, #2462, .F. ) ;
#16084=CARTESIAN_POINT ( 'NONE',  ( -8.786685647604892679, -53.04920435127177569, 7.199674155859498548 ) ) ;
#16092=VERTEX_POINT ( 'NONE', #14339 ) ;
#16108=CARTESIAN_POINT ( 'NONE',  ( -55.24300891470650754, 0.006048736206179803135, 0.007734635432136488173 ) ) ;
#16113=CARTESIAN_POINT ( 'NONE',  ( -8.786685647604898008, 38.68584556812353981, 37.00619870957891777 ) ) ;
#16117=CARTESIAN_POINT ( 'NONE',  ( -20.20700224038492010, -0.9908225410476447781, 29.58392382092673500 ) ) ;
#16118=ORIENTED_EDGE ( 'NONE', *, *, #11244, .T. ) ;
#16120=EDGE_CURVE ( 'NONE', #1416, #16414, #23157, .T. ) ;
#16121=ORIENTED_EDGE ( 'NONE', *, *, #12808, .T. ) ;
#16127=CARTESIAN_POINT ( 'NONE',  ( -2.911734481061392987, 2.802366807346851285, 47.57875121082947345 ) ) ;
#16130=ORIENTED_EDGE ( 'NONE', *, *, #17892, .T. ) ;
#16131=DIRECTION ( 'NONE',  ( 0.000000000000000000, 5.223019709708233256E-21, -1.000000000000000000 ) ) ;
#16135=CARTESIAN_POINT ( 'NONE',  ( -1.155001620486259206, 44.25209926692307505, -12.20337535396694051 ) ) ;
#16157=CARTESIAN_POINT ( 'NONE',  ( -20.38016308990357572, -27.81387210821415223, 10.62413300761014945 ) ) ;
#16163=CARTESIAN_POINT ( 'NONE',  ( -1.044557008772710516, -1.643388457097570088, 45.76404748504492659 ) ) ;
#16170=CARTESIAN_POINT ( 'NONE',  ( -20.24399999263414429, 23.20123049637393464, 18.44171895251370330 ) ) ;
#16183=CARTESIAN_POINT ( 'NONE',  ( -55.24728320129491266, -0.01137345571547045305, -0.009072670231978460439 ) ) ;
#16184=CARTESIAN_POINT ( 'NONE',  ( -21.41427618760447160, -29.81030852927061758, 7.777551129310369404 ) ) ;
#16186=CARTESIAN_POINT ( 'NONE',  ( -1.583189561560256253, 36.01941156322789794, -29.24830400313178203 ) ) ;
#16187=CARTESIAN_POINT ( 'NONE',  ( -20.21097721650786738, 9.464413208035470149, 28.05863614620928459 ) ) ;
#16194=CARTESIAN_POINT ( 'NONE',  ( -8.786685647604890903, -23.24040270374424466, -48.22796981442760256 ) ) ;
#16198=EDGE_LOOP ( 'NONE', ( #24526, #974, #21071, #24774, #2390, #20726, #19072, #12332, #20520, #9042, #1149, #11050, #7619, #2496, #25747, #6787, #5877, #12055, #11801, #19922, #1122, #742, #26042, #10036, #25779, #15252, #20583, #20414, #14700, #19352, #1628, #20095, #15554, #996, #5001, #18852, #14350, #23845, #13286, #15958, #7968, #10254, #22301, #16863, #18703, #16893, #15899, #3904, #11926, #19766, #25983, #6644, #18313, #28218, #26394, #11062, #4208, #11855, #13228, #3055, #16266, #2876, #10904, #21534 ) ) ;
#16200=VECTOR ( 'NONE', #7050, 1000.000000000000000 ) ;
#16206=ADVANCED_FACE ( 'NONE', ( #3544 ), #23038, .T. ) ;
#16207=CARTESIAN_POINT ( 'NONE',  ( -4.473127245936431073, -31.51789735524165081, 37.94261489385753094 ) ) ;
#16211=ADVANCED_FACE ( 'NONE', ( #23724 ), #10587, .F. ) ;
#16216=VECTOR ( 'NONE', #23625, 999.9999999999998863 ) ;
#16217=( BOUNDED_SURFACE ( )  B_SPLINE_SURFACE ( 3, 1, ( 
 ( #20784, #18632 ),
 ( #9864, #7717 ),
 ( #27405, #14298 ),
 ( #16471, #25261 ) ),
 .UNSPECIFIED., .F., .F., .F. ) 
 B_SPLINE_SURFACE_WITH_KNOTS ( ( 4, 4 ),
 ( 2, 2 ),
 ( 0.000000000000000000, 1.000000000000000000 ),
 ( 0.000000000000000000, 1.000000000000000000 ),
 .UNSPECIFIED. ) 
 GEOMETRIC_REPRESENTATION_ITEM ( )  RATIONAL_B_SPLINE_SURFACE ( (
 ( 1.000000000000000000, 1.000000000000000000),
 ( 0.9934239774497837239, 0.8357310067453919133),
 ( 0.9934239774497837239, 0.8357310067453919133),
 ( 1.000000000000000000, 1.000000000000000000) ) ) 
 REPRESENTATION_ITEM ( '' )  SURFACE ( )  );
#16220=B_SPLINE_CURVE_WITH_KNOTS ( 'NONE', 3,
 ( #7079, #26346, #17703, #15251, #2737, #9078, #15838, #288, #24491, #24342 ),
 .UNSPECIFIED., .F., .F.,
 ( 4, 3, 3, 4 ),
 ( 0.001530725384384964971, 0.001531419946797918505, 0.002296279302920153399, 0.003061450627205758099 ),
 .UNSPECIFIED. ) ;
#16231=DIRECTION ( 'NONE',  ( 1.000000000000000000, -6.938893903907226837E-18, 1.734723475976806709E-18 ) ) ;
#16235=CARTESIAN_POINT ( 'NONE',  ( -28.41354790283022069, 21.64275480268759821, 8.345538364876851745 ) ) ;
#16239=CARTESIAN_POINT ( 'NONE',  ( -20.20700224038492721, -29.58392382092674211, -0.9908225410477480288 ) ) ;
#16252=CARTESIAN_POINT ( 'NONE',  ( -1.155001620486248992, 12.20337535396741124, 44.25209926692296136 ) ) ;
#16254=B_SPLINE_CURVE_WITH_KNOTS ( 'NONE', 3,
 ( #4505, #19623, #19490, #19762, #17320, #26526 ),
 .UNSPECIFIED., .F., .F.,
 ( 4, 2, 4 ),
 ( 0.000000000000000000, 0.0004335151646191504364, 0.0008670303292383008727 ),
 .UNSPECIFIED. ) ;
#16260=CARTESIAN_POINT ( 'NONE',  ( -20.20700224038492010, 27.82980252387833886, 10.08426345511560207 ) ) ;
#16262=FACE_OUTER_BOUND ( 'NONE', #9165, .T. ) ;
#16266=ORIENTED_EDGE ( 'NONE', *, *, #7985, .T. ) ;
#16267=CARTESIAN_POINT ( 'NONE',  ( -1.239374126674604337, 28.97829083655491544, 35.79060836339782270 ) ) ;
#16277=CARTESIAN_POINT ( 'NONE',  ( -1.619063947482201282, 16.67502769180561728, -43.26576862488438735 ) ) ;
#16280=CARTESIAN_POINT ( 'NONE',  ( -15.02187109954785704, -33.49412687891593521, -32.04062513125103351 ) ) ;
#16287=EDGE_CURVE ( 'NONE', #23109, #22524, #23858, .T. ) ;
#16294=B_SPLINE_CURVE_WITH_KNOTS ( 'NONE', 3,
 ( #6325, #13072, #2398, #21857, #21715, #4564, #12780, #17664 ),
 .UNSPECIFIED., .F., .F.,
 ( 4, 2, 2, 4 ),
 ( 0.000000000000000000, 0.002761524886576660186, 0.005523049773153320373, 0.01104609954630662340 ),
 .UNSPECIFIED. ) ;
#16301=( BOUNDED_SURFACE ( )  B_SPLINE_SURFACE ( 3, 1, ( 
 ( #26686, #17769 ),
 ( #22093, #22537 ),
 ( #24266, #20069 ),
 ( #22248, #13732 ) ),
 .UNSPECIFIED., .F., .F., .F. ) 
 B_SPLINE_SURFACE_WITH_KNOTS ( ( 4, 4 ),
 ( 2, 2 ),
 ( 0.000000000000000000, 1.000000000000000000 ),
 ( 0.000000000000000000, 1.000000000000000000 ),
 .UNSPECIFIED. ) 
 GEOMETRIC_REPRESENTATION_ITEM ( )  RATIONAL_B_SPLINE_SURFACE ( (
 ( 1.000000000000000000, 1.000000000000000000),
 ( 0.9934239774497838349, 0.8357310067453913582),
 ( 0.9934239774497838349, 0.8357310067453913582),
 ( 1.000000000000000000, 1.000000000000000000) ) ) 
 REPRESENTATION_ITEM ( '' )  SURFACE ( )  );
#16313=DIRECTION ( 'NONE',  ( 1.000000000000000000, -6.938893903907226837E-18, 1.734723475976806709E-18 ) ) ;
#16315=ORIENTED_EDGE ( 'NONE', *, *, #16120, .F. ) ;
#16317=ORIENTED_EDGE ( 'NONE', *, *, #11370, .T. ) ;
#16319=EDGE_CURVE ( 'NONE', #7007, #14740, #15420, .T. ) ;
#16320=EDGE_CURVE ( 'NONE', #5123, #25702, #6310, .T. ) ;
#16325=CARTESIAN_POINT ( 'NONE',  ( -4.473127245936434626, 37.94261489385718988, -31.51789735524207003 ) ) ;
#16326=CARTESIAN_POINT ( 'NONE',  ( -1.323439229708141651, -2.317790194800056547, -46.01398008004440499 ) ) ;
#16331=CARTESIAN_POINT ( 'NONE',  ( -1.050231094221204087, -14.39477892760331024, -43.47885872350351377 ) ) ;
#16337=CARTESIAN_POINT ( 'NONE',  ( -7.711401346138392121, -21.83927363365067364, -47.70038152767084227 ) ) ;
#16344=CARTESIAN_POINT ( 'NONE',  ( -55.24271866751342941, -0.008488649505342596782, -0.004256484107795601053 ) ) ;
#16351=DIRECTION ( 'NONE',  ( 0.000000000000000000, 5.223019709707975211E-21, -1.000000000000000000 ) ) ;
#16352=APPLICATION_CONTEXT ( 'automotive_design' ) ;
#16354=CARTESIAN_POINT ( 'NONE',  ( -20.57838717382308147, -27.96569011373093971, -10.78122205916989529 ) ) ;
#16357=CARTESIAN_POINT ( 'NONE',  ( -20.24419206586952313, 7.929973069813410547, -28.55732805495818383 ) ) ;
#16359=ORIENTED_EDGE ( 'NONE', *, *, #9716, .T. ) ;
#16361=CARTESIAN_POINT ( 'NONE',  ( -1.583189561560256253, 38.94740041318330981, 25.21827308671188916 ) ) ;
#16363=CARTESIAN_POINT ( 'NONE',  ( -20.37983603106074426, 29.73529213200291821, 1.508851015062683487 ) ) ;
#16370=ORIENTED_EDGE ( 'NONE', *, *, #17892, .F. ) ;
#16371=ORIENTED_EDGE ( 'NONE', *, *, #21749, .F. ) ;
#16373=CARTESIAN_POINT ( 'NONE',  ( -20.90916690077964546, -17.17795951644681907, -35.64494649500676360 ) ) ;
#16377=CARTESIAN_POINT ( 'NONE',  ( -22.23342874802668234, 29.33662284748876914, 11.82490389046284029 ) ) ;
#16381=EDGE_CURVE ( 'NONE', #14740, #26927, #19704, .T. ) ;
#16384=CARTESIAN_POINT ( 'NONE',  ( -7.733045908741323693, -35.49239760110648945, 38.67583825854190138 ) ) ;
#16387=EDGE_CURVE ( 'NONE', #607, #19834, #1164, .T. ) ;
#16403=CARTESIAN_POINT ( 'NONE',  ( -10.86508079875812705, -45.04061326950857591, 24.22249093393325836 ) ) ;
#16412=CARTESIAN_POINT ( 'NONE',  ( -55.24271866751342941, -0.009369360294294061531, 0.001545935011626861600 ) ) ;
#16414=VERTEX_POINT ( 'NONE', #6816 ) ;
#16415=EDGE_CURVE ( 'NONE', #11326, #19279, #15711, .T. ) ;
#16417=CARTESIAN_POINT ( 'NONE',  ( -55.25719721206881729, -0.01079965405819445674, 0.002847566758684036761 ) ) ;
#16421=CARTESIAN_POINT ( 'NONE',  ( -1.048994561756786625, 13.42228657661184954, 43.78680886990926524 ) ) ;
#16440=CARTESIAN_POINT ( 'NONE',  ( -55.24390624410018802, 0.01032895241566708991, 0.001451500391952845713 ) ) ;
#16446=CARTESIAN_POINT ( 'NONE',  ( -20.21097721712959583, 24.14932359587290023, -17.13687106192352161 ) ) ;
#16447=CARTESIAN_POINT ( 'NONE',  ( -1.045287976400365970, 45.76855895860943235, -1.530335034934267258 ) ) ;
#16449=CARTESIAN_POINT ( 'NONE',  ( -20.20612092514784308, -27.77903665678158873, 10.22177639105890279 ) ) ;
#16456=CARTESIAN_POINT ( 'NONE',  ( -1.044556982611274831, 36.05793013899099719, -28.22896456560681600 ) ) ;
#16460=CARTESIAN_POINT ( 'NONE',  ( -55.24300891470648622, -0.002702093572889207890, -0.009439835024157681651 ) ) ;
#16471=CARTESIAN_POINT ( 'NONE',  ( -55.24271866751342941, -0.006671293903668846365, 0.006757859501006202411 ) ) ;
#16474=CARTESIAN_POINT ( 'NONE',  ( -1.113427685306993320, 25.34053733836532274, -38.22586258295203265 ) ) ;
#16485=EDGE_CURVE ( 'NONE', #22401, #15242, #3913, .T. ) ;
#16489=CARTESIAN_POINT ( 'NONE',  ( -4.780792508754313275, -25.98388465890110410, -42.16805077400949386 ) ) ;
#16493=FACE_OUTER_BOUND ( 'NONE', #16512, .T. ) ;
#16497=CIRCLE ( 'NONE', #9138, 34.60786435723138510 ) ;
#16512=EDGE_LOOP ( 'NONE', ( #28324, #26425, #24346, #25255 ) ) ;
#16514=CARTESIAN_POINT ( 'NONE',  ( -1.049817751779889008, -14.63752841325019105, 43.39729912094394848 ) ) ;
#16517=ORIENTED_EDGE ( 'NONE', *, *, #1389, .T. ) ;
#16518=ORIENTED_EDGE ( 'NONE', *, *, #3934, .F. ) ;
#16529=ORIENTED_EDGE ( 'NONE', *, *, #12316, .T. ) ;
#16541=CARTESIAN_POINT ( 'NONE',  ( -1.058473599757816963, 25.48501014712399737, -38.06357893967437889 ) ) ;
#16556=CARTESIAN_POINT ( 'NONE',  ( -1.046935749539996685, -43.14401153755477480, -15.35946454248379034 ) ) ;
#16560=AXIS2_PLACEMENT_3D ( 'NONE', #19504, #17333, #6413 ) ;
#16562=CARTESIAN_POINT ( 'NONE',  ( -8.786685647604898008, 38.68584556812353981, 37.00619870957891777 ) ) ;
#16563=CARTESIAN_POINT ( 'NONE',  ( -1.619063947482197729, 46.30105812165548684, -2.489035965910316506 ) ) ;
#16564=CARTESIAN_POINT ( 'NONE',  ( -25.21435515916043002, 30.48034229288640162, -16.39063784838753790 ) ) ;
#16567=CARTESIAN_POINT ( 'NONE',  ( -8.786685647604887350, -38.68584556812326980, -37.00619870957918778 ) ) ;
#16569=B_SPLINE_CURVE_WITH_KNOTS ( 'NONE', 3,
 ( #12865, #13294, #1930, #23982, #4668, #6275, #15026, #28402, #6551, #26537 ),
 .UNSPECIFIED., .F., .F.,
 ( 4, 2, 2, 2, 4 ),
 ( 2.913600445039318278E-16, 0.0003346187017559116412, 0.0006692374035115318488, 0.001003856105267152219, 0.001338474807022772481 ),
 .UNSPECIFIED. ) ;
#16572=VERTEX_POINT ( 'NONE', #24440 ) ;
#16576=ORIENTED_EDGE ( 'NONE', *, *, #10741, .T. ) ;
#16579=CIRCLE ( 'NONE', #10591, 34.60786435723138510 ) ;
#16580=AXIS2_PLACEMENT_3D ( 'NONE', #2114, #8614, #1838 ) ;
#16583=AXIS2_PLACEMENT_3D ( 'NONE', #17377, #28447, #28314 ) ;
#16588=CARTESIAN_POINT ( 'NONE',  ( -25.21435515916043713, -34.05351380035337883, -6.169479169075319014 ) ) ;
#16590=LINE ( 'NONE', #9681, #17552 ) ;
#16592=CARTESIAN_POINT ( 'NONE',  ( -8.786685647604890903, 25.35688121747502066, -47.14957014837363403 ) ) ;
#16599=AXIS2_PLACEMENT_3D ( 'NONE', #15983, #13536, #22335 ) ;
#16607=VECTOR ( 'NONE', #6322, 1000.000000000000000 ) ;
#16623=CARTESIAN_POINT ( 'NONE',  ( -8.786685647604890903, -48.22796981442785835, -23.24040270374372952 ) ) ;
#16624=CARTESIAN_POINT ( 'NONE',  ( -1.259972190295307604, -2.243354636026084759, -45.95417440459613800 ) ) ;
#16626=CARTESIAN_POINT ( 'NONE',  ( -1.048172774974290622, -15.11899685083854727, -43.23017713506519755 ) ) ;
#16628=ORIENTED_EDGE ( 'NONE', *, *, #19568, .F. ) ;
#16629=EDGE_LOOP ( 'NONE', ( #12102, #25068, #5564, #4632 ) ) ;
#16632=CARTESIAN_POINT ( 'NONE',  ( -1.539763995773685945, 25.17088606276602647, 38.84665165401036546 ) ) ;
#16633=CARTESIAN_POINT ( 'NONE',  ( -20.20612091757416451, -8.058516044219402374, -28.48192249925589792 ) ) ;
#16637=CARTESIAN_POINT ( 'NONE',  ( -6.588769196390752647, -26.02756986588571309, -44.25609997968896892 ) ) ;
#16644=ORIENTED_EDGE ( 'NONE', *, *, #19326, .F. ) ;
#16646=VERTEX_POINT ( 'NONE', #6248 ) ;
#16647=EDGE_CURVE ( 'NONE', #10945, #26104, #12423, .T. ) ;
#16648=( BOUNDED_SURFACE ( )  B_SPLINE_SURFACE ( 3, 1, ( 
 ( #24570, #11584 ),
 ( #7422, #13304 ),
 ( #2961, #7147 ),
 ( #647, #7001 ) ),
 .UNSPECIFIED., .F., .F., .F. ) 
 B_SPLINE_SURFACE_WITH_KNOTS ( ( 4, 4 ),
 ( 2, 2 ),
 ( 0.000000000000000000, 1.000000000000000000 ),
 ( 0.000000000000000000, 1.000000000000000000 ),
 .UNSPECIFIED. ) 
 GEOMETRIC_REPRESENTATION_ITEM ( )  RATIONAL_B_SPLINE_SURFACE ( (
 ( 1.000000000000000000, 1.000000000000000000),
 ( 0.9934239774497837239, 0.8357310067453919133),
 ( 0.9934239774497837239, 0.8357310067453919133),
 ( 1.000000000000000000, 1.000000000000000000) ) ) 
 REPRESENTATION_ITEM ( '' )  SURFACE ( )  );
#16652=ADVANCED_FACE ( 'NONE', ( #14724 ), #15360, .F. ) ;
#16659=DIRECTION ( 'NONE',  ( 0.000000000000000000, 5.223019709707975211E-21, -1.000000000000000000 ) ) ;
#16662=ORIENTED_EDGE ( 'NONE', *, *, #24916, .T. ) ;
#16665=CARTESIAN_POINT ( 'NONE',  ( -1.583189561560255143, 38.94740041318295454, -25.21827308671246470 ) ) ;
#16669=VECTOR ( 'NONE', #17669, 1000.000000000000114 ) ;
#16676=CARTESIAN_POINT ( 'NONE',  ( -1.049819825607597235, -43.39756533277870432, 14.63675055554426407 ) ) ;
#16688=CARTESIAN_POINT ( 'NONE',  ( -55.25719721206881729, 0.0006290797159209853082, -0.01115102788683027674 ) ) ;
#16695=AXIS2_PLACEMENT_3D ( 'NONE', #14531, #1435, #10243 ) ;
#16697=CARTESIAN_POINT ( 'NONE',  ( -1.050231094221226291, 36.90262059116464854, -27.12595454131517769 ) ) ;
#16704=CARTESIAN_POINT ( 'NONE',  ( -2.265401668238152588, 45.46007138824041505, -11.98901689611057009 ) ) ;
#16705=CARTESIAN_POINT ( 'NONE',  ( -23.79248802219730052, -13.25839849636379597, -30.42578156345381046 ) ) ;
#16709=CARTESIAN_POINT ( 'NONE',  ( -8.786685647604890903, -48.22796981442753150, 23.24040270374441874 ) ) ;
#16710=LINE ( 'NONE', #19005, #8572 ) ;
#16716=FACE_OUTER_BOUND ( 'NONE', #14310, .T. ) ;
#16719=CARTESIAN_POINT ( 'NONE',  ( -1.050231094221194983, -45.79908322896422135, 0.2545420581353859402 ) ) ;
#16723=AXIS2_PLACEMENT_3D ( 'NONE', #13664, #7501, #11808 ) ;
#16730=B_SPLINE_CURVE_WITH_KNOTS ( 'NONE', 3,
 ( #10707, #10560, #26094, #19475, #6383, #12993 ),
 .UNSPECIFIED., .F., .F.,
 ( 4, 2, 4 ),
 ( 3.178475462313071774E-16, 0.003576372551511121031, 0.007152745103021923741 ),
 .UNSPECIFIED. ) ;
#16731=B_SPLINE_CURVE_WITH_KNOTS ( 'NONE', 3,
 ( #19176, #18748, #1472, #14427, #25676, #27524 ),
 .UNSPECIFIED., .F., .F.,
 ( 4, 2, 4 ),
 ( 4.906538933386797396E-18, 0.0004335184443140297200, 0.0008670368886280544526 ),
 .UNSPECIFIED. ) ;
#16739=CARTESIAN_POINT ( 'NONE',  ( -55.24728320129491266, 0.01214321324517175435, -0.008013189884952098135 ) ) ;
#16742=CARTESIAN_POINT ( 'NONE',  ( -20.24399999263415140, -1.282322917263260198, 29.60996018918694617 ) ) ;
#16743=CARTESIAN_POINT ( 'NONE',  ( -1.045287976400365970, 1.530335034934747318, 45.76855895860941814 ) ) ;
#16746=( BOUNDED_SURFACE ( )  B_SPLINE_SURFACE ( 3, 1, ( 
 ( #8554, #26109 ),
 ( #17456, #13284 ),
 ( #26245, #331 ),
 ( #9121, #2194 ) ),
 .UNSPECIFIED., .F., .F., .F. ) 
 B_SPLINE_SURFACE_WITH_KNOTS ( ( 4, 4 ),
 ( 2, 2 ),
 ( 0.000000000000000000, 1.000000000000000000 ),
 ( 0.000000000000000000, 1.000000000000000000 ),
 .UNSPECIFIED. ) 
 GEOMETRIC_REPRESENTATION_ITEM ( )  RATIONAL_B_SPLINE_SURFACE ( (
 ( 1.000000000000000000, 1.000000000000000000),
 ( 0.7789835883360578528, 0.9689951854195403280),
 ( 0.7789835883360578528, 0.9689951854195403280),
 ( 1.000000000000000000, 1.000000000000000000) ) ) 
 REPRESENTATION_ITEM ( '' )  SURFACE ( )  );
#16753=CARTESIAN_POINT ( 'NONE',  ( -55.24198130335446422, 0.008310594958153458625, -0.004163123460802744397 ) ) ;
#16768=ORIENTED_EDGE ( 'NONE', *, *, #4511, .F. ) ;
#16771=CARTESIAN_POINT ( 'NONE',  ( -23.79248802219722592, -32.40806545715335574, -7.157555990716774730 ) ) ;
#16772=CARTESIAN_POINT ( 'NONE',  ( -20.24419206586952313, 1.282847120831654530, 29.61012937815439017 ) ) ;
#16775=CARTESIAN_POINT ( 'NONE',  ( -1.045287976400365970, 1.530335034934747318, 45.76855895860941814 ) ) ;
#16780=ADVANCED_FACE ( 'NONE', ( #750 ), #21271, .F. ) ;
#16792=ADVANCED_FACE ( 'NONE', ( #9252 ), #22364, .F. ) ;
#16805=CARTESIAN_POINT ( 'NONE',  ( -25.21435515916025594, 1.749597353048488237E-16, -4.373993382621220594E-17 ) ) ;
#16810=CARTESIAN_POINT ( 'NONE',  ( -20.24399999263414784, 29.60996018918694617, 1.282322917263571282 ) ) ;
#16823=CARTESIAN_POINT ( 'NONE',  ( -20.20612092514784308, -8.058517256680906016, 28.48192215759674184 ) ) ;
#16825=ORIENTED_EDGE ( 'NONE', *, *, #676, .F. ) ;
#16827=CARTESIAN_POINT ( 'NONE',  ( -1.539763995773674177, 38.84665165401067810, -25.17088606276561080 ) ) ;
#16829=ORIENTED_EDGE ( 'NONE', *, *, #24422, .T. ) ;
#16830=CARTESIAN_POINT ( 'NONE',  ( -15.02187109954783217, 40.82269973458240031, -21.95370994985588098 ) ) ;
#16835=CARTESIAN_POINT ( 'NONE',  ( -20.20700224038492721, 24.51628800869048419, -16.58740185276719359 ) ) ;
#16836=CARTESIAN_POINT ( 'NONE',  ( -2.904412668506670681, 40.16685646686207889, -25.64203923793588302 ) ) ;
#16850=CARTESIAN_POINT ( 'NONE',  ( -28.41354790283022069, -22.41474081378005323, -5.969609727607934957 ) ) ;
#16852=ORIENTED_EDGE ( 'NONE', *, *, #23364, .F. ) ;
#16856=DIRECTION ( 'NONE',  ( 1.000000000000000000, -6.938893903907226837E-18, 1.734723475976806709E-18 ) ) ;
#16862=CARTESIAN_POINT ( 'NONE',  ( -55.24728320129491266, -0.0006547948648744401781, 0.01453410071985650025 ) ) ;
#16863=ORIENTED_EDGE ( 'NONE', *, *, #12230, .T. ) ;
#16882=ORIENTED_EDGE ( 'NONE', *, *, #15897, .T. ) ;
#16886=CARTESIAN_POINT ( 'NONE',  ( -1.048172774974290178, -1.020161070261438097, -45.78636862970792265 ) ) ;
#16891=CARTESIAN_POINT ( 'NONE',  ( -21.41427618760457818, -16.60878262545437778, -25.94789270595500597 ) ) ;
#16892=CARTESIAN_POINT ( 'NONE',  ( -7.078251931573406708, 47.71415099571806451, -20.86696228105241602 ) ) ;
#16893=ORIENTED_EDGE ( 'NONE', *, *, #11159, .T. ) ;
#16894=EDGE_LOOP ( 'NONE', ( #16371, #3993, #27573, #9130 ) ) ;
#16895=CARTESIAN_POINT ( 'NONE',  ( -8.259864102781673267, -52.60025989855198247, 6.590267880897466846 ) ) ;
#16897=ORIENTED_EDGE ( 'NONE', *, *, #23129, .T. ) ;
#16898=ORIENTED_EDGE ( 'NONE', *, *, #28160, .T. ) ;
#16904=LINE ( 'NONE', #21789, #25863 ) ;
#16908=CARTESIAN_POINT ( 'NONE',  ( -1.464342487929844783, -44.64187261869788870, -11.94843286121900228 ) ) ;
#16912=ORIENTED_EDGE ( 'NONE', *, *, #1840, .F. ) ;
#16913=CARTESIAN_POINT ( 'NONE',  ( -1.049819825607597235, -26.50610175068240792, 37.34982882986871999 ) ) ;
#16915=CARTESIAN_POINT ( 'NONE',  ( -8.786685647604890903, -37.00619870957905277, 38.68584556812340480 ) ) ;
#16917=CARTESIAN_POINT ( 'NONE',  ( -20.21097721712959938, 9.464413111084745367, -28.05863618200111986 ) ) ;
#16919=ORIENTED_EDGE ( 'NONE', *, *, #23129, .F. ) ;
#16922=CARTESIAN_POINT ( 'NONE',  ( -1.583189561560255143, 29.24830400313165413, -36.01941156322797610 ) ) ;
#16926=ORIENTED_EDGE ( 'NONE', *, *, #21752, .T. ) ;
#16929=EDGE_CURVE ( 'NONE', #20088, #20677, #17602, .T. ) ;
#16937=CARTESIAN_POINT ( 'NONE',  ( -20.57838717382308147, 7.715628353034087894, 28.96176188950209962 ) ) ;
#16939=CARTESIAN_POINT ( 'NONE',  ( -1.046935749540010674, 43.93230528057182482, -12.93334586714193790 ) ) ;
#16940=CARTESIAN_POINT ( 'NONE',  ( -1.155001620486255209, 28.62773628245669499, -35.88346938217563320 ) ) ;
#16944=CARTESIAN_POINT ( 'NONE',  ( -7.733045908741326357, -51.44704017882769875, 10.42750254442592706 ) ) ;
#16945=DIRECTION ( 'NONE',  ( 1.000000000000000000, -6.938893903907226837E-18, 1.734723475976806709E-18 ) ) ;
#16955=CARTESIAN_POINT ( 'NONE',  ( -1.583189561560252701, -36.01941156322808268, -29.24830400313153334 ) ) ;
#16959=CARTESIAN_POINT ( 'NONE',  ( -8.786685647604890903, -52.67761315067293282, -9.545808661480407409 ) ) ;
#16963=EDGE_CURVE ( 'NONE', #9224, #12584, #23454, .T. ) ;
#16977=ORIENTED_EDGE ( 'NONE', *, *, #10124, .F. ) ;
#16981=CARTESIAN_POINT ( 'NONE',  ( -28.13707043255157103, 6.342158660427001493, -22.00298671236742010 ) ) ;
#16986=ORIENTED_EDGE ( 'NONE', *, *, #10006, .T. ) ;
#16996=ORIENTED_EDGE ( 'NONE', *, *, #12959, .T. ) ;
#16997=ADVANCED_FACE ( 'NONE', ( #2145 ), #5822, .F. ) ;
#17000=ADVANCED_FACE ( 'NONE', ( #17144 ), #1600, .F. ) ;
#17003=CARTESIAN_POINT ( 'NONE',  ( -1.044557008772714513, -12.57891310333380552, -44.03203053429566438 ) ) ;
#17008=CARTESIAN_POINT ( 'NONE',  ( -25.21435515916043713, 34.05351380035342146, 6.169479169075106739 ) ) ;
#17013=CARTESIAN_POINT ( 'NONE',  ( -55.24271866751342941, 0.004256484107793635611, 0.008488649505346116536 ) ) ;
#17017=CARTESIAN_POINT ( 'NONE',  ( -1.113427685306987991, 38.22586258295232398, 25.34053733836490707 ) ) ;
#17018=CONICAL_SURFACE ( 'NONE', #9213, 34.60786435723138510, 0.8559913436420825139 ) ;
#17019=CARTESIAN_POINT ( 'NONE',  ( -23.79223135445719350, -30.42557260166821109, -13.25822371132282917 ) ) ;
#17021=VECTOR ( 'NONE', #15781, 999.9999999999998863 ) ;
#17025=EDGE_CURVE ( 'NONE', #3564, #21873, #24867, .T. ) ;
#17027=CARTESIAN_POINT ( 'NONE',  ( -55.24300891470650754, 0.002702093572893664395, -0.009439835024159005245 ) ) ;
#17029=CARTESIAN_POINT ( 'NONE',  ( -1.619063947482197729, 2.489035965910159298, -46.30105812165548684 ) ) ;
#17041=CARTESIAN_POINT ( 'NONE',  ( -25.21435515916043713, -23.92354251275918031, 25.00736669481048224 ) ) ;
#17046=VERTEX_POINT ( 'NONE', #21751 ) ;
#17052=DIRECTION ( 'NONE',  ( -1.000000000000000000, 6.938893903907226837E-18, -1.734723475976806709E-18 ) ) ;
#17087=CARTESIAN_POINT ( 'NONE',  ( -55.24271866751342941, 0.001545935011631000867, -0.009369360294295843092 ) ) ;
#17089=EDGE_CURVE ( 'NONE', #27834, #4666, #20286, .T. ) ;
#17094=CARTESIAN_POINT ( 'NONE',  ( -55.24340739397742084, -0.0007387096945734077319, 0.01010924026184317238 ) ) ;
#17095=EDGE_CURVE ( 'NONE', #19279, #18758, #9005, .T. ) ;
#17096=ADVANCED_FACE ( 'NONE', ( #16262 ), #4521, .F. ) ;
#17100=CARTESIAN_POINT ( 'NONE',  ( -1.619063947482197729, -35.99532424477401094, -29.22875152547743838 ) ) ;
#17103=AXIS2_PLACEMENT_3D ( 'NONE', #17933, #2990, #11770 ) ;
#17108=CARTESIAN_POINT ( 'NONE',  ( -22.23226125620943705, -11.82389163795231468, -29.33577758406444858 ) ) ;
#17131=LINE ( 'NONE', #27646, #17163 ) ;
#17141=ORIENTED_EDGE ( 'NONE', *, *, #287, .F. ) ;
#17144=FACE_OUTER_BOUND ( 'NONE', #150, .T. ) ;
#17145=CONICAL_SURFACE ( 'NONE', #11164, 53.53553390275978785, 0.7853981625000051592 ) ;
#17155=CARTESIAN_POINT ( 'NONE',  ( -1.049819078601898825, -0.5100232645223283789, -45.79653735114490587 ) ) ;
#17157=FACE_OUTER_BOUND ( 'NONE', #6872, .T. ) ;
#17163=VECTOR ( 'NONE', #23784, 999.9999999999998863 ) ;
#17165=CARTESIAN_POINT ( 'NONE',  ( -1.619063947482197729, 38.92136151114943488, 25.20140673341330739 ) ) ;
#17171=CIRCLE ( 'NONE', #16723, 37.50000000000001421 ) ;
#17173=FACE_OUTER_BOUND ( 'NONE', #62, .T. ) ;
#17176=CARTESIAN_POINT ( 'NONE',  ( -1.619063947482197729, -46.30105812165550105, -2.489035965909997206 ) ) ;
#17187=CARTESIAN_POINT ( 'NONE',  ( -12.94347594948487057, -47.96504705787739198, 8.691477019903814494 ) ) ;
#17192=MANIFOLD_SOLID_BREP ( 'Boss-Extrude1', #11412 ) ;
#17193=CARTESIAN_POINT ( 'NONE',  ( -8.786685647604890903, -25.35688121747466184, 47.14957014837381166 ) ) ;
#17195=CARTESIAN_POINT ( 'NONE',  ( -1.050230346682690108, -37.05182464822001975, -26.92058491724852942 ) ) ;
#17198=ADVANCED_FACE ( 'NONE', ( #20868 ), #19324, .T. ) ;
#17199=CARTESIAN_POINT ( 'NONE',  ( -2.265401668238153032, -11.98901689611074062, -45.46007138824035820 ) ) ;
#17203=VERTEX_POINT ( 'NONE', #26166 ) ;
#17205=ADVANCED_FACE ( 'NONE', ( #10783 ), #7496, .F. ) ;
#17208=CARTESIAN_POINT ( 'NONE',  ( -1.019300379054419947, 45.76814864815091255, 2.023851374322834573 ) ) ;
#17209=CARTESIAN_POINT ( 'NONE',  ( -55.24728320129491266, 0.01402509393918583563, -0.003868537197317189515 ) ) ;
#17211=ORIENTED_EDGE ( 'NONE', *, *, #3188, .T. ) ;
#17213=DIRECTION ( 'NONE',  ( 0.7563875759206387661, 0.6320336713238499105, -0.1685564395263362270 ) ) ;
#17215=DIRECTION ( 'NONE',  ( 0.000000000000000000, 5.223019709707975211E-21, -1.000000000000000000 ) ) ;
#17217=ORIENTED_EDGE ( 'NONE', *, *, #14999, .T. ) ;
#17223=DIRECTION ( 'NONE',  ( 0.000000000000000000, 5.223019709707975211E-21, -1.000000000000000000 ) ) ;
#17227=VERTEX_POINT ( 'NONE', #14937 ) ;
#17234=CARTESIAN_POINT ( 'NONE',  ( 14.74894986621300319, 4.541450660883840889E-15, -37.50000000000001421 ) ) ;
#17240=CARTESIAN_POINT ( 'NONE',  ( -20.57838717382308502, 23.26537097894105699, -18.89542499756508320 ) ) ;
#17248=CARTESIAN_POINT ( 'NONE',  ( -7.078251931573400491, -11.16394717458712726, -50.86685171665407523 ) ) ;
#17269=CARTESIAN_POINT ( 'NONE',  ( -6.574463467970653952, -11.01561683920017387, 50.12924290857549181 ) ) ;
#17271=ORIENTED_EDGE ( 'NONE', *, *, #10124, .T. ) ;
#17275=ADVANCED_FACE ( 'NONE', ( #24029 ), #26237, .T. ) ;
#17277=CARTESIAN_POINT ( 'NONE',  ( -8.786685647604890903, 37.00619870957935120, -38.68584556812312059 ) ) ;
#17283=CARTESIAN_POINT ( 'NONE',  ( -55.24340739397742794, -0.008612749836242414997, -0.005344433640974251970 ) ) ;
#17287=EDGE_CURVE ( 'NONE', #12283, #17615, #4005, .T. ) ;
#17290=CARTESIAN_POINT ( 'NONE',  ( -1.239374126674604337, 35.79060836339854745, 28.97829083655398819 ) ) ;
#17297=CARTESIAN_POINT ( 'NONE',  ( -1.049817751779888786, 45.79652915392415480, 0.5106138415328438374 ) ) ;
#17300=ORIENTED_EDGE ( 'NONE', *, *, #12133, .T. ) ;
#17306=CARTESIAN_POINT ( 'NONE',  ( -20.20700224038492721, 29.58392382092673500, 0.9908225410479544193 ) ) ;
#17319=CARTESIAN_POINT ( 'NONE',  ( -1.056502255334264895, -45.80535052436396626, 0.5104472526224692608 ) ) ;
#17320=CARTESIAN_POINT ( 'NONE',  ( -20.20612091757421069, 10.22177757278315191, -27.77903622052259536 ) ) ;
#17324=CARTESIAN_POINT ( 'NONE',  ( -8.786685647604896232, -7.199674155858612146, 53.04920435127190359 ) ) ;
#17326=CARTESIAN_POINT ( 'NONE',  ( -1.045287976400379737, -25.66401692420040703, -37.92705037016734337 ) ) ;
#17329=CARTESIAN_POINT ( 'NONE',  ( -55.24198130335446422, -0.001391250620104931938, 0.009190321388308853381 ) ) ;
#17332=B_SPLINE_CURVE_WITH_KNOTS ( 'NONE', 3,
 ( #2749, #20158, #11248, #13680 ),
 .UNSPECIFIED., .F., .F.,
 ( 4, 4 ),
 ( 1.909141801897607538E-16, 0.001982023823822941146 ),
 .UNSPECIFIED. ) ;
#17333=DIRECTION ( 'NONE',  ( 1.000000000000000000, -6.938893903907226837E-18, 1.734723475976806709E-18 ) ) ;
#17334=( BOUNDED_SURFACE ( )  B_SPLINE_SURFACE ( 3, 1, ( 
 ( #28357, #12687 ),
 ( #6650, #8655 ),
 ( #15400, #13241 ),
 ( #19870, #160 ) ),
 .UNSPECIFIED., .F., .F., .F. ) 
 B_SPLINE_SURFACE_WITH_KNOTS ( ( 4, 4 ),
 ( 2, 2 ),
 ( 0.000000000000000000, 1.000000000000000000 ),
 ( 0.000000000000000000, 1.000000000000000000 ),
 .UNSPECIFIED. ) 
 GEOMETRIC_REPRESENTATION_ITEM ( )  RATIONAL_B_SPLINE_SURFACE ( (
 ( 1.000000000000000000, 1.000000000000000000),
 ( 0.9934239774497838349, 0.8357310067453913582),
 ( 0.9934239774497838349, 0.8357310067453913582),
 ( 1.000000000000000000, 1.000000000000000000) ) ) 
 REPRESENTATION_ITEM ( '' )  SURFACE ( )  );
#17338=CARTESIAN_POINT ( 'NONE',  ( -20.57838717382308147, -10.78122205916981358, 27.96569011373096814 ) ) ;
#17341=CARTESIAN_POINT ( 'NONE',  ( -12.82751273423883553, -43.04932478553545394, -23.15139349681293623 ) ) ;
#17342=CARTESIAN_POINT ( 'NONE',  ( -1.046935749540012450, 15.35946454248395376, -43.14401153755472507 ) ) ;
#17346=CARTESIAN_POINT ( 'NONE',  ( -23.79223135445721837, -33.03345552685147624, -3.207301057648224596 ) ) ;
#17353=DIRECTION ( 'NONE',  ( 0.000000000000000000, 5.223019709707975211E-21, -1.000000000000000000 ) ) ;
#17354=CARTESIAN_POINT ( 'NONE',  ( -20.20700224038492721, 10.08426345511588984, -27.82980252387822517 ) ) ;
#17358=CARTESIAN_POINT ( 'NONE',  ( -55.24271866751342941, -0.004365563123935077734, -0.008433070970613952902 ) ) ;
#17374=ORIENTED_EDGE ( 'NONE', *, *, #22607, .F. ) ;
#17377=CARTESIAN_POINT ( 'NONE',  ( -25.21435515916025594, 1.749597353048488237E-16, -4.373993382621220594E-17 ) ) ;
#17381=CARTESIAN_POINT ( 'NONE',  ( -1.619063947482197729, 2.489035965910159298, -46.30105812165548684 ) ) ;
#17388=LINE ( 'NONE', #11339, #18710 ) ;
#17408=EDGE_CURVE ( 'NONE', #27461, #20232, #24875, .T. ) ;
#17412=EDGE_CURVE ( 'NONE', #14332, #15158, #9718, .T. ) ;
#17416=CARTESIAN_POINT ( 'NONE',  ( -4.162674018437141576, 18.33413805792438112, -45.34593312138888876 ) ) ;
#17419=CARTESIAN_POINT ( 'NONE',  ( -7.733045908741337016, 47.75066202881826882, 21.80378472388440514 ) ) ;
#17423=CARTESIAN_POINT ( 'NONE',  ( -1.259972190295302497, -12.06706380853662530, 44.39825172539707410 ) ) ;
#17425=CARTESIAN_POINT ( 'NONE',  ( -1.539760825549681966, -35.94320866319468166, 29.16712717142800670 ) ) ;
#17427=CARTESIAN_POINT ( 'NONE',  ( -20.37983603106074426, -10.62371319148622284, 27.81368274044722000 ) ) ;
#17432=ORIENTED_EDGE ( 'NONE', *, *, #10596, .F. ) ;
#17437=EDGE_LOOP ( 'NONE', ( #15290, #19674, #5491, #23081 ) ) ;
#17444=CARTESIAN_POINT ( 'NONE',  ( -20.57838717382308147, -25.16001208503093522, 16.28767523336148315 ) ) ;
#17453=CARTESIAN_POINT ( 'NONE',  ( -1.583189561560252701, 38.94740041318296164, -25.21827308671245760 ) ) ;
#17456=CARTESIAN_POINT ( 'NONE',  ( -55.25297051322618813, -0.007247191603128547155, 0.01306918787467270006 ) ) ;
#17457=CARTESIAN_POINT ( 'NONE',  ( -1.539763995773687055, -43.19716353142342768, -16.63252574783026816 ) ) ;
#17458=CARTESIAN_POINT ( 'NONE',  ( -1.323439229708149867, 35.86372896917474407, -28.92147054731853828 ) ) ;
#17460=ORIENTED_EDGE ( 'NONE', *, *, #17408, .F. ) ;
#17462=ADVANCED_FACE ( 'NONE', ( #13332 ), #23473, .F. ) ;
#17463=CARTESIAN_POINT ( 'NONE',  ( -20.20700224038492721, -16.58740185276692358, 24.51628800869065827 ) ) ;
#17464=CARTESIAN_POINT ( 'NONE',  ( -1.045287976400383290, -36.12803364096628655, -28.14015102489793918 ) ) ;
#17468=CARTESIAN_POINT ( 'NONE',  ( -1.155031165708871654, -28.62780465193337420, -35.88345263711039479 ) ) ;
#17475=ADVANCED_FACE ( 'NONE', ( #3411 ), #11504, .F. ) ;
#17480=B_SPLINE_CURVE_WITH_KNOTS ( 'NONE', 3,
 ( #2123, #17675, #20116, #4304, #26454, #15083, #19557 ),
 .UNSPECIFIED., .F., .F.,
 ( 4, 3, 4 ),
 ( 0.000000000000000000, 0.006568092053401831769, 0.02506242213020820619 ),
 .UNSPECIFIED. ) ;
#17492=VERTEX_POINT ( 'NONE', #5864 ) ;
#17496=CARTESIAN_POINT ( 'NONE',  ( -1.045287976400365970, 1.530335034933814731, -45.76855895860946788 ) ) ;
#17497=CARTESIAN_POINT ( 'NONE',  ( -21.81686047589427702, 18.24499610240089353, 33.92779429964183890 ) ) ;
#17502=CARTESIAN_POINT ( 'NONE',  ( -55.24390624410018802, 0.001451500391953283731, -0.01032895241566680888 ) ) ;
#17504=CARTESIAN_POINT ( 'NONE',  ( -4.178947244162626973, 31.41809272265978947, 37.51424432987617053 ) ) ;
#17513=DIRECTION ( 'NONE',  ( 1.000000000000000000, -6.938893903907226837E-18, 1.734723475976806709E-18 ) ) ;
#17517=CARTESIAN_POINT ( 'NONE',  ( -25.21435515916043713, -23.92354251275918031, 25.00736669481048224 ) ) ;
#17519=CARTESIAN_POINT ( 'NONE',  ( -1.031422197589711987, 44.01264471863864713, 12.69107518035455762 ) ) ;
#17520=AXIS2_PLACEMENT_3D ( 'NONE', #2288, #26068, #4046 ) ;
#17525=CARTESIAN_POINT ( 'NONE',  ( -25.21435515916043713, 15.02493970636190745, 31.17620025257570759 ) ) ;
#17526=CARTESIAN_POINT ( 'NONE',  ( -4.473127245936431073, -12.17046501147550153, -47.80062405537796622 ) ) ;
#17532=CARTESIAN_POINT ( 'NONE',  ( -23.77929240705206837, -15.74261278740695502, -32.66578242509739027 ) ) ;
#17539=CARTESIAN_POINT ( 'NONE',  ( -1.031422197589716205, -44.01264471863856897, -12.69107518035485782 ) ) ;
#17549=ADVANCED_FACE ( 'NONE', ( #3126 ), #20329, .F. ) ;
#17552=VECTOR ( 'NONE', #758, 999.9999999999998863 ) ;
#17563=CARTESIAN_POINT ( 'NONE',  ( -4.178947244162629637, 25.96944194166794162, -41.47292084251642308 ) ) ;
#17567=CARTESIAN_POINT ( 'NONE',  ( -20.57838717382308147, -25.16001208503093522, 16.28767523336148315 ) ) ;
#17575=VERTEX_POINT ( 'NONE', #12601 ) ;
#17580=VERTEX_POINT ( 'NONE', #13030 ) ;
#17583=AXIS2_PLACEMENT_3D ( 'NONE', #13415, #15715, #11270 ) ;
#17589=CARTESIAN_POINT ( 'NONE',  ( -20.47566338032522637, -18.81547714195493626, -23.19796701701864805 ) ) ;
#17590=CARTESIAN_POINT ( 'NONE',  ( -1.463510566862833207, -25.15876608740840936, -38.76366072687767428 ) ) ;
#17592=CARTESIAN_POINT ( 'NONE',  ( -23.77929240705206126, -6.464423883190137055, 35.68044874544703049 ) ) ;
#17593=CARTESIAN_POINT ( 'NONE',  ( -25.21435515916043002, 34.05351380035335040, -6.169479169075572145 ) ) ;
#17601=EDGE_LOOP ( 'NONE', ( #19893, #22899, #20557, #15198 ) ) ;
#17602=B_SPLINE_CURVE_WITH_KNOTS ( 'NONE', 3,
 ( #1606, #21464, #12680, #19301, #28076, #5804 ),
 .UNSPECIFIED., .F., .F.,
 ( 4, 2, 4 ),
 ( 0.000000000000000000, 0.0004335184443140258710, 0.0008670368886280517421 ),
 .UNSPECIFIED. ) ;
#17605=CARTESIAN_POINT ( 'NONE',  ( -1.045287976400386842, 37.92705037016744285, -25.66401692420027203 ) ) ;
#17611=VECTOR ( 'NONE', #23469, 1000.000000000000000 ) ;
#17613=CARTESIAN_POINT ( 'NONE',  ( -2.911734481061402757, -25.69892591260238746, 40.13920818157105685 ) ) ;
#17615=VERTEX_POINT ( 'NONE', #21952 ) ;
#17617=CARTESIAN_POINT ( 'NONE',  ( -1.259972190295293393, -28.82609802125285015, -35.85909728507041194 ) ) ;
#17619=CARTESIAN_POINT ( 'NONE',  ( -22.34422965417125795, -34.15536449444077505, 16.46028608106144731 ) ) ;
#17629=CARTESIAN_POINT ( 'NONE',  ( -9.156249394959713683, 8.027840202794694235, 53.90509764945120708 ) ) ;
#17630=LINE ( 'NONE', #26414, #22068 ) ;
#17632=CARTESIAN_POINT ( 'NONE',  ( -20.20612092514784308, -16.46550332780508796, 24.59769888281551786 ) ) ;
#17635=EDGE_CURVE ( 'NONE', #19718, #1416, #18194, .T. ) ;
#17638=CARTESIAN_POINT ( 'NONE',  ( -55.24198130335446422, -0.009170435128244797812, -0.001516807524708348827 ) ) ;
#17639=CARTESIAN_POINT ( 'NONE',  ( -1.048994561756789512, -43.78680886990931498, 13.42228657661168789 ) ) ;
#17642=( BOUNDED_SURFACE ( )  B_SPLINE_SURFACE ( 3, 1, ( 
 ( #15869, #13699 ),
 ( #2620, #24236 ),
 ( #22053, #13268 ),
 ( #22503, #4491 ) ),
 .UNSPECIFIED., .F., .F., .F. ) 
 B_SPLINE_SURFACE_WITH_KNOTS ( ( 4, 4 ),
 ( 2, 2 ),
 ( 0.000000000000000000, 1.000000000000000000 ),
 ( 0.000000000000000000, 1.000000000000000000 ),
 .UNSPECIFIED. ) 
 GEOMETRIC_REPRESENTATION_ITEM ( )  RATIONAL_B_SPLINE_SURFACE ( (
 ( 1.000000000000000000, 1.000000000000000000),
 ( 0.9934239774497837239, 0.8357310067453919133),
 ( 0.9934239774497837239, 0.8357310067453919133),
 ( 1.000000000000000000, 1.000000000000000000) ) ) 
 REPRESENTATION_ITEM ( '' )  SURFACE ( )  );
#17647=CARTESIAN_POINT ( 'NONE',  ( -6.574463467970541153, -38.37705091668347279, 34.08059230520071026 ) ) ;
#17651=CARTESIAN_POINT ( 'NONE',  ( -9.156249394959706578, 25.18996226954685369, 48.32878616080981260 ) ) ;
#17654=CARTESIAN_POINT ( 'NONE',  ( -20.20700224038492721, 0.9908225410478516126, -29.58392382092673145 ) ) ;
#17664=CARTESIAN_POINT ( 'NONE',  ( -1.619063947482197729, -2.489035965910479486, -46.30105812165547974 ) ) ;
#17668=CARTESIAN_POINT ( 'NONE',  ( -16.86833981943426153, -20.94590537750580239, 38.94907963570745579 ) ) ;
#17669=DIRECTION ( 'NONE',  ( 0.7637818620346800147, 0.3617919495470829916, 0.5345501402766235088 ) ) ;
#17670=CARTESIAN_POINT ( 'NONE',  ( -10.86508079875782151, 46.07061504567116828, 22.20099862734772245 ) ) ;
#17672=EDGE_CURVE ( 'NONE', #14341, #17203, #26467, .T. ) ;
#17675=CARTESIAN_POINT ( 'NONE',  ( -23.77929240705188008, 35.93174012244194415, -4.877832571065094491 ) ) ;
#17682=CARTESIAN_POINT ( 'NONE',  ( -21.81686047589429833, -6.867757412720954413, -37.90526371014254892 ) ) ;
#17702=EDGE_CURVE ( 'NONE', #3442, #16646, #15591, .T. ) ;
#17703=CARTESIAN_POINT ( 'NONE',  ( -1.050230347360791017, -0.0004630652115286125773, 45.79907861464602092 ) ) ;
#17707=ADVANCED_FACE ( 'NONE', ( #24566 ), #16301, .F. ) ;
#17713=CARTESIAN_POINT ( 'NONE',  ( -6.588769196390754423, -44.25609997968886233, 26.02756986588589072 ) ) ;
#17714=CARTESIAN_POINT ( 'NONE',  ( -20.20700224038492010, -16.58740185276728241, -24.51628800869040958 ) ) ;
#17716=CARTESIAN_POINT ( 'NONE',  ( -24.53237795827005741, 30.86653739599987745, -14.09663893005569513 ) ) ;
#17720=ORIENTED_EDGE ( 'NONE', *, *, #28046, .T. ) ;
#17721=CARTESIAN_POINT ( 'NONE',  ( -22.23226125620944416, 24.24619897613477093, -20.31044300692182603 ) ) ;
#17735=CARTESIAN_POINT ( 'NONE',  ( -1.044557008772712514, -25.56990300677008676, -37.98985164565319650 ) ) ;
#17736=FACE_OUTER_BOUND ( 'NONE', #5417, .T. ) ;
#17737=CARTESIAN_POINT ( 'NONE',  ( -28.13707043255157103, 22.88591869784691113, 0.7675454997507791255 ) ) ;
#17740=CARTESIAN_POINT ( 'NONE',  ( -1.113427685307000203, 12.28784199929934751, -44.18561238466741514 ) ) ;
#17744=ORIENTED_EDGE ( 'NONE', *, *, #6043, .T. ) ;
#17748=DIRECTION ( 'NONE',  ( 1.000000000000000000, -6.938893903907226837E-18, 1.734723475976806709E-18 ) ) ;
#17751=ORIENTED_EDGE ( 'NONE', *, *, #13729, .T. ) ;
#17757=ORIENTED_EDGE ( 'NONE', *, *, #3260, .F. ) ;
#17759=ORIENTED_EDGE ( 'NONE', *, *, #28075, .T. ) ;
#17766=ORIENTED_EDGE ( 'NONE', *, *, #25673, .F. ) ;
#17769=CARTESIAN_POINT ( 'NONE',  ( -1.031422197589711987, -25.67058493451414591, 37.93675465142499803 ) ) ;
#17771=CARTESIAN_POINT ( 'NONE',  ( -9.156249394959713683, -48.32878616081028866, -25.18996226954597972 ) ) ;
#17775=DIRECTION ( 'NONE',  ( 1.000000000000000000, -6.938893903907226837E-18, 1.734723475976806709E-18 ) ) ;
#17791=CARTESIAN_POINT ( 'NONE',  ( -55.25719721206881729, 0.007063345920781645762, 0.008651607285661163521 ) ) ;
#17795=CARTESIAN_POINT ( 'NONE',  ( -20.20997486282892552, 3.551351076220724598E-15, -29.60348406988233450 ) ) ;
#17798=CARTESIAN_POINT ( 'NONE',  ( -12.94347594948481195, 8.691477019903993906, 47.96504705787742040 ) ) ;
#17800=LINE ( 'NONE', #4013, #11578 ) ;
#17802=CARTESIAN_POINT ( 'NONE',  ( -1.031422197589716205, 25.67058493451444079, -37.93675465142481329 ) ) ;
#17803=CARTESIAN_POINT ( 'NONE',  ( -1.056502255334264895, -43.40574022158763512, 14.64009593116146846 ) ) ;
#17804=ORIENTED_EDGE ( 'NONE', *, *, #16320, .F. ) ;
#17805=ORIENTED_EDGE ( 'NONE', *, *, #4990, .F. ) ;
#17807=LINE ( 'NONE', #24890, #24525 ) ;
#17808=CARTESIAN_POINT ( 'NONE',  ( -1.259920593601971062, -38.49623866863331045, 25.19630221849093488 ) ) ;
#17814=CARTESIAN_POINT ( 'NONE',  ( -25.21435515916025594, 1.749597353048488237E-16, -4.373993382621220594E-17 ) ) ;
#17826=VERTEX_POINT ( 'NONE', #8247 ) ;
#17832=CARTESIAN_POINT ( 'NONE',  ( -20.38016308990357217, 16.25718651464982045, -24.94368798801356490 ) ) ;
#17833=VECTOR ( 'NONE', #6623, 1000.000000000000114 ) ;
#17835=FACE_OUTER_BOUND ( 'NONE', #2843, .T. ) ;
#17842=CARTESIAN_POINT ( 'NONE',  ( -1.046935749539994465, -37.78548154587976882, 25.87617179820957602 ) ) ;
#17845=CARTESIAN_POINT ( 'NONE',  ( -1.050230347699842692, 1.897926697972695375E-16, 45.79907861674080749 ) ) ;
#17846=CARTESIAN_POINT ( 'NONE',  ( -23.79223135445719706, 33.03345552685145492, 3.207301057648455966 ) ) ;
#17848=CARTESIAN_POINT ( 'NONE',  ( -4.162674018437132695, -41.48630000627035486, 25.90909455705156006 ) ) ;
#17853=EDGE_LOOP ( 'NONE', ( #7237, #24847, #2551, #8570 ) ) ;
#17865=CARTESIAN_POINT ( 'NONE',  ( -1.259920593601968397, -25.19630221849078211, -38.49623866863340993 ) ) ;
#17869=CARTESIAN_POINT ( 'NONE',  ( -1.113548883309558368, 42.96943836789127147, 16.03115934825484956 ) ) ;
#17880=( BOUNDED_SURFACE ( )  B_SPLINE_SURFACE ( 3, 1, ( 
 ( #14013, #11725 ),
 ( #18481, #5241 ),
 ( #22971, #25117 ),
 ( #3226, #16029 ) ),
 .UNSPECIFIED., .F., .F., .F. ) 
 B_SPLINE_SURFACE_WITH_KNOTS ( ( 4, 4 ),
 ( 2, 2 ),
 ( 0.000000000000000000, 1.000000000000000000 ),
 ( 0.000000000000000000, 1.000000000000000000 ),
 .UNSPECIFIED. ) 
 GEOMETRIC_REPRESENTATION_ITEM ( )  RATIONAL_B_SPLINE_SURFACE ( (
 ( 1.000000000000000000, 1.000000000000000000),
 ( 0.9934239774497838349, 0.8357310067453913582),
 ( 0.9934239774497838349, 0.8357310067453913582),
 ( 1.000000000000000000, 1.000000000000000000) ) ) 
 REPRESENTATION_ITEM ( '' )  SURFACE ( )  );
#17887=EDGE_CURVE ( 'NONE', #27461, #15570, #2761, .T. ) ;
#17892=EDGE_CURVE ( 'NONE', #9035, #9765, #22121, .T. ) ;
#17897=CARTESIAN_POINT ( 'NONE',  ( -20.90916690077965256, -34.84883504600963988, -18.74041620980156253 ) ) ;
#17900=CARTESIAN_POINT ( 'NONE',  ( -21.41427618760458174, 19.54551635498129514, -23.81423075802588940 ) ) ;
#17904=B_SPLINE_CURVE_WITH_KNOTS ( 'NONE', 3,
 ( #1274, #25485, #21131, #21417, #21557, #14516, #10624 ),
 .UNSPECIFIED., .F., .F.,
 ( 4, 3, 4 ),
 ( 1.298148181579757605E-17, 0.009512539173626401862, 0.02506242213020844906 ),
 .UNSPECIFIED. ) ;
#17908=CARTESIAN_POINT ( 'NONE',  ( -4.780792508754331038, -49.38761389561005188, -3.764354093953405922 ) ) ;
#17913=CARTESIAN_POINT ( 'NONE',  ( -55.24728320129491266, -0.008013189884950039019, 0.01214321324516758234 ) ) ;
#17924=CARTESIAN_POINT ( 'NONE',  ( -55.24728320129491266, 0.01453410071985698077, 0.0006547948648746833647 ) ) ;
#17931=( NAMED_UNIT ( * ) PLANE_ANGLE_UNIT ( ) SI_UNIT ( $, .RADIAN. ) );
#17933=CARTESIAN_POINT ( 'NONE',  ( 180.4657679828686980, -1.252232817320263489E-15, 3.130582043300658722E-16 ) ) ;
#17943=AXIS2_PLACEMENT_3D ( 'NONE', #1205, #5677, #914 ) ;
#17949=CARTESIAN_POINT ( 'NONE',  ( -1.050230347699842692, 0.0002315326058698765721, -45.79907861674080749 ) ) ;
#17953=ADVANCED_FACE ( 'NONE', ( #14485 ), #15200, .T. ) ;
#17975=CARTESIAN_POINT ( 'NONE',  ( -18.41936578851708717, 30.66520733838696344, 29.33493038358041360 ) ) ;
#17977=CARTESIAN_POINT ( 'NONE',  ( -20.20700224038492721, -23.35150625415645820, 18.19058640100249491 ) ) ;
#17980=CARTESIAN_POINT ( 'NONE',  ( -1.619063947482197729, -25.20140673341345305, 38.92136151114934961 ) ) ;
#17986=CARTESIAN_POINT ( 'NONE',  ( -1.048172774974287069, 15.11899685083884393, 43.23017713506509097 ) ) ;
#17991=ADVANCED_FACE ( 'NONE', ( #21527 ), #2504, .F. ) ;
#17997=ORIENTED_EDGE ( 'NONE', *, *, #15984, .F. ) ;
#18005=CARTESIAN_POINT ( 'NONE',  ( -20.24419206586953379, 29.61012937815439372, -1.282847120831333898 ) ) ;
#18007=CARTESIAN_POINT ( 'NONE',  ( -1.583189561560253589, -43.29471907393730135, 16.68617981233748537 ) ) ;
#18008=B_SPLINE_CURVE_WITH_KNOTS ( 'NONE', 3,
 ( #14354, #18825, #14071, #7916, #16676, #25470, #21687, #1958, #13173, #17639, #28428, #19381, #1813 ),
 .UNSPECIFIED., .F., .F.,
 ( 4, 3, 3, 3, 4 ),
 ( 1.250926888277100303E-17, 0.0007657099931970524301, 0.001531419946797917637, 0.002296279302920158170, 0.003061450627205759400 ),
 .UNSPECIFIED. ) ;
#18015=CARTESIAN_POINT ( 'NONE',  ( -1.045287976400362417, 43.05558670614268379, 15.59869763335023229 ) ) ;
#18017=ADVANCED_FACE ( 'NONE', ( #13453 ), #19581, .F. ) ;
#18027=CARTESIAN_POINT ( 'NONE',  ( -21.41427618760448581, 7.777551129310475098, 29.81030852927058206 ) ) ;
#18033=CARTESIAN_POINT ( 'NONE',  ( -20.20898977204108604, -0.6607022527615499241, 29.59696883073212703 ) ) ;
#18041=AXIS2_PLACEMENT_3D ( 'NONE', #6819, #15564, #24375 ) ;
#18048=CARTESIAN_POINT ( 'NONE',  ( -10.86508079875781085, 50.32133009257468359, -9.118642906269416315 ) ) ;
#18049=B_SPLINE_CURVE_WITH_KNOTS ( 'NONE', 3,
 ( #2450, #24078, #22032, #11242, #17423, #2296, #297, #15686, #4767, #12969 ),
 .UNSPECIFIED., .F., .F.,
 ( 4, 2, 2, 2, 4 ),
 ( 7.757919228897728493E-18, 0.0003346267210630983675, 0.0006692534421261890371, 0.001003880163189279761, 0.001338506884252370268 ),
 .UNSPECIFIED. ) ;
#18053=CARTESIAN_POINT ( 'NONE',  ( -1.031422197589711764, -28.14735071801717226, 36.13727897780157150 ) ) ;
#18060=EDGE_CURVE ( 'NONE', #23596, #733, #357, .T. ) ;
#18080=CARTESIAN_POINT ( 'NONE',  ( -1.058197053496162665, 45.77356582045591438, 1.754224732379708662 ) ) ;
#18086=ORIENTED_EDGE ( 'NONE', *, *, #27529, .F. ) ;
#18091=EDGE_CURVE ( 'NONE', #27787, #15270, #6616, .T. ) ;
#18096=CARTESIAN_POINT ( 'NONE',  ( -1.056502255334265339, 27.33667001641170557, -36.75727364034741385 ) ) ;
#18102=CARTESIAN_POINT ( 'NONE',  ( -1.031422197589716205, 36.13727897780129439, -28.14735071801756661 ) ) ;
#18119=CARTESIAN_POINT ( 'NONE',  ( -1.619063947482197729, 11.94059994246222622, 44.80407745103770623 ) ) ;
#18121=ORIENTED_EDGE ( 'NONE', *, *, #3422, .T. ) ;
#18122=ORIENTED_EDGE ( 'NONE', *, *, #13703, .F. ) ;
#18130=CARTESIAN_POINT ( 'NONE',  ( -10.86508079875779842, 36.95527278096579948, 35.35100740321738044 ) ) ;
#18132=CARTESIAN_POINT ( 'NONE',  ( -20.20700224038492721, -29.58392382092674211, -0.9908225410477480288 ) ) ;
#18133=ORIENTED_EDGE ( 'NONE', *, *, #22200, .T. ) ;
#18138=CARTESIAN_POINT ( 'NONE',  ( -1.045287976400365970, 15.59869763335156101, 43.05558670614217931 ) ) ;
#18139=CARTESIAN_POINT ( 'NONE',  ( -21.41427618760446094, 30.75468365310879193, 1.815001260755948254 ) ) ;
#18153=EDGE_CURVE ( 'NONE', #4864, #17580, #17480, .T. ) ;
#18154=CARTESIAN_POINT ( 'NONE',  ( -1.046935749539993799, 43.14401153755488849, 15.35946454248350435 ) ) ;
#18155=CARTESIAN_POINT ( 'NONE',  ( -1.239374126674604337, 2.406737988131765871, 45.98822239537605583 ) ) ;
#18156=EDGE_CURVE ( 'NONE', #10460, #26876, #14081, .T. ) ;
#18160=ADVANCED_FACE ( 'NONE', ( #20406 ), #22597, .T. ) ;
#18179=B_SPLINE_CURVE_WITH_KNOTS ( 'NONE', 3,
 ( #17008, #12402, #14987, #8392, #23802, #23374, #25803 ),
 .UNSPECIFIED., .F., .F.,
 ( 4, 3, 4 ),
 ( 0.000000000000000000, 0.006568092053401790135, 0.02506242213020847681 ),
 .UNSPECIFIED. ) ;
#18182=B_SPLINE_CURVE_WITH_KNOTS ( 'NONE', 3,
 ( #26113, #23977, #15299, #23836, #15153, #6400, #6269, #6546 ),
 .UNSPECIFIED., .F., .F.,
 ( 4, 2, 2, 4 ),
 ( 0.000000000000000000, 0.002761524886576648477, 0.005523049773153296954, 0.01104609954630659391 ),
 .UNSPECIFIED. ) ;
#18183=ORIENTED_EDGE ( 'NONE', *, *, #1183, .F. ) ;
#18188=ADVANCED_FACE ( 'NONE', ( #690 ), #978, .F. ) ;
#18194=B_SPLINE_CURVE_WITH_KNOTS ( 'NONE', 3,
 ( #4392, #8573, #27999, #8712, #8441, #8298 ),
 .UNSPECIFIED., .F., .F.,
 ( 4, 2, 4 ),
 ( 0.000000000000000000, 0.0004335151646191501111, 0.0008670303292383002222 ),
 .UNSPECIFIED. ) ;
#18195=FACE_OUTER_BOUND ( 'NONE', #19687, .T. ) ;
#18200=CARTESIAN_POINT ( 'NONE',  ( -1.045287976400351981, 36.12803364096590997, -28.14015102489844011 ) ) ;
#18213=CARTESIAN_POINT ( 'NONE',  ( -25.21435515916025594, 1.749597353048488237E-16, -4.373993382621220594E-17 ) ) ;
#18217=EDGE_CURVE ( 'NONE', #22553, #27179, #9715, .T. ) ;
#18223=CARTESIAN_POINT ( 'NONE',  ( -8.786685647604898008, 38.68584556812353981, 37.00619870957891777 ) ) ;
#18225=ORIENTED_EDGE ( 'NONE', *, *, #9735, .T. ) ;
#18226=B_SPLINE_CURVE_WITH_KNOTS ( 'NONE', 3,
 ( #4533, #13306, #24571, #224, #15596, #6854 ),
 .UNSPECIFIED., .F., .F.,
 ( 4, 2, 4 ),
 ( 3.729292374017667178E-16, 0.003576372551511173073, 0.007152745103021973180 ),
 .UNSPECIFIED. ) ;
#18228=B_SPLINE_CURVE_WITH_KNOTS ( 'NONE', 3,
 ( #16567, #11826, #9967, #16280, #18588, #12251, #18726 ),
 .UNSPECIFIED., .F., .F.,
 ( 4, 3, 4 ),
 ( 1.309687503460226953E-17, 0.009512539173626405331, 0.02506242213020846293 ),
 .UNSPECIFIED. ) ;
#18233=DIRECTION ( 'NONE',  ( 0.000000000000000000, 5.223019709708233256E-21, -1.000000000000000000 ) ) ;
#18240=CARTESIAN_POINT ( 'NONE',  ( -55.24271866751342941, 0.009388511352200527849, -0.001425019990779188969 ) ) ;
#18243=CARTESIAN_POINT ( 'NONE',  ( -20.20612092514791058, -23.26073121129628873, 18.30568145913871447 ) ) ;
#18246=LINE ( 'NONE', #20562, #15193 ) ;
#18250=FACE_OUTER_BOUND ( 'NONE', #16198, .T. ) ;
#18251=VERTEX_POINT ( 'NONE', #15806 ) ;
#18253=ORIENTED_EDGE ( 'NONE', *, *, #13678, .T. ) ;
#18255=VERTEX_POINT ( 'NONE', #16084 ) ;
#18262=CARTESIAN_POINT ( 'NONE',  ( -1.583189561560255143, 43.29471907393764951, 16.68617981233656877 ) ) ;
#18266=CARTESIAN_POINT ( 'NONE',  ( -1.050229599974480843, -43.47850826583062656, -14.39582765040444912 ) ) ;
#18269=CARTESIAN_POINT ( 'NONE',  ( -20.20612091757417161, 27.77903622052274102, 10.22177757278288013 ) ) ;
#18275=CARTESIAN_POINT ( 'NONE',  ( -7.733045908741311258, -38.67583825854175217, -35.49239760110661024 ) ) ;
#18285=ORIENTED_EDGE ( 'NONE', *, *, #7766, .T. ) ;
#18287=CARTESIAN_POINT ( 'NONE',  ( -1.045287976400386842, 37.92705037016744285, -25.66401692420027203 ) ) ;
#18288=CARTESIAN_POINT ( 'NONE',  ( -1.048171036023507474, 43.23005599774320729, 15.11933492062782847 ) ) ;
#18299=CARTESIAN_POINT ( 'NONE',  ( -28.13707043255157103, 0.7675454997506996335, -22.88591869784691113 ) ) ;
#18302=CARTESIAN_POINT ( 'NONE',  ( -24.53239521893650021, -3.868435622621272163, 33.71193723315178659 ) ) ;
#18305=CARTESIAN_POINT ( 'NONE',  ( -1.155001620486251879, -2.068551059060010022, 45.85729774065939779 ) ) ;
#18311=ORIENTED_EDGE ( 'NONE', *, *, #23420, .T. ) ;
#18313=ORIENTED_EDGE ( 'NONE', *, *, #15886, .T. ) ;
#18320=B_SPLINE_CURVE_WITH_KNOTS ( 'NONE', 3,
 ( #27744, #3697, #14634, #7906, #27878, #23434 ),
 .UNSPECIFIED., .F., .F.,
 ( 4, 2, 4 ),
 ( 0.000000000000000000, 0.0004335184443140219679, 0.0008670368886280439358 ),
 .UNSPECIFIED. ) ;
#18321=ORIENTED_EDGE ( 'NONE', *, *, #15387, .F. ) ;
#18325=CARTESIAN_POINT ( 'NONE',  ( -55.25719721206881729, -0.0006290797159227240433, -0.01115102788683359700 ) ) ;
#18338=CARTESIAN_POINT ( 'NONE',  ( -8.786685647604890903, -52.67761315067279781, 9.545808661481174795 ) ) ;
#18346=EDGE_CURVE ( 'NONE', #1690, #25788, #24899, .T. ) ;
#18351=VERTEX_POINT ( 'NONE', #1254 ) ;
#18354=EDGE_CURVE ( 'NONE', #23186, #10231, #18884, .T. ) ;
#18355=CARTESIAN_POINT ( 'NONE',  ( -55.25719721206881729, -0.01115102788682980142, -0.0006290797159206544097 ) ) ;
#18363=CARTESIAN_POINT ( 'NONE',  ( -20.20997486282891131, 0.3303743256174362375, -29.60348406988234871 ) ) ;
#18364=CARTESIAN_POINT ( 'NONE',  ( -1.323439229708128551, -38.58845475799787295, -25.17120723334079457 ) ) ;
#18365=LINE ( 'NONE', #7312, #22655 ) ;
#18366=B_SPLINE_CURVE_WITH_KNOTS ( 'NONE', 3,
 ( #11333, #2695, #20106, #13917, #26869, #7178, #24744, #389, #9470, #11771 ),
 .UNSPECIFIED., .F., .F.,
 ( 4, 2, 2, 2, 4 ),
 ( 2.879654849182128713E-16, 0.0003346187017559071959, 0.0006692374035115264278, 0.001003856105267145714, 0.001338474807022764891 ),
 .UNSPECIFIED. ) ;
#18372=CARTESIAN_POINT ( 'NONE',  ( -20.57838717382308147, -28.96176188950213870, 7.715628353033985753 ) ) ;
#18375=VERTEX_POINT ( 'NONE', #10054 ) ;
#18377=DIRECTION ( 'NONE',  ( -5.541455922705464902E-20, 5.223019709708320524E-21, -1.000000000000000000 ) ) ;
#18378=CARTESIAN_POINT ( 'NONE',  ( -1.583189561560256253, -11.94859433442871399, 44.83405390829683057 ) ) ;
#18388=CARTESIAN_POINT ( 'NONE',  ( -20.38016308990357217, -23.16952666206571365, 18.69911008768360361 ) ) ;
#18389=CARTESIAN_POINT ( 'NONE',  ( -20.20612092514784663, 28.48192215759677737, 8.058517256680804763 ) ) ;
#18395=CARTESIAN_POINT ( 'NONE',  ( -55.25297051322618813, 0.01483298743814672610, -0.001818774723749509541 ) ) ;
#18396=CIRCLE ( 'NONE', #16560, 53.53553390275978785 ) ;
#18401=B_SPLINE_CURVE_WITH_KNOTS ( 'NONE', 3,
 ( #8698, #10580, #11006, #17463 ),
 .UNSPECIFIED., .F., .F.,
 ( 4, 4 ),
 ( 2.005388357681274105E-16, 0.001982023823822939412 ),
 .UNSPECIFIED. ) ;
#18404=ORIENTED_EDGE ( 'NONE', *, *, #4354, .F. ) ;
#18416=MECHANICAL_DESIGN_GEOMETRIC_PRESENTATION_REPRESENTATION('',(#11074),#13327);
#18417=ORIENTED_EDGE ( 'NONE', *, *, #10951, .T. ) ;
#18418=CARTESIAN_POINT ( 'NONE',  ( -55.24340739397742794, 0.007744344507854989193, -0.006539691034608598359 ) ) ;
#18419=CARTESIAN_POINT ( 'NONE',  ( -1.046936909428682672, -36.28616897897433091, 27.93981068760662012 ) ) ;
#18425=CARTESIAN_POINT ( 'NONE',  ( -6.574463467970655728, 51.07975593197905795, -5.014313797967199449 ) ) ;
#18426=B_SPLINE_CURVE_WITH_KNOTS ( 'NONE', 3,
 ( #2970, #11745, #230, #9019, #17908, #799, #6859, #7011 ),
 .UNSPECIFIED., .F., .F.,
 ( 4, 2, 2, 4 ),
 ( 2.324173423859648542E-16, 0.002761568181852869404, 0.005523136363705506355, 0.01104627272741079066 ),
 .UNSPECIFIED. ) ;
#18427=CARTESIAN_POINT ( 'NONE',  ( -1.048994561756806165, -45.79144455904140898, -0.7655149579821828310 ) ) ;
#18433=CARTESIAN_POINT ( 'NONE',  ( -1.056502255334264895, 0.5104472526226292439, 45.80535052436395915 ) ) ;
#18435=CARTESIAN_POINT ( 'NONE',  ( -55.24271866751342941, -0.006671293903667678896, -0.006757859501010191408 ) ) ;
#18436=ORIENTED_EDGE ( 'NONE', *, *, #2687, .T. ) ;
#18437=ORIENTED_EDGE ( 'NONE', *, *, #9767, .T. ) ;
#18440=ORIENTED_EDGE ( 'NONE', *, *, #12847, .F. ) ;
#18441=CIRCLE ( 'NONE', #8349, 34.60786435723138510 ) ;
#18442=B_SPLINE_CURVE_WITH_KNOTS ( 'NONE', 3,
 ( #8080, #16704, #5768, #19269, #25629, #23333, #8202, #5911 ),
 .UNSPECIFIED., .F., .F.,
 ( 4, 2, 2, 4 ),
 ( 2.299172327962918193E-16, 0.002761568181852868970, 0.005523136363705508090, 0.01104627272741078720 ),
 .UNSPECIFIED. ) ;
#18446=( BOUNDED_SURFACE ( )  B_SPLINE_SURFACE ( 3, 1, ( 
 ( #27491, #7803 ),
 ( #14237, #21156 ),
 ( #10248, #25507 ),
 ( #14539, #9958 ) ),
 .UNSPECIFIED., .F., .F., .F. ) 
 B_SPLINE_SURFACE_WITH_KNOTS ( ( 4, 4 ),
 ( 2, 2 ),
 ( 0.000000000000000000, 1.000000000000000000 ),
 ( 0.000000000000000000, 1.000000000000000000 ),
 .UNSPECIFIED. ) 
 GEOMETRIC_REPRESENTATION_ITEM ( )  RATIONAL_B_SPLINE_SURFACE ( (
 ( 1.000000000000000000, 1.000000000000000000),
 ( 0.9934239774497838349, 0.8357310067453913582),
 ( 0.9934239774497838349, 0.8357310067453913582),
 ( 1.000000000000000000, 1.000000000000000000) ) ) 
 REPRESENTATION_ITEM ( '' )  SURFACE ( )  );
#18447=AXIS2_PLACEMENT_3D ( 'NONE', #9183, #9770, #18377 ) ;
#18453=DIRECTION ( 'NONE',  ( -0.7563875759206388771, 0.4122509917856786443, 0.5078650950445640078 ) ) ;
#18456=LINE ( 'NONE', #7385, #12955 ) ;
#18457=AXIS2_PLACEMENT_3D ( 'NONE', #13537, #22035, #2899 ) ;
#18460=B_SPLINE_CURVE_WITH_KNOTS ( 'NONE', 3,
 ( #7232, #27059, #22487, #2750, #16135, #22341, #24934, #5196, #4773, #3050 ),
 .UNSPECIFIED., .F., .F.,
 ( 4, 2, 2, 2, 4 ),
 ( 2.863532086325413454E-16, 0.0003346187017559064912, 0.0006692374035115266446, 0.001003856105267146798, 0.001338474807022767060 ),
 .UNSPECIFIED. ) ;
#18462=CARTESIAN_POINT ( 'NONE',  ( -1.045287976400365970, 45.76855895860943235, -1.530335034934267258 ) ) ;
#18465=CARTESIAN_POINT ( 'NONE',  ( -25.21435515916025594, 1.749597353048488237E-16, -4.373993382621220594E-17 ) ) ;
#18479=VERTEX_POINT ( 'NONE', #4120 ) ;
#18481=CARTESIAN_POINT ( 'NONE',  ( -55.24300891470650754, -0.007734635432136225362, 0.006048736206179294861 ) ) ;
#18491=CARTESIAN_POINT ( 'NONE',  ( -1.464342487929852998, 25.15873223207692178, -38.76467504336592640 ) ) ;
#18493=CARTESIAN_POINT ( 'NONE',  ( -1.259972190295313599, -44.39825172539703146, -12.06706380853675142 ) ) ;
#18501=CARTESIAN_POINT ( 'NONE',  ( -8.259864102781680373, 47.98931516265592734, -22.52209142944943565 ) ) ;
#18503=CIRCLE ( 'NONE', #14374, 34.60786435723138510 ) ;
#18524=CARTESIAN_POINT ( 'NONE',  ( -1.239374126674604337, 38.61989855450975995, 25.08410696974200604 ) ) ;
#18525=( BOUNDED_SURFACE ( )  B_SPLINE_SURFACE ( 3, 1, ( 
 ( #23831, #12719 ),
 ( #10575, #14885 ),
 ( #3811, #10318 ),
 ( #21368, #6394 ) ),
 .UNSPECIFIED., .F., .F., .F. ) 
 B_SPLINE_SURFACE_WITH_KNOTS ( ( 4, 4 ),
 ( 2, 2 ),
 ( 0.000000000000000000, 1.000000000000000000 ),
 ( 0.000000000000000000, 1.000000000000000000 ),
 .UNSPECIFIED. ) 
 GEOMETRIC_REPRESENTATION_ITEM ( )  RATIONAL_B_SPLINE_SURFACE ( (
 ( 1.000000000000000000, 1.000000000000000000),
 ( 0.9593753223639863714, 0.9995975284513187731),
 ( 0.9593753223639863714, 0.9995975284513187731),
 ( 1.000000000000000000, 1.000000000000000000) ) ) 
 REPRESENTATION_ITEM ( '' )  SURFACE ( )  );
#18534=DIRECTION ( 'NONE',  ( 0.000000000000000000, -1.000000000000000000, 0.000000000000000000 ) ) ;
#18535=CARTESIAN_POINT ( 'NONE',  ( -1.058473599757823846, -45.77379534793241334, 1.755404039369906188 ) ) ;
#18536=CARTESIAN_POINT ( 'NONE',  ( -22.34422965417124018, -26.20925041532873223, -27.39717383755272451 ) ) ;
#18539=VERTEX_POINT ( 'NONE', #9577 ) ;
#18540=CARTESIAN_POINT ( 'NONE',  ( -8.786685647604885574, 6.096987947571466530E-17, -1.524246986892866633E-17 ) ) ;
#18541=CARTESIAN_POINT ( 'NONE',  ( -21.41430102051751660, -28.68859753627386766, 11.22990201072307137 ) ) ;
#18544=CARTESIAN_POINT ( 'NONE',  ( -20.47566338032515887, -7.708089572830225222, 28.85746366088577375 ) ) ;
#18546=CARTESIAN_POINT ( 'NONE',  ( -1.031422197589716205, -25.67058493451469658, -37.93675465142464276 ) ) ;
#18548=EDGE_LOOP ( 'NONE', ( #28435, #25856, #19732, #3534 ) ) ;
#18550=CARTESIAN_POINT ( 'NONE',  ( -2.904412668506649808, -30.27712468694961956, 36.79926976721486653 ) ) ;
#18571=VERTEX_POINT ( 'NONE', #7283 ) ;
#18572=CARTESIAN_POINT ( 'NONE',  ( -55.24271866751342941, -0.001425019990778742711, -0.009388511352200234680 ) ) ;
#18573=CARTESIAN_POINT ( 'NONE',  ( -1.019300379054419947, 42.90269154183450695, 16.06793277091947658 ) ) ;
#18582=CARTESIAN_POINT ( 'NONE',  ( -4.780792508754322157, 37.74278713234441796, 32.07473752860738614 ) ) ;
#18588=CARTESIAN_POINT ( 'NONE',  ( -18.41936578851712625, -30.66520733838672186, -29.33493038358061966 ) ) ;
#18591=( BOUNDED_SURFACE ( )  B_SPLINE_SURFACE ( 3, 1, ( 
 ( #19959, #17651 ),
 ( #24150, #21977 ),
 ( #28436, #11041 ),
 ( #8738, #26431 ) ),
 .UNSPECIFIED., .F., .F., .F. ) 
 B_SPLINE_SURFACE_WITH_KNOTS ( ( 4, 4 ),
 ( 2, 2 ),
 ( 0.000000000000000000, 1.000000000000000000 ),
 ( 0.000000000000000000, 1.000000000000000000 ),
 .UNSPECIFIED. ) 
 GEOMETRIC_REPRESENTATION_ITEM ( )  RATIONAL_B_SPLINE_SURFACE ( (
 ( 1.000000000000000000, 1.000000000000000000),
 ( 0.7789835883360578528, 0.9689951854195403280),
 ( 0.7789835883360578528, 0.9689951854195403280),
 ( 1.000000000000000000, 1.000000000000000000) ) ) 
 REPRESENTATION_ITEM ( '' )  SURFACE ( )  );
#18596=VERTEX_POINT ( 'NONE', #20215 ) ;
#18602=PRODUCT_DEFINITION_CONTEXT ( 'detailed design', #4206, 'design' ) ;
#18606=DIRECTION ( 'NONE',  ( 0.000000000000000000, 5.223019709707975211E-21, -1.000000000000000000 ) ) ;
#18607=CARTESIAN_POINT ( 'NONE',  ( -55.24340739397742084, -0.007744344507854280558, -0.006539691034612628989 ) ) ;
#18612=FACE_OUTER_BOUND ( 'NONE', #25519, .T. ) ;
#18622=CARTESIAN_POINT ( 'NONE',  ( -55.24390624410018802, -0.004896917417127438256, -0.009209468562451287102 ) ) ;
#18623=CARTESIAN_POINT ( 'NONE',  ( -1.046936909428682450, 27.93981068760674802, 36.28616897897423144 ) ) ;
#18632=CARTESIAN_POINT ( 'NONE',  ( -1.583189561560255143, 44.83405390829672399, -11.94859433442917762 ) ) ;
#18635=CARTESIAN_POINT ( 'NONE',  ( -25.21435515916025594, 1.749597353048488237E-16, -4.373993382621220594E-17 ) ) ;
#18638=CARTESIAN_POINT ( 'NONE',  ( -1.155031165708886087, 25.28071330859886245, -38.31525684316149949 ) ) ;
#18651=CARTESIAN_POINT ( 'NONE',  ( -1.031422197589711764, 28.14735071801743871, -36.13727897780136544 ) ) ;
#18652=CARTESIAN_POINT ( 'NONE',  ( -21.41427618760447515, -7.777551129310266376, -29.81030852927063890 ) ) ;
#18660=( BOUNDED_SURFACE ( )  B_SPLINE_SURFACE ( 3, 1, ( 
 ( #18622, #12414 ),
 ( #5375, #1485 ),
 ( #16460, #5519 ),
 ( #14141, #3500 ) ),
 .UNSPECIFIED., .F., .F., .F. ) 
 B_SPLINE_SURFACE_WITH_KNOTS ( ( 4, 4 ),
 ( 2, 2 ),
 ( 0.000000000000000000, 1.000000000000000000 ),
 ( 0.000000000000000000, 1.000000000000000000 ),
 .UNSPECIFIED. ) 
 GEOMETRIC_REPRESENTATION_ITEM ( )  RATIONAL_B_SPLINE_SURFACE ( (
 ( 1.000000000000000000, 1.000000000000000000),
 ( 0.9934239774497837239, 0.8357310067453919133),
 ( 0.9934239774497837239, 0.8357310067453919133),
 ( 1.000000000000000000, 1.000000000000000000) ) ) 
 REPRESENTATION_ITEM ( '' )  SURFACE ( )  );
#18670=ORIENTED_EDGE ( 'NONE', *, *, #21425, .F. ) ;
#18674=CARTESIAN_POINT ( 'NONE',  ( -4.473127245936431073, -41.70021447285034810, 26.34600523034583119 ) ) ;
#18678=ORIENTED_EDGE ( 'NONE', *, *, #18346, .T. ) ;
#18679=CARTESIAN_POINT ( 'NONE',  ( -16.86833981943423666, 7.884812276282103127, -43.51541671545727041 ) ) ;
#18683=CARTESIAN_POINT ( 'NONE',  ( -20.38016308990357217, -7.753479680700753107, 28.74660391518353109 ) ) ;
#18689=CARTESIAN_POINT ( 'NONE',  ( -1.058197053496171769, -42.99116279335166269, -15.81317659443667445 ) ) ;
#18697=ORIENTED_EDGE ( 'NONE', *, *, #15631, .F. ) ;
#18701=CARTESIAN_POINT ( 'NONE',  ( -1.058197053496158890, 12.47644286888577270, 44.07533330186774378 ) ) ;
#18702=EDGE_CURVE ( 'NONE', #600, #12444, #13101, .T. ) ;
#18703=ORIENTED_EDGE ( 'NONE', *, *, #15313, .T. ) ;
#18705=( BOUNDED_SURFACE ( )  B_SPLINE_SURFACE ( 3, 1, ( 
 ( #10133, #3784 ),
 ( #21042, #25537 ),
 ( #6767, #23240 ),
 ( #3492, #12276 ) ),
 .UNSPECIFIED., .F., .F., .F. ) 
 B_SPLINE_SURFACE_WITH_KNOTS ( ( 4, 4 ),
 ( 2, 2 ),
 ( 0.000000000000000000, 1.000000000000000000 ),
 ( 0.000000000000000000, 1.000000000000000000 ),
 .UNSPECIFIED. ) 
 GEOMETRIC_REPRESENTATION_ITEM ( )  RATIONAL_B_SPLINE_SURFACE ( (
 ( 1.000000000000000000, 1.000000000000000000),
 ( 0.7789835883360578528, 0.9689951854195403280),
 ( 0.7789835883360578528, 0.9689951854195403280),
 ( 1.000000000000000000, 1.000000000000000000) ) ) 
 REPRESENTATION_ITEM ( '' )  SURFACE ( )  );
#18710=VECTOR ( 'NONE', #20112, 999.9999999999998863 ) ;
#18722=CARTESIAN_POINT ( 'NONE',  ( -5.986830583229486358, 50.53158596890444443, -4.559539818181313819 ) ) ;
#18725=CARTESIAN_POINT ( 'NONE',  ( -55.24340739397742084, -0.009386184976286139278, -0.003826481709803953961 ) ) ;
#18726=CARTESIAN_POINT ( 'NONE',  ( -25.21435515916043357, -25.00736669481038987, -23.92354251275926558 ) ) ;
#18734=EDGE_CURVE ( 'NONE', #26383, #22553, #394, .T. ) ;
#18739=EDGE_LOOP ( 'NONE', ( #6810, #27475, #21929, #27126 ) ) ;
#18740=CARTESIAN_POINT ( 'NONE',  ( -7.078251931573406708, 20.86696228105292761, 47.71415099571781582 ) ) ;
#18744=CARTESIAN_POINT ( 'NONE',  ( -20.20700224038492721, 16.58740185276746359, 24.51628800869029234 ) ) ;
#18748=CARTESIAN_POINT ( 'NONE',  ( -20.20612092514784308, 24.59769888281557471, 16.46550332780499559 ) ) ;
#18758=VERTEX_POINT ( 'NONE', #20018 ) ;
#18760=CIRCLE ( 'NONE', #10950, 44.74884827092600403 ) ;
#18762=CARTESIAN_POINT ( 'NONE',  ( -8.786685647604885574, 6.096987947571466530E-17, -1.524246986892866633E-17 ) ) ;
#18764=CARTESIAN_POINT ( 'NONE',  ( -1.050230346682680560, 26.91946103437159721, 37.05264119692660785 ) ) ;
#18765=ORIENTED_EDGE ( 'NONE', *, *, #22200, .F. ) ;
#18768=ORIENTED_EDGE ( 'NONE', *, *, #28227, .T. ) ;
#18772=CARTESIAN_POINT ( 'NONE',  ( -15.02187109954782862, -41.75590530176324222, -20.12219089991075904 ) ) ;
#18773=CARTESIAN_POINT ( 'NONE',  ( -1.058473599757821404, -1.755404039369745650, -45.77379534793243465 ) ) ;
#18779=( BOUNDED_SURFACE ( )  B_SPLINE_SURFACE ( 3, 1, ( 
 ( #27743, #20680 ),
 ( #3135, #11911 ),
 ( #3278, #18674 ),
 ( #20964, #12059 ) ),
 .UNSPECIFIED., .F., .F., .F. ) 
 B_SPLINE_SURFACE_WITH_KNOTS ( ( 4, 4 ),
 ( 2, 2 ),
 ( 0.000000000000000000, 1.000000000000000000 ),
 ( 0.000000000000000000, 1.000000000000000000 ),
 .UNSPECIFIED. ) 
 GEOMETRIC_REPRESENTATION_ITEM ( )  RATIONAL_B_SPLINE_SURFACE ( (
 ( 1.000000000000000000, 1.000000000000000000),
 ( 0.7789835883360578528, 0.9689951854195403280),
 ( 0.7789835883360578528, 0.9689951854195403280),
 ( 1.000000000000000000, 1.000000000000000000) ) ) 
 REPRESENTATION_ITEM ( '' )  SURFACE ( )  );
#18781=ORIENTED_EDGE ( 'NONE', *, *, #27490, .T. ) ;
#18786=CARTESIAN_POINT ( 'NONE',  ( -20.57838717382308147, -7.715628353033886278, -28.96176188950215646 ) ) ;
#18788=CARTESIAN_POINT ( 'NONE',  ( -4.473127245936431073, 18.25038884639870673, -45.82513704981550262 ) ) ;
#18789=B_SPLINE_CURVE_WITH_KNOTS ( 'NONE', 3,
 ( #16194, #23132, #16337, #12172, #12441, #25134, #1362, #14167 ),
 .UNSPECIFIED., .F., .F.,
 ( 4, 2, 2, 4 ),
 ( 0.000000000000000000, 0.002761524886576648043, 0.005523049773153296087, 0.01104609954630659217 ),
 .UNSPECIFIED. ) ;
#18790=ORIENTED_EDGE ( 'NONE', *, *, #5781, .F. ) ;
#18795=ORIENTED_EDGE ( 'NONE', *, *, #20535, .T. ) ;
#18797=CARTESIAN_POINT ( 'NONE',  ( -7.711401346138398338, -51.42722225669428582, -10.36923727626100522 ) ) ;
#18798=CONICAL_SURFACE ( 'NONE', #19246, 34.60786435723138510, 0.8559913436420825139 ) ;
#18799=ORIENTED_EDGE ( 'NONE', *, *, #7300, .F. ) ;
#18802=CARTESIAN_POINT ( 'NONE',  ( -22.23226125620944771, 26.80886670319662102, 16.78323347921887887 ) ) ;
#18805=CARTESIAN_POINT ( 'NONE',  ( -55.24390624410018802, -0.007245494385991098352, -0.007503127514281985981 ) ) ;
#18806=CARTESIAN_POINT ( 'NONE',  ( -1.583189561560253589, -36.01941156322766346, 29.24830400313204848 ) ) ;
#18809=CARTESIAN_POINT ( 'NONE',  ( -20.21097721712958872, 28.26295595852185727, -8.835581498567558256 ) ) ;
#18813=CARTESIAN_POINT ( 'NONE',  ( -20.21097721712958872, -28.05863618200116250, -9.464413111084637009 ) ) ;
#18822=CARTESIAN_POINT ( 'NONE',  ( 14.74894986621300141, -1.023413983156985299E-16, 2.558534957892463246E-17 ) ) ;
#18823=EDGE_CURVE ( 'NONE', #20516, #10945, #9337, .T. ) ;
#18825=CARTESIAN_POINT ( 'NONE',  ( -1.046936909428679785, -43.14407378092982981, 15.35929614323710801 ) ) ;
#18832=CARTESIAN_POINT ( 'NONE',  ( -10.86508079875781263, 45.04061326950873223, -24.22249093393315533 ) ) ;
#18833=CARTESIAN_POINT ( 'NONE',  ( -55.24390624410018802, 0.007503127514278223366, 0.007245494385991344682 ) ) ;
#18846=VECTOR ( 'NONE', #24688, 1000.000000000000114 ) ;
#18847=ORIENTED_EDGE ( 'NONE', *, *, #1840, .T. ) ;
#18852=ORIENTED_EDGE ( 'NONE', *, *, #2993, .T. ) ;
#18858=ORIENTED_EDGE ( 'NONE', *, *, #11273, .T. ) ;
#18859=ADVANCED_FACE ( 'NONE', ( #14402 ), #11556, .T. ) ;
#18868=CARTESIAN_POINT ( 'NONE',  ( -2.911734481061402757, 47.57875121082948766, -2.802366807346352129 ) ) ;
#18881=ORIENTED_EDGE ( 'NONE', *, *, #23679, .T. ) ;
#18882=CIRCLE ( 'NONE', #13366, 53.53553390275978785 ) ;
#18884=B_SPLINE_CURVE_WITH_KNOTS ( 'NONE', 3,
 ( #19109, #27589, #1542, #23302, #18679, #14778, #25870 ),
 .UNSPECIFIED., .F., .F.,
 ( 4, 3, 4 ),
 ( 0.000000000000000000, 0.006568092053401815289, 0.02506242213020845253 ),
 .UNSPECIFIED. ) ;
#18891=CARTESIAN_POINT ( 'NONE',  ( -1.113427685307000203, 1.967672929087815881, 45.82016658690749722 ) ) ;
#18895=CARTESIAN_POINT ( 'NONE',  ( -1.619063947482197729, 46.30105812165548684, -2.489035965910316506 ) ) ;
#18898=EDGE_CURVE ( 'NONE', #28309, #26876, #19832, .T. ) ;
#18902=AXIS2_PLACEMENT_3D ( 'NONE', #8019, #5844, #14604 ) ;
#18904=CARTESIAN_POINT ( 'NONE',  ( -1.619063947482194177, 35.99532424477422410, 29.22875152547716482 ) ) ;
#18907=CARTESIAN_POINT ( 'NONE',  ( -4.473127245936434626, 45.82513704981544578, -18.25038884639885950 ) ) ;
#18918=VECTOR ( 'NONE', #25289, 999.9999999999998863 ) ;
#18921=CARTESIAN_POINT ( 'NONE',  ( 7.762687761849954095E-17, 6.048924312129458720E-15, -44.74884827092600403 ) ) ;
#18923=EDGE_CURVE ( 'NONE', #20933, #25194, #18228, .T. ) ;
#18924=CARTESIAN_POINT ( 'NONE',  ( -1.044556982611271279, -1.643392503293034768, -45.76404732357878657 ) ) ;
#18929=CARTESIAN_POINT ( 'NONE',  ( -23.79248802219722592, -7.157555990716680583, 32.40806545715339126 ) ) ;
#18936=CARTESIAN_POINT ( 'NONE',  ( -20.21097721650786738, 8.835581399095163491, -28.26295598655176633 ) ) ;
#18950=CARTESIAN_POINT ( 'NONE',  ( -25.21435515916043713, 30.48034229288662544, 16.39063784838709736 ) ) ;
#18953=CARTESIAN_POINT ( 'NONE',  ( -55.25297051322618813, 0.001818774723749727032, -0.01483298743815054943 ) ) ;
#18957=DIRECTION ( 'NONE',  ( 0.7637818620346800147, 0.3965875333584841234, -0.5092696688508654423 ) ) ;
#18958=CARTESIAN_POINT ( 'NONE',  ( -22.23226125620943705, 20.31044300692207472, 24.24619897613454000 ) ) ;
#18962=CARTESIAN_POINT ( 'NONE',  ( -1.619063947482197729, 46.30105812165548684, -2.489035965910316506 ) ) ;
#18966=VECTOR ( 'NONE', #4397, 1000.000000000000000 ) ;
#18967=ORIENTED_EDGE ( 'NONE', *, *, #16963, .F. ) ;
#18973=CARTESIAN_POINT ( 'NONE',  ( -20.57838717382308147, 27.96569011373101077, 10.78122205916971055 ) ) ;
#18977=CARTESIAN_POINT ( 'NONE',  ( -1.463510566862838091, -44.64091840826481672, 11.94877850058549029 ) ) ;
#18985=CARTESIAN_POINT ( 'NONE',  ( -9.156249394959706578, 8.027840202793937507, -53.90509764945131366 ) ) ;
#18988=ADVANCED_FACE ( 'NONE', ( #21588 ), #14827, .T. ) ;
#18993=ORIENTED_EDGE ( 'NONE', *, *, #7940, .F. ) ;
#19004=FACE_OUTER_BOUND ( 'NONE', #25685, .T. ) ;
#19005=CARTESIAN_POINT ( 'NONE',  ( -28.13707043255157103, 18.06394523322453693, -14.07296284901339334 ) ) ;
#19008=CARTESIAN_POINT ( 'NONE',  ( -1.045287976400365970, -43.05558670614224326, 15.59869763335140469 ) ) ;
#19009=CARTESIAN_POINT ( 'NONE',  ( -25.21435515916025594, 1.749597353048488237E-16, -4.373993382621220594E-17 ) ) ;
#19020=CARTESIAN_POINT ( 'NONE',  ( -1.045287976400365970, -36.12803364096568259, 28.14015102489869591 ) ) ;
#19024=B_SPLINE_CURVE_WITH_KNOTS ( 'NONE', 3,
 ( #15516, #136, #6629, #21880, #24627, #15238, #2137, #415 ),
 .UNSPECIFIED., .F., .F.,
 ( 4, 2, 2, 4 ),
 ( 0.000000000000000000, 0.002761524886576667125, 0.005523049773153334251, 0.01104609954630666677 ),
 .UNSPECIFIED. ) ;
#19044=CARTESIAN_POINT ( 'NONE',  ( -1.031422197589716205, -36.13727897780108123, 28.14735071801782951 ) ) ;
#19050=CARTESIAN_POINT ( 'NONE',  ( -55.24728320129491266, -0.008013189884951492717, -0.01214321324517155139 ) ) ;
#19054=CARTESIAN_POINT ( 'NONE',  ( -20.37983603106073716, 23.16947629293390065, 18.69865230096500852 ) ) ;
#19055=CARTESIAN_POINT ( 'NONE',  ( -1.048996300304505747, 27.53442103413745912, 36.59642367107714023 ) ) ;
#19062=ADVANCED_FACE ( 'NONE', ( #4734 ), #26264, .T. ) ;
#19066=CARTESIAN_POINT ( 'NONE',  ( -1.056502255334265339, -27.33667001641142846, 36.75727364034761990 ) ) ;
#19067=CARTESIAN_POINT ( 'NONE',  ( -20.20612092514784663, 1.137292630518469849, 29.57813644637188233 ) ) ;
#19072=ORIENTED_EDGE ( 'NONE', *, *, #19618, .T. ) ;
#19073=ORIENTED_EDGE ( 'NONE', *, *, #17408, .T. ) ;
#19078=DIRECTION ( 'NONE',  ( 1.000000000000000000, -6.938893903907226837E-18, 1.734723475976806709E-18 ) ) ;
#19094=CARTESIAN_POINT ( 'NONE',  ( -20.57838717382308147, 7.715628353033680220, -28.96176188950220975 ) ) ;
#19095=FACE_OUTER_BOUND ( 'NONE', #13752, .T. ) ;
#19098=CARTESIAN_POINT ( 'NONE',  ( -7.078251931573406708, -38.93060825814203696, 34.59014398252958244 ) ) ;
#19101=CARTESIAN_POINT ( 'NONE',  ( -20.57838717382308147, 29.92853265176831812, 1.611677988432465014 ) ) ;
#19104=DIRECTION ( 'NONE',  ( 0.7563875759206388771, 0.4122509917856751471, -0.5078650950445667833 ) ) ;
#19105=CARTESIAN_POINT ( 'NONE',  ( -1.155031165708893415, -45.85732438018708024, 2.068616213631418344 ) ) ;
#19109=CARTESIAN_POINT ( 'NONE',  ( -25.21435515916043357, 6.169479169075458458, -34.05351380035335751 ) ) ;
#19118=CARTESIAN_POINT ( 'NONE',  ( -1.113548883309563253, -44.18588492042580640, 12.28732181966563886 ) ) ;
#19123=FACE_OUTER_BOUND ( 'NONE', #20123, .T. ) ;
#19138=LINE ( 'NONE', #1574, #17611 ) ;
#19144=VERTEX_POINT ( 'NONE', #7630 ) ;
#19157=EDGE_CURVE ( 'NONE', #6911, #9397, #1765, .T. ) ;
#19163=VERTEX_POINT ( 'NONE', #23027 ) ;
#19166=B_SPLINE_CURVE_WITH_KNOTS ( 'NONE', 3,
 ( #25918, #14680, #10389, #21307 ),
 .UNSPECIFIED., .F., .F.,
 ( 4, 4 ),
 ( 1.977889076651310254E-16, 0.001982023823822937677 ),
 .UNSPECIFIED. ) ;
#19172=CARTESIAN_POINT ( 'NONE',  ( -1.031422197589711987, 36.13727897780127307, -28.14735071801756661 ) ) ;
#19176=CARTESIAN_POINT ( 'NONE',  ( -20.20700224038492010, 24.51628800869071867, 16.58740185276683832 ) ) ;
#19178=CARTESIAN_POINT ( 'NONE',  ( -20.90916690077959927, 17.17795951644708907, 35.64494649500667833 ) ) ;
#19181=EDGE_CURVE ( 'NONE', #17575, #21619, #26147, .T. ) ;
#19189=CARTESIAN_POINT ( 'NONE',  ( -1.259972190295298500, 38.49631882650683679, 25.19627397134255986 ) ) ;
#19211=VERTEX_POINT ( 'NONE', #13934 ) ;
#19213=CARTESIAN_POINT ( 'NONE',  ( -4.178947244162637631, -25.96944194166761832, 41.47292084251660782 ) ) ;
#19228=CARTESIAN_POINT ( 'NONE',  ( -4.473127245936434626, 3.196405119334491562, 49.22197550883364414 ) ) ;
#19233=CARTESIAN_POINT ( 'NONE',  ( -20.37983603106074781, 24.94323704205437409, -16.25728007463414571 ) ) ;
#19246=AXIS2_PLACEMENT_3D ( 'NONE', #18465, #22952, #20332 ) ;
#19255=CARTESIAN_POINT ( 'NONE',  ( -4.473127245936431073, -37.94261489385741015, -31.51789735524179648 ) ) ;
#19258=FACE_OUTER_BOUND ( 'NONE', #26620, .T. ) ;
#19260=ADVANCED_FACE ( 'NONE', ( #6032 ), #26341, .F. ) ;
#19261=ORIENTED_EDGE ( 'NONE', *, *, #1816, .T. ) ;
#19264=CARTESIAN_POINT ( 'NONE',  ( -1.155001620486255431, -35.88346938217574689, -28.62773628245655644 ) ) ;
#19268=CIRCLE ( 'NONE', #9640, 53.53553390275978785 ) ;
#19269=CARTESIAN_POINT ( 'NONE',  ( -4.162674018437153123, 47.46216648493558665, -11.82104147411576989 ) ) ;
#19279=VERTEX_POINT ( 'NONE', #10219 ) ;
#19288=CARTESIAN_POINT ( 'NONE',  ( -20.20700224038492010, 8.199606986804733211, 28.44216453106527709 ) ) ;
#19293=ORIENTED_EDGE ( 'NONE', *, *, #27529, .T. ) ;
#19297=ORIENTED_EDGE ( 'NONE', *, *, #24070, .T. ) ;
#19301=CARTESIAN_POINT ( 'NONE',  ( -20.38016308990357928, 10.62413300761025425, 27.81387210821410250 ) ) ;
#19303=ADVANCED_FACE ( 'NONE', ( #3711 ), #29, .F. ) ;
#19305=CARTESIAN_POINT ( 'NONE',  ( -1.619063947482194177, 25.20140673341374438, -38.92136151114915066 ) ) ;
#19319=ORIENTED_EDGE ( 'NONE', *, *, #2865, .T. ) ;
#19324=CONICAL_SURFACE ( 'NONE', #16583, 34.60786435723138510, 0.8559913436420825139 ) ;
#19326=EDGE_CURVE ( 'NONE', #11861, #4018, #12095, .T. ) ;
#19328=CARTESIAN_POINT ( 'NONE',  ( -22.23226125620930560, 7.677408153694024406, -30.68305173820428067 ) ) ;
#19338=CARTESIAN_POINT ( 'NONE',  ( -28.13707043255157103, -0.7675454997505393173, 22.88591869784691468 ) ) ;
#19345=CARTESIAN_POINT ( 'NONE',  ( -1.056502255334265339, 43.72121397317224734, -13.66916755949864637 ) ) ;
#19352=ORIENTED_EDGE ( 'NONE', *, *, #3645, .T. ) ;
#19354=B_SPLINE_CURVE_WITH_KNOTS ( 'NONE', 3,
 ( #22184, #9086, #17846, #4908, #18139, #15687 ),
 .UNSPECIFIED., .F., .F.,
 ( 4, 2, 4 ),
 ( 9.341771812940338307E-18, 0.003576372551510817021, 0.007152745103021624501 ),
 .UNSPECIFIED. ) ;
#19359=AXIS2_PLACEMENT_3D ( 'NONE', #12377, #28058, #28194 ) ;
#19362=( BOUNDED_SURFACE ( )  B_SPLINE_SURFACE ( 3, 1, ( 
 ( #8155, #16922 ),
 ( #3822, #12587 ),
 ( #20812, #1097 ),
 ( #9886, #18651 ) ),
 .UNSPECIFIED., .F., .F., .F. ) 
 B_SPLINE_SURFACE_WITH_KNOTS ( ( 4, 4 ),
 ( 2, 2 ),
 ( 0.000000000000000000, 1.000000000000000000 ),
 ( 0.000000000000000000, 1.000000000000000000 ),
 .UNSPECIFIED. ) 
 GEOMETRIC_REPRESENTATION_ITEM ( )  RATIONAL_B_SPLINE_SURFACE ( (
 ( 1.000000000000000000, 1.000000000000000000),
 ( 0.9934239774497837239, 0.8357310067453919133),
 ( 0.9934239774497837239, 0.8357310067453919133),
 ( 1.000000000000000000, 1.000000000000000000) ) ) 
 REPRESENTATION_ITEM ( '' )  SURFACE ( )  );
#19368=CARTESIAN_POINT ( 'NONE',  ( -1.239374126674604337, 45.98822239537607004, 2.406737988131282702 ) ) ;
#19369=CARTESIAN_POINT ( 'NONE',  ( -25.21435515916043713, -34.05351380035328646, 6.169479169075816394 ) ) ;
#19377=CARTESIAN_POINT ( 'NONE',  ( -28.41354790283022069, 1.249099604787076601, -23.16239616762931064 ) ) ;
#19381=CARTESIAN_POINT ( 'NONE',  ( -1.046935749539998906, -43.93230528057173956, 12.93334586714225054 ) ) ;
#19382=B_SPLINE_CURVE_WITH_KNOTS ( 'NONE', 3,
 ( #9082, #9383, #26913, #6933, #24786, #4763, #3320, #3460, #12244, #23479 ),
 .UNSPECIFIED., .F., .F.,
 ( 4, 2, 2, 2, 4 ),
 ( 4.210279659405072890E-18, 0.0003346267210630959280, 0.0006692534421261876277, 0.001003880163189279110, 0.001338506884252370919 ),
 .UNSPECIFIED. ) ;
#19386=EDGE_LOOP ( 'NONE', ( #7743, #7349, #9068, #25912 ) ) ;
#19391=ORIENTED_EDGE ( 'NONE', *, *, #3912, .T. ) ;
#19392=CARTESIAN_POINT ( 'NONE',  ( -55.24390624410018802, -0.004896917417131185259, 0.009209468562452437224 ) ) ;
#19393=ADVANCED_FACE ( 'NONE', ( #15052 ), #7975, .F. ) ;
#19401=FACE_OUTER_BOUND ( 'NONE', #14712, .T. ) ;
#19405=CARTESIAN_POINT ( 'NONE',  ( -1.049817751779888786, 36.75003908324330837, 27.33161971822157810 ) ) ;
#19407=CARTESIAN_POINT ( 'NONE',  ( -55.24271866751342941, -0.006671293903667674559, -0.006757859501010194010 ) ) ;
#19411=CARTESIAN_POINT ( 'NONE',  ( -4.162674018437130030, 3.424137510344948510, -48.79210541969630555 ) ) ;
#19412=CARTESIAN_POINT ( 'NONE',  ( -25.21435515916043357, -16.39063784838764093, -30.48034229288631991 ) ) ;
#19414=CARTESIAN_POINT ( 'NONE',  ( -9.156249394959706578, -9.022661520478157726, -53.74753343182698728 ) ) ;
#19416=CARTESIAN_POINT ( 'NONE',  ( -20.47566338032535782, -10.72601609985042792, -27.87687989047296355 ) ) ;
#19417=ORIENTED_EDGE ( 'NONE', *, *, #2993, .F. ) ;
#19421=CARTESIAN_POINT ( 'NONE',  ( -8.786685647604898008, 48.22796981442765940, -23.24040270374399952 ) ) ;
#19422=CARTESIAN_POINT ( 'NONE',  ( -8.786685647604885574, 6.096987947571466530E-17, -1.524246986892866633E-17 ) ) ;
#19437=ORIENTED_EDGE ( 'NONE', *, *, #27770, .F. ) ;
#19442=B_SPLINE_CURVE_WITH_KNOTS ( 'NONE', 3,
 ( #24714, #15597, #26416, #20077, #15907, #9014 ),
 .UNSPECIFIED., .F., .F.,
 ( 4, 2, 4 ),
 ( 6.505213034913026604E-19, 0.0004335151646191478343, 0.0008670303292382950180 ),
 .UNSPECIFIED. ) ;
#19446=DIRECTION ( 'NONE',  ( 1.000000000000000000, -6.938893903907226837E-18, 1.734723475976806709E-18 ) ) ;
#19449=VECTOR ( 'NONE', #12140, 1000.000000000000000 ) ;
#19453=CARTESIAN_POINT ( 'NONE',  ( -8.786685647604706162, -38.68584556812290032, 37.00619870957955015 ) ) ;
#19457=CARTESIAN_POINT ( 'NONE',  ( -55.24198130335446422, -0.006527480770973291720, -0.006617369590172134802 ) ) ;
#19462=B_SPLINE_CURVE_WITH_KNOTS ( 'NONE', 3,
 ( #11207, #20118, #2558, #5004, #26881, #17808, #4578, #13641, #266, #22587 ),
 .UNSPECIFIED., .F., .F.,
 ( 4, 2, 2, 2, 4 ),
 ( 2.799429325053882983E-16, 0.0003346187017559012328, 0.0006692374035115225247, 0.001003856105267143762, 0.001338474807022765108 ),
 .UNSPECIFIED. ) ;
#19468=ORIENTED_EDGE ( 'NONE', *, *, #909, .F. ) ;
#19473=EDGE_CURVE ( 'NONE', #20885, #14674, #10667, .T. ) ;
#19475=CARTESIAN_POINT ( 'NONE',  ( -22.23342874802668589, 26.81018246605539446, -16.78332232459650797 ) ) ;
#19490=CARTESIAN_POINT ( 'NONE',  ( -20.37983603106074426, 10.62371319148641291, -27.81368274044714539 ) ) ;
#19496=CARTESIAN_POINT ( 'NONE',  ( -1.049819825607600121, -37.34982882986862052, -26.50610175068254293 ) ) ;
#19504=CARTESIAN_POINT ( 'NONE',  ( -8.786685647604885574, 6.096987947571466530E-17, -1.524246986892866633E-17 ) ) ;
#19510=CARTESIAN_POINT ( 'NONE',  ( -25.21435515916043713, -30.48034229288650820, -16.39063784838731053 ) ) ;
#19514=CARTESIAN_POINT ( 'NONE',  ( -20.47566262905010248, 7.708089517695595028, 28.85746289809567600 ) ) ;
#19515=CARTESIAN_POINT ( 'NONE',  ( -24.53239521893647179, -33.71193723315173685, -3.868435622621356096 ) ) ;
#19516=CARTESIAN_POINT ( 'NONE',  ( -1.019300379054419947, -12.21833869579496579, -44.15350047934394695 ) ) ;
#19533=CARTESIAN_POINT ( 'NONE',  ( -1.619063947482194177, -46.30105812165547974, 2.489035965910640247 ) ) ;
#19537=( BOUNDED_SURFACE ( )  B_SPLINE_SURFACE ( 3, 1, ( 
 ( #3068, #27519 ),
 ( #7688, #20612 ),
 ( #18607, #20755 ),
 ( #2926, #14266 ) ),
 .UNSPECIFIED., .F., .F., .F. ) 
 B_SPLINE_SURFACE_WITH_KNOTS ( ( 4, 4 ),
 ( 2, 2 ),
 ( 0.000000000000000000, 1.000000000000000000 ),
 ( 0.000000000000000000, 1.000000000000000000 ),
 .UNSPECIFIED. ) 
 GEOMETRIC_REPRESENTATION_ITEM ( )  RATIONAL_B_SPLINE_SURFACE ( (
 ( 1.000000000000000000, 1.000000000000000000),
 ( 0.9934239774497838349, 0.8357310067453913582),
 ( 0.9934239774497838349, 0.8357310067453913582),
 ( 1.000000000000000000, 1.000000000000000000) ) ) 
 REPRESENTATION_ITEM ( '' )  SURFACE ( )  );
#19542=ORIENTED_EDGE ( 'NONE', *, *, #25561, .T. ) ;
#19555=EDGE_CURVE ( 'NONE', #19834, #28309, #25754, .T. ) ;
#19557=CARTESIAN_POINT ( 'NONE',  ( -8.786685647604887350, 53.04920435127183254, -7.199674155859138835 ) ) ;
#19563=CARTESIAN_POINT ( 'NONE',  ( -7.078251931573406708, -50.86685171665420313, -11.16394717458656949 ) ) ;
#19568=EDGE_CURVE ( 'NONE', #27747, #7819, #12931, .T. ) ;
#19569=B_SPLINE_CURVE_WITH_KNOTS ( 'NONE', 3,
 ( #6501, #15250, #8945, #24069, #9076, #4330, #22025, #17277 ),
 .UNSPECIFIED., .F., .F.,
 ( 4, 2, 2, 4 ),
 ( 2.193594746808674791E-16, 0.002761568181852864200, 0.005523136363705508957, 0.01104627272741079240 ),
 .UNSPECIFIED. ) ;
#19578=VERTEX_POINT ( 'NONE', #8023 ) ;
#19581=( BOUNDED_SURFACE ( )  B_SPLINE_SURFACE ( 3, 1, ( 
 ( #2362, #19641 ),
 ( #6852, #10882 ),
 ( #19939, #9011 ),
 ( #8715, #17771 ) ),
 .UNSPECIFIED., .F., .F., .F. ) 
 B_SPLINE_SURFACE_WITH_KNOTS ( ( 4, 4 ),
 ( 2, 2 ),
 ( 0.000000000000000000, 1.000000000000000000 ),
 ( 0.000000000000000000, 1.000000000000000000 ),
 .UNSPECIFIED. ) 
 GEOMETRIC_REPRESENTATION_ITEM ( )  RATIONAL_B_SPLINE_SURFACE ( (
 ( 1.000000000000000000, 1.000000000000000000),
 ( 0.7789835883360576307, 0.9689951854195403280),
 ( 0.7789835883360576307, 0.9689951854195403280),
 ( 1.000000000000000000, 1.000000000000000000) ) ) 
 REPRESENTATION_ITEM ( '' )  SURFACE ( )  );
#19582=CARTESIAN_POINT ( 'NONE',  ( -25.21435515916044423, -16.39063784838720395, 30.48034229288656505 ) ) ;
#19588=CARTESIAN_POINT ( 'NONE',  ( -1.045287976400362417, -44.00138577190658395, -12.68782741917276446 ) ) ;
#19590=CARTESIAN_POINT ( 'NONE',  ( -28.13707043255157103, 21.52861750560949972, 7.802116958608778852 ) ) ;
#19592=CARTESIAN_POINT ( 'NONE',  ( -55.24198130335446422, -0.008310594958150379491, -0.004163123460805868634 ) ) ;
#19594=CARTESIAN_POINT ( 'NONE',  ( -1.048171036023500369, -27.73816396939538009, 36.44209502233739073 ) ) ;
#19600=ORIENTED_EDGE ( 'NONE', *, *, #4676, .F. ) ;
#19601=ORIENTED_EDGE ( 'NONE', *, *, #1306, .T. ) ;
#19612=CARTESIAN_POINT ( 'NONE',  ( -55.24271866751342941, 0.008488649505346579707, -0.004256484107793386679 ) ) ;
#19615=EDGE_CURVE ( 'NONE', #13110, #15665, #1365, .T. ) ;
#19617=CARTESIAN_POINT ( 'NONE',  ( -21.81686047589431965, 5.181745222995449929, -38.17230180719251820 ) ) ;
#19618=EDGE_CURVE ( 'NONE', #10231, #2725, #18182, .T. ) ;
#19623=CARTESIAN_POINT ( 'NONE',  ( -20.47566262905010603, 10.72601569609896366, -27.87687924095551750 ) ) ;
#19624=CARTESIAN_POINT ( 'NONE',  ( -1.259920593601971950, -43.01175804832021043, -16.33409644610535594 ) ) ;
#19625=CARTESIAN_POINT ( 'NONE',  ( -1.539760825549691958, 35.94320866319490193, -29.16712717142773315 ) ) ;
#19627=CARTESIAN_POINT ( 'NONE',  ( -55.24390624410018802, 0.001811362924359719581, 0.01027195578987765215 ) ) ;
#19629=CARTESIAN_POINT ( 'NONE',  ( -1.048994561756799060, -26.29622118251707619, -37.49601524795400564 ) ) ;
#19631=ORIENTED_EDGE ( 'NONE', *, *, #22480, .T. ) ;
#19632=LINE ( 'NONE', #22239, #1103 ) ;
#19633=B_SPLINE_CURVE_WITH_KNOTS ( 'NONE', 3,
 ( #14174, #21085, #16060, #3256, #18652, #24860 ),
 .UNSPECIFIED., .F., .F.,
 ( 4, 2, 4 ),
 ( 3.467809420226820728E-16, 0.003576372551511154425, 0.007152745103021954098 ),
 .UNSPECIFIED. ) ;
#19641=CARTESIAN_POINT ( 'NONE',  ( -1.583189561560253589, -38.94740041318312507, -25.21827308671218049 ) ) ;
#19655=ADVANCED_FACE ( 'NONE', ( #13013 ), #13649, .F. ) ;
#19670=CARTESIAN_POINT ( 'NONE',  ( -25.21435515916043357, -15.02493970636125198, 31.17620025257602379 ) ) ;
#19672=CARTESIAN_POINT ( 'NONE',  ( -1.323830074806774837, -35.86387698262934265, -28.92190886481852274 ) ) ;
#19674=ORIENTED_EDGE ( 'NONE', *, *, #4502, .F. ) ;
#19682=DIRECTION ( 'NONE',  ( -0.7563875759206389882, 0.03500244528123006016, 0.6531865459554675457 ) ) ;
#19683=CARTESIAN_POINT ( 'NONE',  ( -20.21097721650786738, -24.14932365326965069, -17.13687097598128517 ) ) ;
#19687=EDGE_LOOP ( 'NONE', ( #23848, #13259, #4998, #14522 ) ) ;
#19691=CARTESIAN_POINT ( 'NONE',  ( -20.90916690077966322, 35.64494649500682755, -17.17795951644668762 ) ) ;
#19693=DIRECTION ( 'NONE',  ( 1.000000000000000000, -6.938893903907226837E-18, 1.734723475976806709E-18 ) ) ;
#19701=( BOUNDED_SURFACE ( )  B_SPLINE_SURFACE ( 3, 1, ( 
 ( #24453, #13773 ),
 ( #11338, #9610 ),
 ( #396, #7041 ),
 ( #24607, #16078 ) ),
 .UNSPECIFIED., .F., .F., .F. ) 
 B_SPLINE_SURFACE_WITH_KNOTS ( ( 4, 4 ),
 ( 2, 2 ),
 ( 0.000000000000000000, 1.000000000000000000 ),
 ( 0.000000000000000000, 1.000000000000000000 ),
 .UNSPECIFIED. ) 
 GEOMETRIC_REPRESENTATION_ITEM ( )  RATIONAL_B_SPLINE_SURFACE ( (
 ( 1.000000000000000000, 1.000000000000000000),
 ( 0.9934239774497837239, 0.8357310067453919133),
 ( 0.9934239774497837239, 0.8357310067453919133),
 ( 1.000000000000000000, 1.000000000000000000) ) ) 
 REPRESENTATION_ITEM ( '' )  SURFACE ( )  );
#19702=CARTESIAN_POINT ( 'NONE',  ( -19.53423201713129842, 1.355459634611817431E-16, -3.388649086529543578E-17 ) ) ;
#19704=B_SPLINE_CURVE_WITH_KNOTS ( 'NONE', 3,
 ( #15278, #21919, #24373, #11126, #22358, #2177, #4358, #10986, #19746, #8971 ),
 .UNSPECIFIED., .F., .F.,
 ( 4, 2, 2, 2, 4 ),
 ( 2.884421207865725401E-16, 0.0003346187017559067080, 0.0006692374035115243678, 0.001003856105267142028, 0.001338474807022759687 ),
 .UNSPECIFIED. ) ;
#19705=B_SPLINE_CURVE_WITH_KNOTS ( 'NONE', 3,
 ( #8306, #18813, #21103, #10469 ),
 .UNSPECIFIED., .F., .F.,
 ( 4, 4 ),
 ( 1.892757412642747523E-16, 0.001982023823822947652 ),
 .UNSPECIFIED. ) ;
#19707=CARTESIAN_POINT ( 'NONE',  ( -10.86508079875781618, 50.67624451685635734, 6.877801422380954044 ) ) ;
#19716=CARTESIAN_POINT ( 'NONE',  ( -2.904412668506665351, 17.42365698954698061, -44.35433137608945486 ) ) ;
#19718=VERTEX_POINT ( 'NONE', #24394 ) ;
#19720=CARTESIAN_POINT ( 'NONE',  ( -1.323830074806773061, -12.01461446423233781, -44.47857376182264488 ) ) ;
#19724=FACE_OUTER_BOUND ( 'NONE', #16894, .T. ) ;
#19727=CARTESIAN_POINT ( 'NONE',  ( -20.20612092514784663, 18.30568145913877132, 23.26073121129616439 ) ) ;
#19729=DIRECTION ( 'NONE',  ( 1.000000000000000000, -6.938893903907226837E-18, 1.734723475976806709E-18 ) ) ;
#19732=ORIENTED_EDGE ( 'NONE', *, *, #23843, .F. ) ;
#19739=ORIENTED_EDGE ( 'NONE', *, *, #12808, .F. ) ;
#19745=B_SPLINE_CURVE_WITH_KNOTS ( 'NONE', 3,
 ( #11895, #20663, #18080, #377, #19808, #11043, #19961, #2680, #24021, #13476 ),
 .UNSPECIFIED., .F., .F.,
 ( 4, 2, 2, 2, 4 ),
 ( 2.884421207865724908E-16, 0.0003346187017559065996, 0.0006692374035115252352, 0.001003856105267143979, 0.001338474807022762723 ),
 .UNSPECIFIED. ) ;
#19746=CARTESIAN_POINT ( 'NONE',  ( -1.539763995773684835, -46.22267697748605997, -2.469814354917328370 ) ) ;
#19747=ADVANCED_FACE ( 'NONE', ( #7128 ), #7023, .F. ) ;
#19750=CARTESIAN_POINT ( 'NONE',  ( -16.86833981943425442, 30.57013526701963713, 31.95666732167528323 ) ) ;
#19760=CARTESIAN_POINT ( 'NONE',  ( -1.463510566862824991, -29.09194585123808707, 35.90603835816536815 ) ) ;
#19761=CARTESIAN_POINT ( 'NONE',  ( -55.24271866751342941, 0.008433070970614320663, 0.004365563123939306990 ) ) ;
#19762=CARTESIAN_POINT ( 'NONE',  ( -20.24399999263414429, 10.36954246768245547, -27.76448601145544259 ) ) ;
#19763=CARTESIAN_POINT ( 'NONE',  ( -2.911734481061404534, -30.23325065583388138, -36.84482841982639911 ) ) ;
#19765=CARTESIAN_POINT ( 'NONE',  ( -55.25297051322618813, 0.01306918787467309905, 0.007247191603128975632 ) ) ;
#19766=ORIENTED_EDGE ( 'NONE', *, *, #7137, .T. ) ;
#19768=CARTESIAN_POINT ( 'NONE',  ( -1.050231094221210526, -27.12595454131532691, -36.90262059116457038 ) ) ;
#19773=CARTESIAN_POINT ( 'NONE',  ( -25.21435515916043713, -31.17620025257576799, 15.02493970636179377 ) ) ;
#19774=VERTEX_POINT ( 'NONE', #481 ) ;
#19779=CIRCLE ( 'NONE', #1847, 34.60786435723138510 ) ;
#19782=CARTESIAN_POINT ( 'NONE',  ( -1.044556982611274387, -37.98985389331830476, -25.56989963842190150 ) ) ;
#19787=B_SPLINE_CURVE_WITH_KNOTS ( 'NONE', 3,
 ( #6299, #12894, #11033, #6435, #24008, #17497, #26283 ),
 .UNSPECIFIED., .F., .F.,
 ( 4, 3, 4 ),
 ( 1.430489624538199204E-17, 0.009512539173626433087, 0.02506242213020844906 ),
 .UNSPECIFIED. ) ;
#19803=VECTOR ( 'NONE', #23732, 1000.000000000000000 ) ;
#19806=CARTESIAN_POINT ( 'NONE',  ( -9.156249394959713683, -24.29252099376526530, -48.78605533024730789 ) ) ;
#19808=CARTESIAN_POINT ( 'NONE',  ( -1.155001620486253877, 45.85729774065937647, 2.068551059060488750 ) ) ;
#19814=B_SPLINE_CURVE_WITH_KNOTS ( 'NONE', 3,
 ( #14836, #1598, #28210, #17269, #25787, #6083, #13518, #2429 ),
 .UNSPECIFIED., .F., .F.,
 ( 4, 2, 2, 4 ),
 ( 0.000000000000000000, 0.002761524886576653681, 0.005523049773153307362, 0.01104609954630661472 ),
 .UNSPECIFIED. ) ;
#19817=EDGE_CURVE ( 'NONE', #9726, #12126, #26091, .T. ) ;
#19818=CARTESIAN_POINT ( 'NONE',  ( -4.473127245936431073, 49.22197550883368677, 3.196405119333978639 ) ) ;
#19828=DIRECTION ( 'NONE',  ( 0.000000000000000000, 5.223019709708233256E-21, -1.000000000000000000 ) ) ;
#19829=LINE ( 'NONE', #26311, #13441 ) ;
#19832=CIRCLE ( 'NONE', #10651, 53.53553390275978785 ) ;
#19834=VERTEX_POINT ( 'NONE', #14441 ) ;
#19842=CARTESIAN_POINT ( 'NONE',  ( -20.20700224038492721, 0.9908225410478516126, -29.58392382092673145 ) ) ;
#19844=CARTESIAN_POINT ( 'NONE',  ( -55.24271866751342941, 0.009369360294294836952, -0.001545935011626992572 ) ) ;
#19850=EDGE_CURVE ( 'NONE', #23016, #12412, #20770, .T. ) ;
#19852=CARTESIAN_POINT ( 'NONE',  ( -7.078251931573406708, 26.33626633876224332, -44.92740138729174504 ) ) ;
#19857=ORIENTED_EDGE ( 'NONE', *, *, #253, .T. ) ;
#19862=B_SPLINE_CURVE_WITH_KNOTS ( 'NONE', 3,
 ( #21253, #1246, #18958, #7609, #25727, #27578 ),
 .UNSPECIFIED., .F., .F.,
 ( 4, 2, 4 ),
 ( 1.536381426628689196E-16, 0.003570751334075638293, 0.007141502668151123064 ),
 .UNSPECIFIED. ) ;
#19864=CARTESIAN_POINT ( 'NONE',  ( -20.20700224038492721, -28.44216453106531617, 8.199606986804630182 ) ) ;
#19865=CARTESIAN_POINT ( 'NONE',  ( -2.265401668238147259, 43.82493763960408728, 17.02144111536834004 ) ) ;
#19867=CARTESIAN_POINT ( 'NONE',  ( -1.259972190295307604, -25.19627397134270197, 38.49631882650675152 ) ) ;
#19870=CARTESIAN_POINT ( 'NONE',  ( -55.24390624410018802, -0.007503127514281482044, 0.007245494385991411469 ) ) ;
#19875=CARTESIAN_POINT ( 'NONE',  ( -20.57838717382308147, 18.89542499756533545, 23.26537097894084383 ) ) ;
#19880=CARTESIAN_POINT ( 'NONE',  ( -20.20700224038492721, -24.51628800869059432, -16.58740185276701951 ) ) ;
#19882=CARTESIAN_POINT ( 'NONE',  ( -21.41430102051752016, 28.68859753627394582, -11.22990201072285466 ) ) ;
#19887=EDGE_LOOP ( 'NONE', ( #5253, #16825, #6667, #15032 ) ) ;
#19888=CARTESIAN_POINT ( 'NONE',  ( -1.259972190295307382, 44.39825172539712383, 12.06706380853646188 ) ) ;
#19889=FACE_OUTER_BOUND ( 'NONE', #23281, .T. ) ;
#19893=ORIENTED_EDGE ( 'NONE', *, *, #3422, .F. ) ;
#19899=CARTESIAN_POINT ( 'NONE',  ( -1.045287976400379737, -25.66401692420040703, -37.92705037016734337 ) ) ;
#19901=CARTESIAN_POINT ( 'NONE',  ( -22.34422965417125795, 33.39267070835848017, 17.95715691811010828 ) ) ;
#19902=CARTESIAN_POINT ( 'NONE',  ( -25.21435515916043713, 23.92354251275973809, 25.00736669480994934 ) ) ;
#19904=CARTESIAN_POINT ( 'NONE',  ( -1.259972190295312267, 12.06706380853692551, -44.39825172539698883 ) ) ;
#19910=VERTEX_POINT ( 'NONE', #2736 ) ;
#19913=CARTESIAN_POINT ( 'NONE',  ( -20.20700224038492010, -0.9908225410480588913, -29.58392382092672435 ) ) ;
#19922=ORIENTED_EDGE ( 'NONE', *, *, #287, .T. ) ;
#19932=ORIENTED_EDGE ( 'NONE', *, *, #18354, .T. ) ;
#19938=CARTESIAN_POINT ( 'NONE',  ( -24.53239521893646824, 3.868435622621471115, -33.71193723315172264 ) ) ;
#19939=CARTESIAN_POINT ( 'NONE',  ( -55.25297051322618813, -0.01019003092403672657, 0.01093108995495161231 ) ) ;
#19944=CARTESIAN_POINT ( 'NONE',  ( -25.21435515916043002, -4.655591116594591128, -34.29329011225954105 ) ) ;
#19946=ADVANCED_FACE ( 'NONE', ( #433 ), #1143, .F. ) ;
#19959=CARTESIAN_POINT ( 'NONE',  ( -55.25719721206881729, -0.004044147484874425005, 0.01041086141212271658 ) ) ;
#19961=CARTESIAN_POINT ( 'NONE',  ( -1.323830074806771506, 46.01435746200691312, 2.318057800980871885 ) ) ;
#19962=ORIENTED_EDGE ( 'NONE', *, *, #3484, .T. ) ;
#19966=CARTESIAN_POINT ( 'NONE',  ( -7.078251931573400491, 11.16394717458747898, 50.86685171665398997 ) ) ;
#19969=CARTESIAN_POINT ( 'NONE',  ( -8.786685647604896232, 9.545808661481343549, 52.67761315067276229 ) ) ;
#19976=ORIENTED_EDGE ( 'NONE', *, *, #99, .T. ) ;
#19977=ORIENTED_EDGE ( 'NONE', *, *, #24451, .F. ) ;
#19981=EDGE_CURVE ( 'NONE', #14674, #27787, #7203, .T. ) ;
#19982=CARTESIAN_POINT ( 'NONE',  ( -21.41430102051744200, -1.815007301162189446, -30.75470819672111134 ) ) ;
#19983=CARTESIAN_POINT ( 'NONE',  ( -1.056502255334264895, 36.75727364034733569, -27.33667001641181926 ) ) ;
#19984=CARTESIAN_POINT ( 'NONE',  ( -20.20700224038492721, -10.08426345511609235, -27.82980252387815767 ) ) ;
#19989=CARTESIAN_POINT ( 'NONE',  ( 14.74894986621300319, -1.023413983156987147E-16, 2.558534957892467869E-17 ) ) ;
#19992=ORIENTED_EDGE ( 'NONE', *, *, #3645, .F. ) ;
#19996=CARTESIAN_POINT ( 'NONE',  ( -1.056502255334264895, -14.64009593116132457, -43.40574022158768486 ) ) ;
#20003=ORIENTED_EDGE ( 'NONE', *, *, #14754, .F. ) ;
#20005=CARTESIAN_POINT ( 'NONE',  ( -1.619063947482197729, 43.26576862488456499, 16.67502769180516964 ) ) ;
#20009=DIRECTION ( 'NONE',  ( -0.7637818620346800147, -0.5345501402766327237, -0.3617919495470695579 ) ) ;
#20018=CARTESIAN_POINT ( 'NONE',  ( -20.57838717382308147, 16.28767523336121315, -25.16001208503110931 ) ) ;
#20022=CARTESIAN_POINT ( 'NONE',  ( -55.24340739397742084, 0.002421372372454598174, 0.009842732675352095298 ) ) ;
#20024=ORIENTED_EDGE ( 'NONE', *, *, #17672, .T. ) ;
#20026=CARTESIAN_POINT ( 'NONE',  ( -7.078251931573406708, -26.33626633876190937, 44.92740138729193689 ) ) ;
#20028=ORIENTED_EDGE ( 'NONE', *, *, #14289, .T. ) ;
#20031=CARTESIAN_POINT ( 'NONE',  ( -1.050229599974492833, 37.20249516760172526, -26.71319688967646755 ) ) ;
#20034=CARTESIAN_POINT ( 'NONE',  ( -1.113548883309547266, -25.34012683631582519, -38.22628252420800976 ) ) ;
#20045=VERTEX_POINT ( 'NONE', #17525 ) ;
#20050=FACE_OUTER_BOUND ( 'NONE', #17853, .T. ) ;
#20069=CARTESIAN_POINT ( 'NONE',  ( -1.239374126674604337, -25.08410696974215170, 38.61989855450968179 ) ) ;
#20070=CARTESIAN_POINT ( 'NONE',  ( -4.178947244162637631, 47.46809051147737080, 11.88256963646688824 ) ) ;
#20077=CARTESIAN_POINT ( 'NONE',  ( -20.24399999263415850, -29.60996018918693551, -1.282322917263360340 ) ) ;
#20078=FACE_OUTER_BOUND ( 'NONE', #5109, .T. ) ;
#20088=VERTEX_POINT ( 'NONE', #9043 ) ;
#20090=CARTESIAN_POINT ( 'NONE',  ( -20.57838717382308147, -28.96176188950224528, -7.715628353033566533 ) ) ;
#20095=ORIENTED_EDGE ( 'NONE', *, *, #17887, .T. ) ;
#20097=CARTESIAN_POINT ( 'NONE',  ( -1.019300379054419725, -16.06793277092022976, -42.90269154183422984 ) ) ;
#20102=EDGE_CURVE ( 'NONE', #22079, #3709, #17800, .T. ) ;
#20104=B_SPLINE_CURVE_WITH_KNOTS ( 'NONE', 3,
 ( #9291, #18048, #23758, #644, #5529, #10010, #7716 ),
 .UNSPECIFIED., .F., .F.,
 ( 4, 3, 4 ),
 ( 8.845388854693243284E-18, 0.009512539173626379310, 0.02506242213020843518 ),
 .UNSPECIFIED. ) ;
#20106=CARTESIAN_POINT ( 'NONE',  ( -1.058197053496171325, 15.81317659443684143, -42.99116279335158453 ) ) ;
#20109=EDGE_CURVE ( 'NONE', #23222, #27304, #26393, .T. ) ;
#20112=DIRECTION ( 'NONE',  ( 0.7563875759206388771, 0.1685564395263429993, 0.6320336713238481341 ) ) ;
#20116=CARTESIAN_POINT ( 'NONE',  ( -22.34422965417106965, 37.57019010019570260, -5.100074259622762618 ) ) ;
#20118=CARTESIAN_POINT ( 'NONE',  ( -1.044557008772710516, -37.98985164565307571, 25.56990300677022177 ) ) ;
#20119=CARTESIAN_POINT ( 'NONE',  ( -2.265401668238148591, 46.93990709177546705, 2.645701981445969686 ) ) ;
#20121=CARTESIAN_POINT ( 'NONE',  ( -20.20700224038492721, 29.58392382092673500, -0.9908225410479557516 ) ) ;
#20123=EDGE_LOOP ( 'NONE', ( #24087, #11739, #7950, #25008 ) ) ;
#20127=CARTESIAN_POINT ( 'NONE',  ( -55.24271866751342941, 0.009388511352198142604, 0.001425019990782173561 ) ) ;
#20135=ORIENTED_EDGE ( 'NONE', *, *, #12566, .F. ) ;
#20138=CARTESIAN_POINT ( 'NONE',  ( -28.13707043255157103, -22.00298671236744497, -6.342158660426917116 ) ) ;
#20145=CARTESIAN_POINT ( 'NONE',  ( -25.21435515916043713, 25.00736669481056751, 23.92354251275909505 ) ) ;
#20148=VERTEX_POINT ( 'NONE', #19412 ) ;
#20158=CARTESIAN_POINT ( 'NONE',  ( -20.21097721712958517, -9.464413111084555297, 28.05863618200118381 ) ) ;
#20167=CARTESIAN_POINT ( 'NONE',  ( -1.046935749539997573, 45.77872888003167162, 1.275486069320633353 ) ) ;
#20168=ORIENTED_EDGE ( 'NONE', *, *, #9707, .T. ) ;
#20175=CARTESIAN_POINT ( 'NONE',  ( -1.031422197589711987, 1.530725436378101989, 45.78027046666441180 ) ) ;
#20189=CARTESIAN_POINT ( 'NONE',  ( -55.24271866751342941, -0.004365563123939050251, 0.008433070970613824532 ) ) ;
#20190=CARTESIAN_POINT ( 'NONE',  ( -25.21435515916043713, -30.48034229288627017, 16.39063784838775462 ) ) ;
#20197=CARTESIAN_POINT ( 'NONE',  ( -18.41936578851710493, -5.707900577127883679, 42.05131332928132082 ) ) ;
#20204=FACE_OUTER_BOUND ( 'NONE', #13262, .T. ) ;
#20215=CARTESIAN_POINT ( 'NONE',  ( -1.045287976400365970, -43.05558670614224326, 15.59869763335140469 ) ) ;
#20217=CARTESIAN_POINT ( 'NONE',  ( -1.619063947482197729, -38.92136151114925724, -25.20140673341360227 ) ) ;
#20218=CARTESIAN_POINT ( 'NONE',  ( -22.23226125620929139, 2.179935373562892131, 31.55376588768475798 ) ) ;
#20226=CARTESIAN_POINT ( 'NONE',  ( -1.323439229708149867, -16.42345129173367013, -43.04565903621277556 ) ) ;
#20230=CARTESIAN_POINT ( 'NONE',  ( -8.786685647604896232, 25.35688121747570278, 47.14957014837326454 ) ) ;
#20232=VERTEX_POINT ( 'NONE', #3512 ) ;
#20233=CARTESIAN_POINT ( 'NONE',  ( -55.24390624410018802, 0.009374879212971231821, -0.004572280736701976080 ) ) ;
#20243=CARTESIAN_POINT ( 'NONE',  ( -20.57838717382308147, -28.96176188950224528, -7.715628353033566533 ) ) ;
#20249=CARTESIAN_POINT ( 'NONE',  ( -8.786685647604890903, -37.00619870957905277, 38.68584556812340480 ) ) ;
#20258=AXIS2_PLACEMENT_3D ( 'NONE', #23695, #5838, #14308 ) ;
#20268=CARTESIAN_POINT ( 'NONE',  ( -1.031422197589716205, -36.13727897780147202, -28.14735071801731792 ) ) ;
#20286=LINE ( 'NONE', #9073, #21627 ) ;
#20289=CARTESIAN_POINT ( 'NONE',  ( 0.000000000000000000, 0.000000000000000000, 0.000000000000000000 ) ) ;
#20291=CARTESIAN_POINT ( 'NONE',  ( -21.81686047589426636, 27.83628745321488296, 26.62923599424938459 ) ) ;
#20296=CARTESIAN_POINT ( 'NONE',  ( -1.031422197589711764, -45.78027046666444733, -1.530725436377303073 ) ) ;
#20303=EDGE_CURVE ( 'NONE', #21873, #19211, #2020, .T. ) ;
#20305=CARTESIAN_POINT ( 'NONE',  ( -20.47566262905010248, 16.24827521404687403, 25.06314747784817243 ) ) ;
#20307=CARTESIAN_POINT ( 'NONE',  ( -1.031422197589716205, 44.01264471863865424, 12.69107518035457005 ) ) ;
#20310=CARTESIAN_POINT ( 'NONE',  ( -8.786685647604890903, -53.04920435127188938, -7.199674155858766689 ) ) ;
#20326=CARTESIAN_POINT ( 'NONE',  ( -1.619063947482197729, 43.26576862488456499, 16.67502769180516964 ) ) ;
#20329=( BOUNDED_SURFACE ( )  B_SPLINE_SURFACE ( 3, 1, ( 
 ( #20673, #966 ),
 ( #9902, #5571 ),
 ( #9751, #18524 ),
 ( #14336, #16361 ) ),
 .UNSPECIFIED., .F., .F., .F. ) 
 B_SPLINE_SURFACE_WITH_KNOTS ( ( 4, 4 ),
 ( 2, 2 ),
 ( 0.000000000000000000, 1.000000000000000000 ),
 ( 0.000000000000000000, 1.000000000000000000 ),
 .UNSPECIFIED. ) 
 GEOMETRIC_REPRESENTATION_ITEM ( )  RATIONAL_B_SPLINE_SURFACE ( (
 ( 1.000000000000000000, 1.000000000000000000),
 ( 0.9934239774497838349, 0.8357310067453913582),
 ( 0.9934239774497838349, 0.8357310067453913582),
 ( 1.000000000000000000, 1.000000000000000000) ) ) 
 REPRESENTATION_ITEM ( '' )  SURFACE ( )  );
#20330=CARTESIAN_POINT ( 'NONE',  ( -1.619063947482197729, -43.26576862488421682, 16.67502769180607203 ) ) ;
#20331=CARTESIAN_POINT ( 'NONE',  ( -1.583189561560253589, -2.490696082060195327, -46.33203782964460515 ) ) ;
#20332=DIRECTION ( 'NONE',  ( 0.000000000000000000, 5.223019709707975211E-21, -1.000000000000000000 ) ) ;
#20334=CARTESIAN_POINT ( 'NONE',  ( -4.473127245936434626, 47.80062405537817938, 12.17046501147466842 ) ) ;
#20336=EDGE_CURVE ( 'NONE', #12735, #21937, #10310, .T. ) ;
#20339=CARTESIAN_POINT ( 'NONE',  ( -55.24198130335446422, -0.001516807524707838167, 0.009170435128245089246 ) ) ;
#20342=CARTESIAN_POINT ( 'NONE',  ( -1.031422197589711764, 15.60268798220637798, -43.06660437151313658 ) ) ;
#20344=DIRECTION ( 'NONE',  ( 1.000000000000000000, -6.938893903907226837E-18, 1.734723475976806709E-18 ) ) ;
#20348=ORIENTED_EDGE ( 'NONE', *, *, #16929, .F. ) ;
#20358=CARTESIAN_POINT ( 'NONE',  ( -28.41354790283022069, -22.41474081377996441, 5.969609727608259142 ) ) ;
#20363=CARTESIAN_POINT ( 'NONE',  ( -1.050230346682680560, 26.92058491724867153, -37.05182464821992028 ) ) ;
#20367=ORIENTED_EDGE ( 'NONE', *, *, #14089, .F. ) ;
#20378=CARTESIAN_POINT ( 'NONE',  ( -18.41936578851705519, -42.05131332928132082, -5.707900577128024011 ) ) ;
#20383=CARTESIAN_POINT ( 'NONE',  ( -1.113427685307007531, -16.03057832159182539, -42.96952363574826705 ) ) ;
#20406=FACE_OUTER_BOUND ( 'NONE', #26041, .T. ) ;
#20412=CARTESIAN_POINT ( 'NONE',  ( -1.056502255334265339, -26.51074901220530222, -37.35734037467625512 ) ) ;
#20414=ORIENTED_EDGE ( 'NONE', *, *, #8933, .T. ) ;
#20419=( BOUNDED_SURFACE ( )  B_SPLINE_SURFACE ( 3, 1, ( 
 ( #11558, #3075 ),
 ( #11848, #20334 ),
 ( #10258, #25651 ),
 ( #22371, #2634 ) ),
 .UNSPECIFIED., .F., .F., .F. ) 
 B_SPLINE_SURFACE_WITH_KNOTS ( ( 4, 4 ),
 ( 2, 2 ),
 ( 0.000000000000000000, 1.000000000000000000 ),
 ( 0.000000000000000000, 1.000000000000000000 ),
 .UNSPECIFIED. ) 
 GEOMETRIC_REPRESENTATION_ITEM ( )  RATIONAL_B_SPLINE_SURFACE ( (
 ( 1.000000000000000000, 1.000000000000000000),
 ( 0.7789835883360576307, 0.9689951854195403280),
 ( 0.7789835883360576307, 0.9689951854195403280),
 ( 1.000000000000000000, 1.000000000000000000) ) ) 
 REPRESENTATION_ITEM ( '' )  SURFACE ( )  );
#20427=CARTESIAN_POINT ( 'NONE',  ( -1.539763995773685723, 11.93465967526358185, 44.72359274866469292 ) ) ;
#20431=ORIENTED_EDGE ( 'NONE', *, *, #2162, .F. ) ;
#20432=CARTESIAN_POINT ( 'NONE',  ( -9.156249394959713683, -38.17928057392020236, -38.89149400288393821 ) ) ;
#20433=CARTESIAN_POINT ( 'NONE',  ( -1.031422197589711987, -44.01264471863856187, -12.69107518035484361 ) ) ;
#20434=EDGE_CURVE ( 'NONE', #6842, #21998, #8249, .T. ) ;
#20438=CARTESIAN_POINT ( 'NONE',  ( -18.41936578851709783, 18.42310649277627022, -38.22933728004698395 ) ) ;
#20444=CARTESIAN_POINT ( 'NONE',  ( -1.050230346682684113, -43.55729751025872787, -14.15335421912565828 ) ) ;
#20447=CARTESIAN_POINT ( 'NONE',  ( -20.57838717382308147, 27.96569011373101077, 10.78122205916971055 ) ) ;
#20452=CARTESIAN_POINT ( 'NONE',  ( -4.780792508754315051, -37.74278713234418348, -32.07473752860764904 ) ) ;
#20457=VERTEX_POINT ( 'NONE', #22361 ) ;
#20458=B_SPLINE_CURVE_WITH_KNOTS ( 'NONE', 3,
 ( #445, #20305, #24658, #9785, #27321, #7636 ),
 .UNSPECIFIED., .F., .F.,
 ( 4, 2, 4 ),
 ( 0.000000000000000000, 0.0004335151646191536890, 0.0008670303292383073780 ),
 .UNSPECIFIED. ) ;
#20463=CARTESIAN_POINT ( 'NONE',  ( -28.13707043255157103, 0.7675454997510209321, 22.88591869784690047 ) ) ;
#20477=EDGE_CURVE ( 'NONE', #27511, #13048, #4766, .T. ) ;
#20480=CARTESIAN_POINT ( 'NONE',  ( -1.050230347699842692, 5.964912479342754695E-15, -45.79907861674080749 ) ) ;
#20482=CARTESIAN_POINT ( 'NONE',  ( -1.045287976400362417, -1.530335034933495653, 45.76855895860946788 ) ) ;
#20488=ORIENTED_EDGE ( 'NONE', *, *, #11370, .F. ) ;
#20491=EDGE_LOOP ( 'NONE', ( #1207, #9209 ) ) ;
#20495=EDGE_CURVE ( 'NONE', #19910, #9180, #1348, .T. ) ;
#20509=EDGE_LOOP ( 'NONE', ( #8706, #10586, #15553, #22820 ) ) ;
#20513=CARTESIAN_POINT ( 'NONE',  ( -1.045287976400383290, -36.12803364096628655, -28.14015102489793918 ) ) ;
#20515=CARTESIAN_POINT ( 'NONE',  ( -9.156249394959706578, 24.29252099376491358, -48.78605533024748553 ) ) ;
#20516=VERTEX_POINT ( 'NONE', #17444 ) ;
#20519=CARTESIAN_POINT ( 'NONE',  ( -7.078251931573400491, 47.71415099571833451, 20.86696228105175166 ) ) ;
#20520=ORIENTED_EDGE ( 'NONE', *, *, #16287, .T. ) ;
#20521=CARTESIAN_POINT ( 'NONE',  ( -4.473127245936431073, -45.82513704981557368, -18.25038884639852199 ) ) ;
#20530=EDGE_CURVE ( 'NONE', #23146, #6702, #21592, .T. ) ;
#20533=CARTESIAN_POINT ( 'NONE',  ( -20.20898977204109670, 0.6607022527616891461, -29.59696883073212348 ) ) ;
#20535=EDGE_CURVE ( 'NONE', #11485, #24558, #3391, .T. ) ;
#20547=ORIENTED_EDGE ( 'NONE', *, *, #1745, .T. ) ;
#20549=ADVANCED_FACE ( 'NONE', ( #22659 ), #19537, .F. ) ;
#20557=ORIENTED_EDGE ( 'NONE', *, *, #19850, .F. ) ;
#20562=CARTESIAN_POINT ( 'NONE',  ( -28.41354790283022069, -5.969609727608182759, -22.41474081377998218 ) ) ;
#20567=CARTESIAN_POINT ( 'NONE',  ( -8.786685647604885574, 6.096987947571466530E-17, -1.524246986892866633E-17 ) ) ;
#20583=ORIENTED_EDGE ( 'NONE', *, *, #21634, .T. ) ;
#20584=EDGE_LOOP ( 'NONE', ( #25932, #16370 ) ) ;
#20593=CARTESIAN_POINT ( 'NONE',  ( -20.20700224038492721, -24.51628800869035274, 16.58740185276737122 ) ) ;
#20596=( BOUNDED_SURFACE ( )  B_SPLINE_SURFACE ( 3, 1, ( 
 ( #22013, #4318 ),
 ( #6916, #15823 ),
 ( #24476, #19996 ),
 ( #24632, #2275 ) ),
 .UNSPECIFIED., .F., .F., .F. ) 
 B_SPLINE_SURFACE_WITH_KNOTS ( ( 4, 4 ),
 ( 2, 2 ),
 ( 0.000000000000000000, 1.000000000000000000 ),
 ( 0.000000000000000000, 1.000000000000000000 ),
 .UNSPECIFIED. ) 
 GEOMETRIC_REPRESENTATION_ITEM ( )  RATIONAL_B_SPLINE_SURFACE ( (
 ( 1.000000000000000000, 1.000000000000000000),
 ( 0.9593753223639863714, 0.9995975284513187731),
 ( 0.9593753223639863714, 0.9995975284513187731),
 ( 1.000000000000000000, 1.000000000000000000) ) ) 
 REPRESENTATION_ITEM ( '' )  SURFACE ( )  );
#20597=CARTESIAN_POINT ( 'NONE',  ( -55.24198130335446422, -0.008252882783648586573, -0.004276389980780055493 ) ) ;
#20600=ORIENTED_EDGE ( 'NONE', *, *, #19473, .F. ) ;
#20607=CARTESIAN_POINT ( 'NONE',  ( -55.24271866751342941, 0.004365563123939763222, -0.008433070970614044842 ) ) ;
#20612=CARTESIAN_POINT ( 'NONE',  ( -1.019300379054419725, 45.76814864815091255, -2.023851374322835017 ) ) ;
#20614=EDGE_CURVE ( 'NONE', #23277, #21774, #16590, .T. ) ;
#20615=CARTESIAN_POINT ( 'NONE',  ( -20.57838717382308147, -27.96569011373078339, 10.78122205917029675 ) ) ;
#20620=CARTESIAN_POINT ( 'NONE',  ( -1.463510566862821882, -2.430838777909866355, 46.14841196428346848 ) ) ;
#20622=CARTESIAN_POINT ( 'NONE',  ( -1.031422197589716205, -1.530725436377772031, -45.78027046666443312 ) ) ;
#20632=EDGE_CURVE ( 'NONE', #4332, #26927, #18456, .T. ) ;
#20638=DIRECTION ( 'NONE',  ( 0.7563875759206387661, -0.6320336713238486892, 0.1685564395263406956 ) ) ;
#20660=ORIENTED_EDGE ( 'NONE', *, *, #13875, .F. ) ;
#20663=CARTESIAN_POINT ( 'NONE',  ( -1.044557008772710072, 45.76404748504490527, 1.643388457098048372 ) ) ;
#20668=CARTESIAN_POINT ( 'NONE',  ( -23.79248802219731118, 28.61009539422409631, 16.82188324679449565 ) ) ;
#20669=CARTESIAN_POINT ( 'NONE',  ( -1.619063947482201282, -44.80407745103776307, 11.94059994246206635 ) ) ;
#20671=VERTEX_POINT ( 'NONE', #19453 ) ;
#20673=CARTESIAN_POINT ( 'NONE',  ( -55.24271866751342941, -0.004256484107792932181, -0.008488649505346277865 ) ) ;
#20677=VERTEX_POINT ( 'NONE', #3774 ) ;
#20680=CARTESIAN_POINT ( 'NONE',  ( -9.156249394959706578, -48.32878616080991208, 25.18996226954667605 ) ) ;
#20694=CARTESIAN_POINT ( 'NONE',  ( -1.045287976400365970, 15.59869763335156101, 43.05558670614217931 ) ) ;
#20698=CIRCLE ( 'NONE', #5073, 53.53553390275978785 ) ;
#20705=AXIS2_PLACEMENT_3D ( 'NONE', #12325, #15321, #13035 ) ;
#20708=B_SPLINE_CURVE_WITH_KNOTS ( 'NONE', 3,
 ( #27444, #5872, #23295, #8045, #20962, #5576, #1118, #22873, #16514, #3133, #11910, #3417, #9762 ),
 .UNSPECIFIED., .F., .F.,
 ( 4, 3, 3, 3, 4 ),
 ( 6.938893903907227607E-18, 0.0007657099931970539480, 0.001531419946797919806, 0.002296279302920154267, 0.003061450627205759834 ),
 .UNSPECIFIED. ) ;
#20711=ORIENTED_EDGE ( 'NONE', *, *, #12316, .F. ) ;
#20721=CIRCLE ( 'NONE', #11067, 53.53553390275978785 ) ;
#20722=EDGE_CURVE ( 'NONE', #25788, #12126, #12547, .T. ) ;
#20725=VECTOR ( 'NONE', #24838, 999.9999999999998863 ) ;
#20726=ORIENTED_EDGE ( 'NONE', *, *, #21964, .T. ) ;
#20727=CARTESIAN_POINT ( 'NONE',  ( -25.21435515916042647, 25.00736669481023355, -23.92354251275945742 ) ) ;
#20745=VECTOR ( 'NONE', #4730, 999.9999999999998863 ) ;
#20755=CARTESIAN_POINT ( 'NONE',  ( -1.239374126674604337, 45.98822239537608425, -2.406737988131283146 ) ) ;
#20759=ADVANCED_FACE ( 'NONE', ( #1743 ), #22497, .F. ) ;
#20760=CARTESIAN_POINT ( 'NONE',  ( -25.21435515916043357, 16.39063784838743132, -30.48034229288645136 ) ) ;
#20766=CARTESIAN_POINT ( 'NONE',  ( -1.058197053496165552, -1.754224732379234153, 45.77356582045592859 ) ) ;
#20770=LINE ( 'NONE', #14283, #2375 ) ;
#20771=ORIENTED_EDGE ( 'NONE', *, *, #28000, .F. ) ;
#20772=CARTESIAN_POINT ( 'NONE',  ( -20.20997486282892552, 1.395963739018065216E-16, 29.60348406988233450 ) ) ;
#20774=ORIENTED_EDGE ( 'NONE', *, *, #25404, .T. ) ;
#20784=CARTESIAN_POINT ( 'NONE',  ( -55.24390624410018802, -0.004572280736702649152, 0.009374879212966917563 ) ) ;
#20788=B_SPLINE_CURVE_WITH_KNOTS ( 'NONE', 3,
 ( #8955, #19727, #24080, #11104, #13538, #19875 ),
 .UNSPECIFIED., .F., .F.,
 ( 4, 2, 4 ),
 ( 0.000000000000000000, 0.0004335184443140234316, 0.0008670368886280468632 ),
 .UNSPECIFIED. ) ;
#20798=ORIENTED_EDGE ( 'NONE', *, *, #7972, .F. ) ;
#20799=VECTOR ( 'NONE', #22382, 999.9999999999998863 ) ;
#20806=VECTOR ( 'NONE', #25872, 1000.000000000000000 ) ;
#20807=EDGE_CURVE ( 'NONE', #6648, #3087, #11376, .T. ) ;
#20811=FACE_OUTER_BOUND ( 'NONE', #22623, .T. ) ;
#20812=CARTESIAN_POINT ( 'NONE',  ( -55.24300891470648622, -0.0003472257464243277253, 0.009812809446890398413 ) ) ;
#20818=CARTESIAN_POINT ( 'NONE',  ( -20.20700224038492721, -27.82980252387826781, -10.08426345511578504 ) ) ;
#20820=CARTESIAN_POINT ( 'NONE',  ( -28.41354790283022069, 12.60397206714860729, 19.47297445639535596 ) ) ;
#20823=SHAPE_DEFINITION_REPRESENTATION ( #26227, #22271 ) ;
#20830=ADVANCED_FACE ( 'NONE', ( #4466 ), #25444, .F. ) ;
#20833=CARTESIAN_POINT ( 'NONE',  ( -1.019300379054419947, 38.21680004809164899, -25.26451264419658571 ) ) ;
#20838=ORIENTED_EDGE ( 'NONE', *, *, #6198, .T. ) ;
#20841=CARTESIAN_POINT ( 'NONE',  ( -1.019300379054419725, -12.21833869579434761, 44.15350047934410327 ) ) ;
#20855=DIRECTION ( 'NONE',  ( 1.000000000000000000, -6.938893903907226837E-18, 1.734723475976806709E-18 ) ) ;
#20868=FACE_OUTER_BOUND ( 'NONE', #24226, .T. ) ;
#20875=ORIENTED_EDGE ( 'NONE', *, *, #2874, .F. ) ;
#20876=EDGE_CURVE ( 'NONE', #13127, #22027, #7174, .T. ) ;
#20880=EDGE_CURVE ( 'NONE', #15661, #19144, #3756, .T. ) ;
#20883=CARTESIAN_POINT ( 'NONE',  ( -8.786685647604894456, 7.199674155859698388, 53.04920435127174017 ) ) ;
#20885=VERTEX_POINT ( 'NONE', #20727 ) ;
#20886=CARTESIAN_POINT ( 'NONE',  ( -1.031422197589711987, 43.06660437151308685, -15.60268798220652720 ) ) ;
#20888=CARTESIAN_POINT ( 'NONE',  ( -28.13707043255157103, -6.342158660427161365, -22.00298671236737391 ) ) ;
#20892=CARTESIAN_POINT ( 'NONE',  ( -15.02187109954783750, -6.234056423739195552, 45.93032478317469725 ) ) ;
#20896=DIRECTION ( 'NONE',  ( 1.000000000000000000, -6.938893903907226837E-18, 1.734723475976806709E-18 ) ) ;
#20899=EDGE_CURVE ( 'NONE', #10702, #22524, #5037, .T. ) ;
#20900=CARTESIAN_POINT ( 'NONE',  ( -28.13707043255157103, -21.52861750560933984, 7.802116958609231823 ) ) ;
#20902=ADVANCED_FACE ( 'NONE', ( #22625 ), #28348, .F. ) ;
#20908=CARTESIAN_POINT ( 'NONE',  ( -22.23342874802667879, -2.180636882146296696, 31.55488258420093572 ) ) ;
#20914=CARTESIAN_POINT ( 'NONE',  ( -1.058473599757834283, 35.99997772736212198, -28.32531354681296420 ) ) ;
#20920=ORIENTED_EDGE ( 'NONE', *, *, #19181, .F. ) ;
#20926=ADVANCED_FACE ( 'NONE', ( #5327 ), #13816, .F. ) ;
#20927=CARTESIAN_POINT ( 'NONE',  ( -23.79223135445719706, 24.83942264280432610, 22.01133905265658441 ) ) ;
#20933=VERTEX_POINT ( 'NONE', #7223 ) ;
#20937=CARTESIAN_POINT ( 'NONE',  ( -1.619063947482197729, 25.20140673341430571, 38.92136151114879539 ) ) ;
#20944=CARTESIAN_POINT ( 'NONE',  ( -1.056502255334265339, 26.51074901220557933, 37.35734037467605617 ) ) ;
#20946=CARTESIAN_POINT ( 'NONE',  ( -55.25297051322618813, 0.002853887643042873987, -0.01466904165775150676 ) ) ;
#20949=EDGE_CURVE ( 'NONE', #12283, #18596, #12304, .T. ) ;
#20950=B_SPLINE_CURVE_WITH_KNOTS ( 'NONE', 3,
 ( #15579, #11567, #9423, #13579, #9127, #26672 ),
 .UNSPECIFIED., .F., .F.,
 ( 4, 2, 4 ),
 ( 8.673617379884034509E-19, 0.0004335184443140208837, 0.0008670368886280409000 ),
 .UNSPECIFIED. ) ;
#20955=CARTESIAN_POINT ( 'NONE',  ( -20.47566338032523348, 7.708089572830403746, -28.85746366088566361 ) ) ;
#20962=CARTESIAN_POINT ( 'NONE',  ( -1.049819825607573254, -13.66706894614408618, 43.71263398674766876 ) ) ;
#20964=CARTESIAN_POINT ( 'NONE',  ( -55.24390624410018802, 0.001451500391953283731, -0.01032895241566680888 ) ) ;
#20967=EDGE_LOOP ( 'NONE', ( #15618, #9923, #26139, #8328 ) ) ;
#20970=CARTESIAN_POINT ( 'NONE',  ( -1.239374126674604337, -11.92219841463799135, 44.48112152129359487 ) ) ;
#20986=CARTESIAN_POINT ( 'NONE',  ( -55.25297051322618813, -0.001818774723748856851, 0.01483298743815036902 ) ) ;
#20989=DIRECTION ( 'NONE',  ( -1.000000000000000000, 6.938893903907226837E-18, -1.734723475976806709E-18 ) ) ;
#21002=ORIENTED_EDGE ( 'NONE', *, *, #23288, .T. ) ;
#21005=DIRECTION ( 'NONE',  ( -0.7637818620346801257, -0.5092696688508642211, 0.3965875333584858997 ) ) ;
#21007=ORIENTED_EDGE ( 'NONE', *, *, #10871, .F. ) ;
#21013=CARTESIAN_POINT ( 'NONE',  ( -6.588769196390765970, 38.42957692275894033, 34.04709086065274448 ) ) ;
#21015=CARTESIAN_POINT ( 'NONE',  ( -7.711401346138401891, 52.11446537925913702, -6.030154970217080468 ) ) ;
#21016=CARTESIAN_POINT ( 'NONE',  ( -1.048172774974307053, -45.78636862970790133, 1.020161070261597303 ) ) ;
#21022=LINE ( 'NONE', #10106, #15776 ) ;
#21029=ORIENTED_EDGE ( 'NONE', *, *, #13220, .F. ) ;
#21031=CARTESIAN_POINT ( 'NONE',  ( -1.583189561560253589, 16.68617981233763814, 43.29471907393723029 ) ) ;
#21035=CARTESIAN_POINT ( 'NONE',  ( -8.786685647604890903, -52.67761315067293282, -9.545808661480407409 ) ) ;
#21042=CARTESIAN_POINT ( 'NONE',  ( -55.25297051322618813, 0.006313402748432478395, 0.01354497706059498707 ) ) ;
#21043=CARTESIAN_POINT ( 'NONE',  ( -1.539763995773681060, -2.469814354917172494, 46.22267697748607418 ) ) ;
#21052=ORIENTED_EDGE ( 'NONE', *, *, #6348, .T. ) ;
#21054=ORIENTED_EDGE ( 'NONE', *, *, #11402, .F. ) ;
#21058=B_SPLINE_CURVE_WITH_KNOTS ( 'NONE', 3,
 ( #10209, #18541, #25468, #3701, #1255, #23170 ),
 .UNSPECIFIED., .F., .F.,
 ( 4, 2, 4 ),
 ( 1.499206600309199041E-16, 0.003570751334075636992, 0.007141502668151123931 ),
 .UNSPECIFIED. ) ;
#21059=CARTESIAN_POINT ( 'NONE',  ( -1.583189561560256253, 16.68617981233763459, 43.29471907393723029 ) ) ;
#21063=CARTESIAN_POINT ( 'NONE',  ( -25.21435515916043713, 25.00736669481056751, 23.92354251275909505 ) ) ;
#21071=ORIENTED_EDGE ( 'NONE', *, *, #10485, .T. ) ;
#21080=ORIENTED_EDGE ( 'NONE', *, *, #18060, .F. ) ;
#21085=CARTESIAN_POINT ( 'NONE',  ( -24.53239521893647890, -6.738460611583005466, -33.25736993155761922 ) ) ;
#21089=ORIENTED_EDGE ( 'NONE', *, *, #17287, .F. ) ;
#21091=B_SPLINE_CURVE_WITH_KNOTS ( 'NONE', 3,
 ( #8367, #3896, #21449, #10102, #4311, #17682, #21874 ),
 .UNSPECIFIED., .F., .F.,
 ( 4, 3, 4 ),
 ( 5.463690523629807176E-17, 0.009512539173626407066, 0.02506242213020838661 ),
 .UNSPECIFIED. ) ;
#21094=CARTESIAN_POINT ( 'NONE',  ( -21.41430102051751305, 25.94791611261640085, 16.60879216503605704 ) ) ;
#21097=CARTESIAN_POINT ( 'NONE',  ( -55.24390624410018802, 0.01027195578988056128, 0.001811362924362418811 ) ) ;
#21103=CARTESIAN_POINT ( 'NONE',  ( -20.21097721650788159, -28.26295598655178765, -8.835581399095051580 ) ) ;
#21118=CARTESIAN_POINT ( 'NONE',  ( -1.619063947482197729, -29.22875152547730337, 35.99532424477411041 ) ) ;
#21122=CARTESIAN_POINT ( 'NONE',  ( -20.90916690077965612, 5.322316104228523415, 39.20864005633514893 ) ) ;
#21131=CARTESIAN_POINT ( 'NONE',  ( -12.94347594948481728, -21.16159467081325474, 43.91326021875537577 ) ) ;
#21134=ORIENTED_EDGE ( 'NONE', *, *, #20109, .F. ) ;
#21136=AXIS2_PLACEMENT_3D ( 'NONE', #25743, #6035, #3860 ) ;
#21142=CARTESIAN_POINT ( 'NONE',  ( -8.786685647604890903, -47.14957014837335691, 25.35688121747554291 ) ) ;
#21152=EDGE_CURVE ( 'NONE', #9239, #11658, #22253, .T. ) ;
#21153=EDGE_LOOP ( 'NONE', ( #11613, #27043, #19391, #15786, #16118, #6041, #23674, #25114, #8594, #18781, #9322, #12286, #18285, #11085, #19542, #12221, #16829, #13670, #1697, #24003, #23274, #14834, #19601, #12889, #5722, #4776, #23696, #15163, #21806, #687, #16576, #26610, #25574, #14356, #14063, #1977, #1776, #9810, #69, #8622, #19962, #4205, #5713, #23996, #18225, #13430, #7742, #2188, #26667, #19857, #22933, #16897, #4449, #13527, #8794, #1519, #5428, #15429, #10202, #22989, #27858, #7308, #1582, #10737 ) ) ;
#21156=CARTESIAN_POINT ( 'NONE',  ( -1.019300379054419725, -45.76814864815089123, 2.023851374323154761 ) ) ;
#21163=DIRECTION ( 'NONE',  ( -5.541455922705464902E-20, 5.223019709708320524E-21, -1.000000000000000000 ) ) ;
#21167=CARTESIAN_POINT ( 'NONE',  ( -8.786685647604885574, 6.096987947571466530E-17, -1.524246986892866633E-17 ) ) ;
#21176=VECTOR ( 'NONE', #4050, 1000.000000000000114 ) ;
#21182=B_SPLINE_CURVE_WITH_KNOTS ( 'NONE', 3,
 ( #22550, #22109, #20218, #24721, #16050, #11175 ),
 .UNSPECIFIED., .F., .F.,
 ( 4, 2, 4 ),
 ( 0.000000000000000000, 0.003570751334075635258, 0.007141502668151270515 ),
 .UNSPECIFIED. ) ;
#21187=CARTESIAN_POINT ( 'NONE',  ( -1.464342487929856995, 46.14921266389555399, -2.431462367721493045 ) ) ;
#21189=CARTESIAN_POINT ( 'NONE',  ( -1.045287976400362417, -1.530335034934427574, -45.76855895860943235 ) ) ;
#21195=B_SPLINE_CURVE_WITH_KNOTS ( 'NONE', 3,
 ( #23682, #23535, #12569, #5354, #9536, #22355, #3058, #9401, #9251, #11977, #18288, #18154, #26934 ),
 .UNSPECIFIED., .F., .F.,
 ( 4, 3, 3, 3, 4 ),
 ( 1.040834085586084257E-17, 0.0007657099931970558996, 0.001531419946797916336, 0.002296279302920154267, 0.003061450627205756364 ),
 .UNSPECIFIED. ) ;
#21198=B_SPLINE_CURVE_WITH_KNOTS ( 'NONE', 3,
 ( #17605, #26388, #6691, #24247, #4504, #21272, #199, #5886, #16827, #6176 ),
 .UNSPECIFIED., .F., .F.,
 ( 4, 2, 2, 2, 4 ),
 ( 2.799429325053882983E-16, 0.0003346187017559026965, 0.0006692374035115254520, 0.001003856105267148099, 0.001338474807022770963 ),
 .UNSPECIFIED. ) ;
#21225=ORIENTED_EDGE ( 'NONE', *, *, #10736, .T. ) ;
#21227=CARTESIAN_POINT ( 'NONE',  ( -1.049817751779875907, -27.33161971822171310, 36.75003908324323021 ) ) ;
#21230=EDGE_CURVE ( 'NONE', #25910, #17046, #26368, .T. ) ;
#21235=CARTESIAN_POINT ( 'NONE',  ( -7.733045908741331687, -25.81515396910893045, -45.70676731105710644 ) ) ;
#21236=CARTESIAN_POINT ( 'NONE',  ( -4.473127245936431073, -49.22197550883370809, -3.196405119333634470 ) ) ;
#21250=CARTESIAN_POINT ( 'NONE',  ( -55.24728320129491266, 0.01137345571547128398, 0.009072670231978179414 ) ) ;
#21253=CARTESIAN_POINT ( 'NONE',  ( -20.57838717382308147, 18.89542499756533545, 23.26537097894084383 ) ) ;
#21258=CARTESIAN_POINT ( 'NONE',  ( -1.259972190295316485, -45.95417440459613090, 2.243354636026243742 ) ) ;
#21262=EDGE_LOOP ( 'NONE', ( #28294, #24255, #2608, #14656 ) ) ;
#21271=( BOUNDED_SURFACE ( )  B_SPLINE_SURFACE ( 3, 1, ( 
 ( #20607, #20175 ),
 ( #22356, #11401 ),
 ( #22499, #18155 ),
 ( #11697, #15999 ) ),
 .UNSPECIFIED., .F., .F., .F. ) 
 B_SPLINE_SURFACE_WITH_KNOTS ( ( 4, 4 ),
 ( 2, 2 ),
 ( 0.000000000000000000, 1.000000000000000000 ),
 ( 0.000000000000000000, 1.000000000000000000 ),
 .UNSPECIFIED. ) 
 GEOMETRIC_REPRESENTATION_ITEM ( )  RATIONAL_B_SPLINE_SURFACE ( (
 ( 1.000000000000000000, 1.000000000000000000),
 ( 0.9934239774497838349, 0.8357310067453913582),
 ( 0.9934239774497838349, 0.8357310067453913582),
 ( 1.000000000000000000, 1.000000000000000000) ) ) 
 REPRESENTATION_ITEM ( '' )  SURFACE ( )  );
#21272=CARTESIAN_POINT ( 'NONE',  ( -1.259920593601986383, 38.49623866863347388, -25.19630221849063290 ) ) ;
#21275=CARTESIAN_POINT ( 'NONE',  ( -1.031422197589716205, 12.69107518035563764, 44.01264471863834160 ) ) ;
#21292=EDGE_CURVE ( 'NONE', #20516, #26383, #15268, .T. ) ;
#21296=CARTESIAN_POINT ( 'NONE',  ( -1.619063947482201282, 35.99532424477380488, -29.22875152547769062 ) ) ;
#21298=CARTESIAN_POINT ( 'NONE',  ( -1.464342487929857439, 29.09292098541713401, 35.90631960086386698 ) ) ;
#21307=CARTESIAN_POINT ( 'NONE',  ( -20.20700224038492010, 24.51628800869071867, 16.58740185276683832 ) ) ;
#21318=ORIENTED_EDGE ( 'NONE', *, *, #7537, .T. ) ;
#21323=FACE_OUTER_BOUND ( 'NONE', #13834, .T. ) ;
#21331=CARTESIAN_POINT ( 'NONE',  ( -55.24271866751342941, -0.009388511352199774979, 0.001425019990778928110 ) ) ;
#21334=CARTESIAN_POINT ( 'NONE',  ( -23.77929240705205416, 15.74261278740719128, 32.66578242509729790 ) ) ;
#21336=CARTESIAN_POINT ( 'NONE',  ( -28.13707043255157103, 22.00298671236740233, -6.342158660427079653 ) ) ;
#21342=CARTESIAN_POINT ( 'NONE',  ( -55.25719721206881729, 0.002847566758683125598, -0.01079965405819887508 ) ) ;
#21347=CARTESIAN_POINT ( 'NONE',  ( -24.53239521893646824, -30.86654523348673962, -14.09666242510777145 ) ) ;
#21352=EDGE_CURVE ( 'NONE', #15570, #10003, #3687, .T. ) ;
#21353=ADVANCED_FACE ( 'NONE', ( #19889 ), #11979, .F. ) ;
#21362=CARTESIAN_POINT ( 'NONE',  ( -28.41354790283022069, -5.969609727607868344, 22.41474081378006744 ) ) ;
#21368=CARTESIAN_POINT ( 'NONE',  ( -55.24271866751342941, 0.006757859501010503658, -0.006671293903668132526 ) ) ;
#21371=DIRECTION ( 'NONE',  ( 0.000000000000000000, 5.223019709707975211E-21, -1.000000000000000000 ) ) ;
#21381=ORIENTED_EDGE ( 'NONE', *, *, #16075, .F. ) ;
#21397=CARTESIAN_POINT ( 'NONE',  ( -1.463510566862830986, 29.09194585123833932, -35.90603835816513367 ) ) ;
#21406=CARTESIAN_POINT ( 'NONE',  ( -18.41936578851711559, 29.33493038358074045, -30.66520733838660462 ) ) ;
#21408=CARTESIAN_POINT ( 'NONE',  ( -23.79248802219729697, -22.01156985585185311, -24.83956736572401525 ) ) ;
#21409=CARTESIAN_POINT ( 'NONE',  ( -1.539763995773690164, -44.72359274866473555, 11.93465967526341842 ) ) ;
#21415=CARTESIAN_POINT ( 'NONE',  ( -1.045287976400365970, -45.76855895860942525, 1.530335034934587002 ) ) ;
#21417=CARTESIAN_POINT ( 'NONE',  ( -15.02187109954783040, -20.12219089991063825, 41.75590530176331328 ) ) ;
#21418=LINE ( 'NONE', #12635, #27244 ) ;
#21422=ORIENTED_EDGE ( 'NONE', *, *, #9767, .F. ) ;
#21425=EDGE_CURVE ( 'NONE', #9239, #9063, #19829, .T. ) ;
#21426=CARTESIAN_POINT ( 'NONE',  ( -21.41427618760457818, -19.54551635498111395, 23.81423075802604217 ) ) ;
#21427=CARTESIAN_POINT ( 'NONE',  ( -1.050230346682684113, 37.05182464822020449, 26.92058491724826297 ) ) ;
#21434=CARTESIAN_POINT ( 'NONE',  ( -20.20700224038492721, -24.51628800869059432, -16.58740185276701951 ) ) ;
#21440=CARTESIAN_POINT ( 'NONE',  ( -1.539760825549689516, -43.19716078875427456, 16.63252404870400269 ) ) ;
#21449=CARTESIAN_POINT ( 'NONE',  ( -12.94347594948484392, -8.691477019903656398, -47.96504705787742040 ) ) ;
#21464=CARTESIAN_POINT ( 'NONE',  ( -20.20612092514784663, 10.22177639105900226, 27.77903665678154255 ) ) ;
#21469=ORIENTED_EDGE ( 'NONE', *, *, #26542, .F. ) ;
#21470=CARTESIAN_POINT ( 'NONE',  ( -1.239374126674604337, 35.79060836339814955, -28.97829083655452820 ) ) ;
#21471=ORIENTED_EDGE ( 'NONE', *, *, #28075, .F. ) ;
#21475=CARTESIAN_POINT ( 'NONE',  ( -8.786685647604896232, 23.24040270374459993, 48.22796981442743913 ) ) ;
#21479=B_SPLINE_CURVE_WITH_KNOTS ( 'NONE', 3,
 ( #17714, #8958, #22486, #2302 ),
 .UNSPECIFIED., .F., .F.,
 ( 4, 4 ),
 ( 1.847623020647441449E-16, 0.001982023823822945483 ),
 .UNSPECIFIED. ) ;
#21485=ORIENTED_EDGE ( 'NONE', *, *, #18091, .F. ) ;
#21490=ORIENTED_EDGE ( 'NONE', *, *, #8113, .F. ) ;
#21501=EDGE_CURVE ( 'NONE', #6333, #11658, #21861, .T. ) ;
#21506=CARTESIAN_POINT ( 'NONE',  ( -1.583189561560253589, 29.24830400313217638, 36.01941156322755688 ) ) ;
#21510=CARTESIAN_POINT ( 'NONE',  ( -8.786685647604887350, -25.35688121747534751, -47.14957014837345639 ) ) ;
#21514=EDGE_LOOP ( 'NONE', ( #24244, #10818, #22063, #2294, #11740, #6148 ) ) ;
#21516=CARTESIAN_POINT ( 'NONE',  ( -25.21435515916043713, -31.17620025257576799, 15.02493970636179377 ) ) ;
#21517=( BOUNDED_SURFACE ( )  B_SPLINE_SURFACE ( 3, 1, ( 
 ( #8563, #10584 ),
 ( #17329, #2347 ),
 ( #210, #15446 ),
 ( #4516, #26118 ) ),
 .UNSPECIFIED., .F., .F., .F. ) 
 B_SPLINE_SURFACE_WITH_KNOTS ( ( 4, 4 ),
 ( 2, 2 ),
 ( 0.000000000000000000, 1.000000000000000000 ),
 ( 0.000000000000000000, 1.000000000000000000 ),
 .UNSPECIFIED. ) 
 GEOMETRIC_REPRESENTATION_ITEM ( )  RATIONAL_B_SPLINE_SURFACE ( (
 ( 1.000000000000000000, 1.000000000000000000),
 ( 0.9593753223639863714, 0.9995975284513187731),
 ( 0.9593753223639863714, 0.9995975284513187731),
 ( 1.000000000000000000, 1.000000000000000000) ) ) 
 REPRESENTATION_ITEM ( '' )  SURFACE ( )  );
#21518=EDGE_CURVE ( 'NONE', #6478, #8163, #2661, .T. ) ;
#21527=FACE_OUTER_BOUND ( 'NONE', #11136, .T. ) ;
#21534=ORIENTED_EDGE ( 'NONE', *, *, #3912, .F. ) ;
#21542=CARTESIAN_POINT ( 'NONE',  ( -20.57838717382308147, -18.89542499756516847, -23.26537097894098594 ) ) ;
#21544=CARTESIAN_POINT ( 'NONE',  ( -1.045287976400383290, -44.00138577190632816, 12.68782741917368106 ) ) ;
#21546=CARTESIAN_POINT ( 'NONE',  ( -55.24198130335446422, -0.001391250620101175178, -0.009190321388310287998 ) ) ;
#21547=VECTOR ( 'NONE', #14606, 1000.000000000000000 ) ;
#21549=ADVANCED_FACE ( 'NONE', ( #5144 ), #15840, .F. ) ;
#21557=CARTESIAN_POINT ( 'NONE',  ( -18.41936578851709783, -18.42310649277602508, 38.22933728004711185 ) ) ;
#21572=CARTESIAN_POINT ( 'NONE',  ( -55.24728320129491266, 0.01453410071985307417, -0.0006547948648738343260 ) ) ;
#21574=CARTESIAN_POINT ( 'NONE',  ( -1.619063947482194177, 29.22875152547808852, 35.99532424477347092 ) ) ;
#21576=VERTEX_POINT ( 'NONE', #2995 ) ;
#21582=DIRECTION ( 'NONE',  ( -0.7637818620346800147, 0.2198041754873925890, 0.6068965246771022004 ) ) ;
#21586=ORIENTED_EDGE ( 'NONE', *, *, #28032, .F. ) ;
#21588=FACE_OUTER_BOUND ( 'NONE', #6560, .T. ) ;
#21592=B_SPLINE_CURVE_WITH_KNOTS ( 'NONE', 3,
 ( #19902, #26233, #41, #6530, #19750, #24376, #22215 ),
 .UNSPECIFIED., .F., .F.,
 ( 4, 3, 4 ),
 ( 0.000000000000000000, 0.006568092053401806615, 0.02506242213020846293 ),
 .UNSPECIFIED. ) ;
#21594=VERTEX_POINT ( 'NONE', #27004 ) ;
#21605=ADVANCED_FACE ( 'NONE', ( #7316 ), #19701, .F. ) ;
#21610=LINE ( 'NONE', #15113, #3234 ) ;
#21611=CARTESIAN_POINT ( 'NONE',  ( -1.048996300304498419, -14.87787369922200043, -43.31387123529974303 ) ) ;
#21615=CARTESIAN_POINT ( 'NONE',  ( -4.473127245936431073, -3.196405119333463496, 49.22197550883370809 ) ) ;
#21619=VERTEX_POINT ( 'NONE', #20249 ) ;
#21621=AXIS2_PLACEMENT_3D ( 'NONE', #27886, #16945, #27455 ) ;
#21625=VERTEX_POINT ( 'NONE', #18372 ) ;
#21627=VECTOR ( 'NONE', #3166, 999.9999999999998863 ) ;
#21634=EDGE_CURVE ( 'NONE', #15497, #18539, #23243, .T. ) ;
#21654=CARTESIAN_POINT ( 'NONE',  ( -1.049819825607588575, -27.33096219556267670, -36.75053263699379613 ) ) ;
#21657=FACE_OUTER_BOUND ( 'NONE', #5117, .T. ) ;
#21659=ORIENTED_EDGE ( 'NONE', *, *, #22531, .T. ) ;
#21667=VECTOR ( 'NONE', #18453, 999.9999999999998863 ) ;
#21670=ADVANCED_FACE ( 'NONE', ( #1538 ), #18779, .F. ) ;
#21687=CARTESIAN_POINT ( 'NONE',  ( -1.050230346682675231, -43.55772679531839486, 14.15203301556477378 ) ) ;
#21690=( BOUNDED_SURFACE ( )  B_SPLINE_SURFACE ( 3, 1, ( 
 ( #20127, #20268 ),
 ( #9491, #9628 ),
 ( #9195, #15512 ),
 ( #7058, #2866 ) ),
 .UNSPECIFIED., .F., .F., .F. ) 
 B_SPLINE_SURFACE_WITH_KNOTS ( ( 4, 4 ),
 ( 2, 2 ),
 ( 0.000000000000000000, 1.000000000000000000 ),
 ( 0.000000000000000000, 1.000000000000000000 ),
 .UNSPECIFIED. ) 
 GEOMETRIC_REPRESENTATION_ITEM ( )  RATIONAL_B_SPLINE_SURFACE ( (
 ( 1.000000000000000000, 1.000000000000000000),
 ( 0.9593753223639863714, 0.9995975284513187731),
 ( 0.9593753223639863714, 0.9995975284513187731),
 ( 1.000000000000000000, 1.000000000000000000) ) ) 
 REPRESENTATION_ITEM ( '' )  SURFACE ( )  );
#21694=CARTESIAN_POINT ( 'NONE',  ( -8.786685647604890903, 47.14957014837354876, -25.35688121747519119 ) ) ;
#21699=B_SPLINE_CURVE_WITH_KNOTS ( 'NONE', 3,
 ( #16623, #388, #5532, #18772, #10153, #4857, #25413 ),
 .UNSPECIFIED., .F., .F.,
 ( 4, 3, 4 ),
 ( 1.868354362588067661E-17, 0.009512539173626417474, 0.02506242213020845253 ),
 .UNSPECIFIED. ) ;
#21701=CARTESIAN_POINT ( 'NONE',  ( -28.13707043255157103, 22.00298671236748760, 6.342158660426773231 ) ) ;
#21702=EDGE_CURVE ( 'NONE', #711, #710, #14996, .T. ) ;
#21703=VERTEX_POINT ( 'NONE', #14193 ) ;
#21704=CARTESIAN_POINT ( 'NONE',  ( -1.045287976400383290, -36.12803364096628655, -28.14015102489793918 ) ) ;
#21709=CARTESIAN_POINT ( 'NONE',  ( -1.048171036023513025, 36.44209502233747600, 27.73816396939524509 ) ) ;
#21710=CARTESIAN_POINT ( 'NONE',  ( -28.41354790283022069, -21.64275480268742058, 8.345538364877306492 ) ) ;
#21715=CARTESIAN_POINT ( 'NONE',  ( -5.986830583229489022, -4.559539818181495896, -50.53158596890440180 ) ) ;
#21716=CARTESIAN_POINT ( 'NONE',  ( -4.780792508754321268, 3.764354093953580449, -49.38761389561002346 ) ) ;
#21737=B_SPLINE_CURVE_WITH_KNOTS ( 'NONE', 3,
 ( #4150, #6329, #19683, #21434 ),
 .UNSPECIFIED., .F., .F.,
 ( 4, 4 ),
 ( 1.956780383866537384E-16, 0.001982023823822938111 ),
 .UNSPECIFIED. ) ;
#21742=CIRCLE ( 'NONE', #27717, 34.60786435723138510 ) ;
#21748=ORIENTED_EDGE ( 'NONE', *, *, #8205, .T. ) ;
#21749=EDGE_CURVE ( 'NONE', #9286, #16092, #12610, .T. ) ;
#21751=CARTESIAN_POINT ( 'NONE',  ( -20.57838717382308147, -27.96569011373093971, -10.78122205916989529 ) ) ;
#21752=EDGE_CURVE ( 'NONE', #23016, #11485, #5369, .T. ) ;
#21760=CARTESIAN_POINT ( 'NONE',  ( -24.53237795827031320, 33.25734978085278470, 6.738475012719742807 ) ) ;
#21763=CARTESIAN_POINT ( 'NONE',  ( -8.786685647604890903, 25.35688121747502066, -47.14957014837363403 ) ) ;
#21764=CARTESIAN_POINT ( 'NONE',  ( -1.056502255334264895, 37.35734037467673119, 26.51074901220462721 ) ) ;
#21774=VERTEX_POINT ( 'NONE', #23731 ) ;
#21786=B_SPLINE_CURVE_WITH_KNOTS ( 'NONE', 3,
 ( #2199, #15302, #26398, #10732, #19496, #8430, #17195, #24116, #28125, #4379, #23979, #1925, #17464 ),
 .UNSPECIFIED., .F., .F.,
 ( 4, 3, 3, 3, 4 ),
 ( 1.250926888277100303E-17, 0.0007657099931970583933, 0.001531419946797919589, 0.002296279302920155134, 0.003061450627205745088 ),
 .UNSPECIFIED. ) ;
#21789=CARTESIAN_POINT ( 'NONE',  ( -28.41354790283022069, -21.64275480268754137, -8.345538364876993853 ) ) ;
#21799=CARTESIAN_POINT ( 'NONE',  ( -1.155001620486252101, -42.97366440495923001, -16.13799328198405902 ) ) ;
#21804=CARTESIAN_POINT ( 'NONE',  ( -1.045287976400351981, 12.68782741917293855, -44.00138577190654132 ) ) ;
#21806=ORIENTED_EDGE ( 'NONE', *, *, #24449, .T. ) ;
#21807=CARTESIAN_POINT ( 'NONE',  ( -6.588769196390764193, -11.07780292579730208, -50.13301368233293687 ) ) ;
#21808=EDGE_CURVE ( 'NONE', #384, #4332, #24964, .T. ) ;
#21811=EDGE_LOOP ( 'NONE', ( #16628, #451 ) ) ;
#21812=EDGE_CURVE ( 'NONE', #14642, #9224, #6571, .T. ) ;
#21817=DIRECTION ( 'NONE',  ( 0.000000000000000000, 5.223019709708190374E-21, -1.000000000000000000 ) ) ;
#21837=CARTESIAN_POINT ( 'NONE',  ( -1.619063947482197729, -35.99532424477357750, 29.22875152547795707 ) ) ;
#21838=CARTESIAN_POINT ( 'NONE',  ( -23.79248802219723302, -33.03370827286728684, 3.207402715357496881 ) ) ;
#21849=CARTESIAN_POINT ( 'NONE',  ( -1.058197053496161999, -36.00048521498973031, -28.32422455455065347 ) ) ;
#21855=B_SPLINE_CURVE_WITH_KNOTS ( 'NONE', 3,
 ( #16260, #22613, #13662, #22464 ),
 .UNSPECIFIED., .F., .F.,
 ( 4, 4 ),
 ( 1.892757412642747770E-16, 0.001982023823822945049 ),
 .UNSPECIFIED. ) ;
#21857=CARTESIAN_POINT ( 'NONE',  ( -6.574463467970651287, -5.014313797967385966, -51.07975593197902953 ) ) ;
#21861=LINE ( 'NONE', #4015, #16669 ) ;
#21867=CARTESIAN_POINT ( 'NONE',  ( -20.47566262905010603, 28.85746289809577547, -7.708089517695290382 ) ) ;
#21873=VERTEX_POINT ( 'NONE', #19944 ) ;
#21874=CARTESIAN_POINT ( 'NONE',  ( -25.21435515916043713, -6.169479169075696490, -34.05351380035330777 ) ) ;
#21877=EDGE_CURVE ( 'NONE', #4332, #7007, #19442, .T. ) ;
#21878=CARTESIAN_POINT ( 'NONE',  ( -1.056502255334265339, -37.35734037467615565, 26.51074901220544433 ) ) ;
#21880=CARTESIAN_POINT ( 'NONE',  ( -6.574463467970683261, 44.27173031830773908, 25.96726214983142000 ) ) ;
#21882=EDGE_CURVE ( 'NONE', #11326, #16414, #6389, .T. ) ;
#21885=B_SPLINE_CURVE_WITH_KNOTS ( 'NONE', 3,
 ( #27275, #18501, #11451, #13744, #14168, #2819, #5116, #2668 ),
 .UNSPECIFIED., .F., .F.,
 ( 4, 2, 2, 4 ),
 ( 0.000000000000000000, 0.002761524886576637201, 0.005523049773153274403, 0.01104609954630654707 ),
 .UNSPECIFIED. ) ;
#21889=CARTESIAN_POINT ( 'NONE',  ( -20.20612091757422846, -18.30568244821359869, 23.26073043121652262 ) ) ;
#21890=CARTESIAN_POINT ( 'NONE',  ( -8.786685647604890903, 23.24040270374391426, -48.22796981442777309 ) ) ;
#21894=EDGE_LOOP ( 'NONE', ( #27413, #23916, #27457, #28442 ) ) ;
#21895=CARTESIAN_POINT ( 'NONE',  ( -1.058473599757816963, -25.48501014712370960, 38.06357893967457784 ) ) ;
#21897=CARTESIAN_POINT ( 'NONE',  ( -1.050231094221214301, -43.63617436699747287, -13.91061116148175536 ) ) ;
#21900=CARTESIAN_POINT ( 'NONE',  ( -6.574463467970649511, 25.96726214983191383, -44.27173031830743355 ) ) ;
#21905=DIRECTION ( 'NONE',  ( 0.000000000000000000, 5.223019709707975211E-21, -1.000000000000000000 ) ) ;
#21906=CARTESIAN_POINT ( 'NONE',  ( -8.786685647604885574, 6.096987947571466530E-17, -1.524246986892866633E-17 ) ) ;
#21911=EDGE_CURVE ( 'NONE', #24805, #17826, #13260, .T. ) ;
#21916=EDGE_LOOP ( 'NONE', ( #17211, #5374, #16882, #24766 ) ) ;
#21919=CARTESIAN_POINT ( 'NONE',  ( -1.044557008772710072, -45.76404748504492659, -1.643388457097728184 ) ) ;
#21925=CARTESIAN_POINT ( 'NONE',  ( -8.786685647604890903, -48.22796981442753150, 23.24040270374441874 ) ) ;
#21928=ORIENTED_EDGE ( 'NONE', *, *, #11402, .T. ) ;
#21929=ORIENTED_EDGE ( 'NONE', *, *, #2387, .T. ) ;
#21930=CARTESIAN_POINT ( 'NONE',  ( -8.786685647604885574, 6.096987947571466530E-17, -1.524246986892866633E-17 ) ) ;
#21933=CARTESIAN_POINT ( 'NONE',  ( -1.031422197589716205, 43.06660437151310816, -15.60268798220652187 ) ) ;
#21935=CARTESIAN_POINT ( 'NONE',  ( -1.155031165708882979, 35.88345263711048716, -28.62780465193323920 ) ) ;
#21937=VERTEX_POINT ( 'NONE', #25126 ) ;
#21938=CARTESIAN_POINT ( 'NONE',  ( -1.619063947482197729, -2.489035965909835557, 46.30105812165550816 ) ) ;
#21941=CARTESIAN_POINT ( 'NONE',  ( -1.050230346682680782, -26.91946103437133431, -37.05264119692680680 ) ) ;
#21942=ORIENTED_EDGE ( 'NONE', *, *, #27552, .T. ) ;
#21946=EDGE_LOOP ( 'NONE', ( #12869, #18967, #25067, #9320 ) ) ;
#21950=ORIENTED_EDGE ( 'NONE', *, *, #12234, .F. ) ;
#21952=CARTESIAN_POINT ( 'NONE',  ( -20.57838717382308147, -27.96569011373078339, 10.78122205917029675 ) ) ;
#21963=CARTESIAN_POINT ( 'NONE',  ( -1.031422197589716205, 45.78027046666444733, 1.530725436377623927 ) ) ;
#21964=EDGE_CURVE ( 'NONE', #1898, #10231, #12062, .T. ) ;
#21977=CARTESIAN_POINT ( 'NONE',  ( -7.078251931573400491, 26.33626633876288636, 44.92740138729136135 ) ) ;
#21990=VECTOR ( 'NONE', #14434, 1000.000000000000000 ) ;
#21998=VERTEX_POINT ( 'NONE', #17845 ) ;
#22000=CARTESIAN_POINT ( 'NONE',  ( -20.20700224038492721, -28.44216453106531617, 8.199606986804630182 ) ) ;
#22005=ORIENTED_EDGE ( 'NONE', *, *, #23139, .T. ) ;
#22013=CARTESIAN_POINT ( 'NONE',  ( -55.24271866751342941, 0.006757859501006707216, 0.006671293903669109175 ) ) ;
#22016=B_SPLINE_CURVE_WITH_KNOTS ( 'NONE', 3,
 ( #11167, #17632, #7277, #24270, #503, #11586 ),
 .UNSPECIFIED., .F., .F.,
 ( 4, 2, 4 ),
 ( 7.757919228897728493E-18, 0.0004335184443140311294, 0.0008670368886280545610 ),
 .UNSPECIFIED. ) ;
#22019=ORIENTED_EDGE ( 'NONE', *, *, #23139, .F. ) ;
#22025=CARTESIAN_POINT ( 'NONE',  ( -7.733045908741324581, 35.49239760110675945, -38.67583825854160295 ) ) ;
#22026=CARTESIAN_POINT ( 'NONE',  ( -1.058197053496160667, -12.47644286888545828, -44.07533330186785037 ) ) ;
#22027=VERTEX_POINT ( 'NONE', #8802 ) ;
#22032=CARTESIAN_POINT ( 'NONE',  ( -1.464342487929843006, -11.94843286121887438, 44.64187261869788870 ) ) ;
#22035=DIRECTION ( 'NONE',  ( -1.000000000000000000, 6.938893903907226837E-18, -1.734723475976806709E-18 ) ) ;
#22039=DIRECTION ( 'NONE',  ( -0.7637818620346800147, -0.2198041754873968356, -0.6068965246771005351 ) ) ;
#22049=B_SPLINE_CURVE_WITH_KNOTS ( 'NONE', 3,
 ( #23221, #24701, #4948, #20892, #20197, #9973, #11571 ),
 .UNSPECIFIED., .F., .F.,
 ( 4, 3, 4 ),
 ( 1.114146325429624918E-17, 0.009512539173626377575, 0.02506242213020845946 ),
 .UNSPECIFIED. ) ;
#22050=EDGE_CURVE ( 'NONE', #12735, #2493, #18049, .T. ) ;
#22053=CARTESIAN_POINT ( 'NONE',  ( -55.24300891470648622, -0.009225237711097735230, -0.003362556190414862749 ) ) ;
#22055=EDGE_CURVE ( 'NONE', #25403, #6415, #22937, .T. ) ;
#22057=CARTESIAN_POINT ( 'NONE',  ( -1.050230347699842692, 1.897926697972695375E-16, 45.79907861674080749 ) ) ;
#22059=CARTESIAN_POINT ( 'NONE',  ( -1.045287976400351981, 12.68782741917293855, -44.00138577190654132 ) ) ;
#22061=CARTESIAN_POINT ( 'NONE',  ( -12.94347594948494340, 6.555928820869281637, -48.30328466416744249 ) ) ;
#22063=ORIENTED_EDGE ( 'NONE', *, *, #20434, .F. ) ;
#22067=CARTESIAN_POINT ( 'NONE',  ( -55.24390624410018802, -0.001451500391952595045, 0.01032895241566660592 ) ) ;
#22068=VECTOR ( 'NONE', #8446, 999.9999999999998863 ) ;
#22070=FACE_OUTER_BOUND ( 'NONE', #937, .T. ) ;
#22075=ORIENTED_EDGE ( 'NONE', *, *, #27825, .T. ) ;
#22079=VERTEX_POINT ( 'NONE', #11102 ) ;
#22091=AXIS2_PLACEMENT_3D ( 'NONE', #14015, #11868, #13730 ) ;
#22093=CARTESIAN_POINT ( 'NONE',  ( -55.24300891470650754, 0.009225237711101738972, -0.003362556190412665288 ) ) ;
#22104=EDGE_LOOP ( 'NONE', ( #12314, #4301, #9265, #13106 ) ) ;
#22109=CARTESIAN_POINT ( 'NONE',  ( -21.41430102051744555, 1.815007301162403497, 30.75470819672109002 ) ) ;
#22113=CARTESIAN_POINT ( 'NONE',  ( -12.82751273423884442, 6.573887447703498310, 48.43568301531131937 ) ) ;
#22114=CIRCLE ( 'NONE', #23957, 53.53553390275978785 ) ;
#22120=CARTESIAN_POINT ( 'NONE',  ( -55.24728320129491266, -0.01214321324517104832, 0.008013189884951824049 ) ) ;
#22121=CIRCLE ( 'NONE', #25813, 37.50000000000001421 ) ;
#22125=CARTESIAN_POINT ( 'NONE',  ( -1.583189561560253589, -11.94859433442870866, 44.83405390829683057 ) ) ;
#22130=CARTESIAN_POINT ( 'NONE',  ( -1.583189561560252701, 46.33203782964461936, 2.490696082060036343 ) ) ;
#22131=EDGE_CURVE ( 'NONE', #10550, #9180, #9349, .T. ) ;
#22142=EDGE_LOOP ( 'NONE', ( #2525, #22964, #19976, #4035 ) ) ;
#22148=CARTESIAN_POINT ( 'NONE',  ( -25.21435515916043002, -4.655591116594591128, -34.29329011225954105 ) ) ;
#22156=CARTESIAN_POINT ( 'NONE',  ( -21.41430102051752016, 11.22990201072317262, 28.68859753627381792 ) ) ;
#22158=EDGE_LOOP ( 'NONE', ( #4303, #3132, #21002, #23066 ) ) ;
#22171=CARTESIAN_POINT ( 'NONE',  ( -55.24271866751342941, -0.008488649505345847654, 0.004256484107793125603 ) ) ;
#22177=CARTESIAN_POINT ( 'NONE',  ( -1.044556982611280382, -25.56989963842174873, 37.98985389331836870 ) ) ;
#22179=CARTESIAN_POINT ( 'NONE',  ( -28.13707043255157103, 18.96624908365864925, 12.83104814250432923 ) ) ;
#22184=CARTESIAN_POINT ( 'NONE',  ( -25.21435515916025594, 34.29329011225976132, 4.655591116594488099 ) ) ;
#22186=CARTESIAN_POINT ( 'NONE',  ( -1.619063947482197729, -35.99532424477357750, 29.22875152547795707 ) ) ;
#22192=VERTEX_POINT ( 'NONE', #26736 ) ;
#22200=EDGE_CURVE ( 'NONE', #6724, #23613, #11897, .T. ) ;
#22201=VERTEX_POINT ( 'NONE', #3430 ) ;
#22203=CARTESIAN_POINT ( 'NONE',  ( -20.47566338032518019, 29.82700953060488303, -1.586617869343990739 ) ) ;
#22212=CARTESIAN_POINT ( 'NONE',  ( -12.82751273423881777, 43.04932478553568842, 23.15139349681263070 ) ) ;
#22215=CARTESIAN_POINT ( 'NONE',  ( -8.786685647604894456, 37.00619870957989832, 38.68584556812258768 ) ) ;
#22217=B_SPLINE_CURVE_WITH_KNOTS ( 'NONE', 3,
 ( #3707, #2338, #11140, #19913 ),
 .UNSPECIFIED., .F., .F.,
 ( 4, 4 ),
 ( 0.0009910334943227156780, 0.001982023823822944616 ),
 .UNSPECIFIED. ) ;
#22224=CARTESIAN_POINT ( 'NONE',  ( -1.155001620486273861, 35.88346938217592452, 28.62773628245626867 ) ) ;
#22234=B_SPLINE_CURVE_WITH_KNOTS ( 'NONE', 3,
 ( #5311, #5457, #18701, #9791, #16252, #14216, #1277, #24771, #20427, #18119 ),
 .UNSPECIFIED., .F., .F.,
 ( 4, 2, 2, 2, 4 ),
 ( 2.847672227753435151E-16, 0.0003346187017559034554, 0.0006692374035115221994, 0.001003856105267140727, 0.001338474807022759470 ),
 .UNSPECIFIED. ) ;
#22239=CARTESIAN_POINT ( 'NONE',  ( -28.13707043255157103, 18.06394523322473944, 14.07296284901312688 ) ) ;
#22242=ORIENTED_EDGE ( 'NONE', *, *, #6775, .F. ) ;
#22247=CARTESIAN_POINT ( 'NONE',  ( -1.049819825607596568, 37.34982882986881236, 26.50610175068227292 ) ) ;
#22248=CARTESIAN_POINT ( 'NONE',  ( -55.24390624410018802, 0.01032895241567037548, -0.001451500391950801341 ) ) ;
#22251=CARTESIAN_POINT ( 'NONE',  ( -23.77929240705206482, -31.93650644494352875, -17.17389748746951739 ) ) ;
#22253=B_SPLINE_CURVE_WITH_KNOTS ( 'NONE', 3,
 ( #916, #18623, #11859, #19055, #14287, #23108, #18764, #1486, #3367, #5826, #12416, #23388, #27393 ),
 .UNSPECIFIED., .F., .F.,
 ( 4, 3, 3, 3, 4 ),
 ( 1.551583845779545699E-17, 0.0007657099931970509123, 0.001531419946797920456, 0.002296279302920149930, 0.003061450627205759834 ),
 .UNSPECIFIED. ) ;
#22256=CARTESIAN_POINT ( 'NONE',  ( -1.031422197589711764, -12.69107518035532856, -44.01264471863841266 ) ) ;
#22260=CARTESIAN_POINT ( 'NONE',  ( -1.619063947482197729, 16.67502769180622835, 43.26576862488415287 ) ) ;
#22268=ORIENTED_EDGE ( 'NONE', *, *, #19157, .T. ) ;
#22271=SHAPE_REPRESENTATION ( 'pinion 3', ( #27263 ), #2919 ) ;
#22274=B_SPLINE_CURVE_WITH_KNOTS ( 'NONE', 3,
 ( #24895, #5156, #13931, #22743, #14644, #2192, #1404, #19760, #23310, #21118 ),
 .UNSPECIFIED., .F., .F.,
 ( 4, 2, 2, 2, 4 ),
 ( 2.976713740813343128E-16, 0.0003346187017559147311, 0.0006692374035115318488, 0.001003856105267148966, 0.001338474807022765976 ),
 .UNSPECIFIED. ) ;
#22284=CARTESIAN_POINT ( 'NONE',  ( -1.239374126674604337, -42.99367564261289942, -16.50008610789281605 ) ) ;
#22297=CARTESIAN_POINT ( 'NONE',  ( -1.045287976400365970, -37.92705037016778391, -25.66401692419976399 ) ) ;
#22301=ORIENTED_EDGE ( 'NONE', *, *, #3939, .T. ) ;
#22314=ORIENTED_EDGE ( 'NONE', *, *, #10002, .T. ) ;
#22319=CARTESIAN_POINT ( 'NONE',  ( -20.20997486282892552, 3.551351076220724598E-15, -29.60348406988233450 ) ) ;
#22321=( BOUNDED_SURFACE ( )  B_SPLINE_SURFACE ( 3, 1, ( 
 ( #18240, #11925 ),
 ( #9777, #25043 ),
 ( #11789, #5443 ),
 ( #25474, #7773 ) ),
 .UNSPECIFIED., .F., .F., .F. ) 
 B_SPLINE_SURFACE_WITH_KNOTS ( ( 4, 4 ),
 ( 2, 2 ),
 ( 0.000000000000000000, 1.000000000000000000 ),
 ( 0.000000000000000000, 1.000000000000000000 ),
 .UNSPECIFIED. ) 
 GEOMETRIC_REPRESENTATION_ITEM ( )  RATIONAL_B_SPLINE_SURFACE ( (
 ( 1.000000000000000000, 1.000000000000000000),
 ( 0.9934239774497838349, 0.8357310067453913582),
 ( 0.9934239774497838349, 0.8357310067453913582),
 ( 1.000000000000000000, 1.000000000000000000) ) ) 
 REPRESENTATION_ITEM ( '' )  SURFACE ( )  );
#22330=CARTESIAN_POINT ( 'NONE',  ( -7.078251931573406708, 44.92740138729204347, 26.33626633876174239 ) ) ;
#22335=DIRECTION ( 'NONE',  ( 0.000000000000000000, 5.223019709707975211E-21, -1.000000000000000000 ) ) ;
#22341=CARTESIAN_POINT ( 'NONE',  ( -1.259920593601978833, 44.39818421957814820, -12.06711544331578168 ) ) ;
#22346=ORIENTED_EDGE ( 'NONE', *, *, #17635, .T. ) ;
#22353=CARTESIAN_POINT ( 'NONE',  ( -1.048996300304507523, 36.59642367107745997, -27.53442103413706477 ) ) ;
#22355=CARTESIAN_POINT ( 'NONE',  ( -1.050231094221198536, 43.63617436699759367, 13.91061116148147292 ) ) ;
#22356=CARTESIAN_POINT ( 'NONE',  ( -55.24300891470650754, 0.005486913146700745682, -0.008142823778062297305 ) ) ;
#22358=CARTESIAN_POINT ( 'NONE',  ( -1.155001620486255209, -45.85729774065936937, -2.068551059060163677 ) ) ;
#22360=DIRECTION ( 'NONE',  ( 0.7637818620346800147, 0.6451161201712181104, 0.02150485345384620800 ) ) ;
#22361=CARTESIAN_POINT ( 'NONE',  ( -20.20700224038492721, -16.58740185276692358, 24.51628800869065827 ) ) ;
#22364=( BOUNDED_SURFACE ( )  B_SPLINE_SURFACE ( 3, 1, ( 
 ( #5210, #18007 ),
 ( #24808, #15866 ),
 ( #13986, #5060 ),
 ( #7533, #11544 ) ),
 .UNSPECIFIED., .F., .F., .F. ) 
 B_SPLINE_SURFACE_WITH_KNOTS ( ( 4, 4 ),
 ( 2, 2 ),
 ( 0.000000000000000000, 1.000000000000000000 ),
 ( 0.000000000000000000, 1.000000000000000000 ),
 .UNSPECIFIED. ) 
 GEOMETRIC_REPRESENTATION_ITEM ( )  RATIONAL_B_SPLINE_SURFACE ( (
 ( 1.000000000000000000, 1.000000000000000000),
 ( 0.7789835883360576307, 0.9689951854195403280),
 ( 0.7789835883360576307, 0.9689951854195403280),
 ( 1.000000000000000000, 1.000000000000000000) ) ) 
 REPRESENTATION_ITEM ( '' )  SURFACE ( )  );
#22366=CARTESIAN_POINT ( 'NONE',  ( -7.733045908741329022, -47.75066202881810540, -21.80378472388470001 ) ) ;
#22367=CARTESIAN_POINT ( 'NONE',  ( -7.078251931573406708, -5.101176922831029081, -51.82710018979473432 ) ) ;
#22369=EDGE_CURVE ( 'NONE', #1487, #18251, #14846, .T. ) ;
#22371=CARTESIAN_POINT ( 'NONE',  ( -55.25719721206881729, 0.008651607285661618019, -0.007063345920781386421 ) ) ;
#22376=CARTESIAN_POINT ( 'NONE',  ( -4.178947244162637631, -31.41809272265950170, -37.51424432987639079 ) ) ;
#22377=ORIENTED_EDGE ( 'NONE', *, *, #3188, .F. ) ;
#22379=ORIENTED_EDGE ( 'NONE', *, *, #20477, .F. ) ;
#22382=DIRECTION ( 'NONE',  ( 0.7563875759206388771, -0.2351350468682826267, 0.6104009704506950795 ) ) ;
#22386=CARTESIAN_POINT ( 'NONE',  ( -1.045287976400365970, -45.76855895860947498, -1.530335034933654859 ) ) ;
#22401=VERTEX_POINT ( 'NONE', #20513 ) ;
#22404=CARTESIAN_POINT ( 'NONE',  ( -2.911734481061364566, -40.13920818157090054, -25.69892591260251535 ) ) ;
#22418=ORIENTED_EDGE ( 'NONE', *, *, #22838, .T. ) ;
#22423=CARTESIAN_POINT ( 'NONE',  ( -55.25719721206881729, 0.006045473558784881206, 0.009391134844728978373 ) ) ;
#22433=CARTESIAN_POINT ( 'NONE',  ( -55.24271866751342941, -0.008488649505345844185, 0.004256484107793130807 ) ) ;
#22435=ORIENTED_EDGE ( 'NONE', *, *, #24485, .F. ) ;
#22439=CARTESIAN_POINT ( 'NONE',  ( -25.21435515916043713, -30.48034229288650820, -16.39063784838731053 ) ) ;
#22442=LINE ( 'NONE', #6475, #20745 ) ;
#22449=CARTESIAN_POINT ( 'NONE',  ( -23.79248802219728276, 13.25839849636400203, 30.42578156345371454 ) ) ;
#22452=ORIENTED_EDGE ( 'NONE', *, *, #15897, .F. ) ;
#22462=CARTESIAN_POINT ( 'NONE',  ( -24.53239521893646469, 14.09666242510788337, -30.86654523348667567 ) ) ;
#22464=CARTESIAN_POINT ( 'NONE',  ( -20.20700224038492721, 28.44216453106548315, 8.199606986804035103 ) ) ;
#22473=CARTESIAN_POINT ( 'NONE',  ( -2.904412668506656026, 44.35433137608966092, 17.42365698954652586 ) ) ;
#22480=EDGE_CURVE ( 'NONE', #3442, #8511, #17332, .T. ) ;
#22486=CARTESIAN_POINT ( 'NONE',  ( -20.21097721650785672, -17.67178726257375487, -23.76068422213751674 ) ) ;
#22487=CARTESIAN_POINT ( 'NONE',  ( -1.058197053496178874, 44.07533330186787168, -12.47644286888530019 ) ) ;
#22497=( BOUNDED_SURFACE ( )  B_SPLINE_SURFACE ( 3, 1, ( 
 ( #14984, #4049 ),
 ( #17283, #15112 ),
 ( #4189, #23372 ),
 ( #3623, #12400 ) ),
 .UNSPECIFIED., .F., .F., .F. ) 
 B_SPLINE_SURFACE_WITH_KNOTS ( ( 4, 4 ),
 ( 2, 2 ),
 ( 0.000000000000000000, 1.000000000000000000 ),
 ( 0.000000000000000000, 1.000000000000000000 ),
 .UNSPECIFIED. ) 
 GEOMETRIC_REPRESENTATION_ITEM ( )  RATIONAL_B_SPLINE_SURFACE ( (
 ( 1.000000000000000000, 1.000000000000000000),
 ( 0.9934239774497837239, 0.8357310067453919133),
 ( 0.9934239774497837239, 0.8357310067453919133),
 ( 1.000000000000000000, 1.000000000000000000) ) ) 
 REPRESENTATION_ITEM ( '' )  SURFACE ( )  );
#22498=CARTESIAN_POINT ( 'NONE',  ( -1.049817751779873465, 37.35030165458175588, -26.50542916749582645 ) ) ;
#22499=CARTESIAN_POINT ( 'NONE',  ( -55.24340739397742084, 0.006539691034612836289, -0.007744344507854826129 ) ) ;
#22500=CARTESIAN_POINT ( 'NONE',  ( -4.162674018437130030, -18.33413805792406492, 45.34593312138898824 ) ) ;
#22502=CARTESIAN_POINT ( 'NONE',  ( -20.37983603106074071, -16.25728007463423808, -24.94323704205431369 ) ) ;
#22503=CARTESIAN_POINT ( 'NONE',  ( -55.24271866751342941, -0.008488649505342596782, -0.004256484107795601053 ) ) ;
#22508=CARTESIAN_POINT ( 'NONE',  ( -6.574463467970653063, -47.03022655117387529, 20.55340846381182018 ) ) ;
#22517=CARTESIAN_POINT ( 'NONE',  ( -1.259972190295300054, 16.33417789844434509, 43.01178231151312303 ) ) ;
#22524=VERTEX_POINT ( 'NONE', #4914 ) ;
#22528=B_SPLINE_CURVE_WITH_KNOTS ( 'NONE', 3,
 ( #646, #19938, #9437, #13303, #220, #7000 ),
 .UNSPECIFIED., .F., .F.,
 ( 4, 2, 4 ),
 ( 3.565531997320606436E-16, 0.003576372551511159629, 0.007152745103021962772 ),
 .UNSPECIFIED. ) ;
#22531=EDGE_CURVE ( 'NONE', #25702, #1293, #21479, .T. ) ;
#22534=LINE ( 'NONE', #20358, #24407 ) ;
#22535=EDGE_CURVE ( 'NONE', #1639, #6924, #1546, .T. ) ;
#22537=CARTESIAN_POINT ( 'NONE',  ( -1.019300379054419725, -25.26451264419615939, 38.21680004809191189 ) ) ;
#22538=CARTESIAN_POINT ( 'NONE',  ( -1.583189561560253589, 36.01941156322789084, -29.24830400313178558 ) ) ;
#22542=CIRCLE ( 'NONE', #15147, 34.60786435723138510 ) ;
#22543=DIRECTION ( 'NONE',  ( 1.000000000000000000, -6.938893903907226837E-18, 1.734723475976806709E-18 ) ) ;
#22550=CARTESIAN_POINT ( 'NONE',  ( -20.57838717382308147, 1.611677988432778319, 29.92853265176829325 ) ) ;
#22553=VERTEX_POINT ( 'NONE', #15693 ) ;
#22560=CARTESIAN_POINT ( 'NONE',  ( -1.464342487929867209, -16.57334911911542363, -43.13914623307952922 ) ) ;
#22566=CARTESIAN_POINT ( 'NONE',  ( -20.24399999263415495, -27.76448601145549233, -10.36954246768234889 ) ) ;
#22571=ORIENTED_EDGE ( 'NONE', *, *, #6738, .T. ) ;
#22574=( BOUNDED_SURFACE ( )  B_SPLINE_SURFACE ( 3, 1, ( 
 ( #9522, #20886 ),
 ( #5193, #13968 ),
 ( #18725, #2747 ),
 ( #27498, #1171 ) ),
 .UNSPECIFIED., .F., .F., .F. ) 
 B_SPLINE_SURFACE_WITH_KNOTS ( ( 4, 4 ),
 ( 2, 2 ),
 ( 0.000000000000000000, 1.000000000000000000 ),
 ( 0.000000000000000000, 1.000000000000000000 ),
 .UNSPECIFIED. ) 
 GEOMETRIC_REPRESENTATION_ITEM ( )  RATIONAL_B_SPLINE_SURFACE ( (
 ( 1.000000000000000000, 1.000000000000000000),
 ( 0.9934239774497838349, 0.8357310067453913582),
 ( 0.9934239774497838349, 0.8357310067453913582),
 ( 1.000000000000000000, 1.000000000000000000) ) ) 
 REPRESENTATION_ITEM ( '' )  SURFACE ( )  );
#22577=ORIENTED_EDGE ( 'NONE', *, *, #7766, .F. ) ;
#22587=CARTESIAN_POINT ( 'NONE',  ( -1.619063947482197729, -38.92136151114888776, 25.20140673341416360 ) ) ;
#22590=CARTESIAN_POINT ( 'NONE',  ( -7.733045908741315699, 52.15131830128827062, 5.980865481988326238 ) ) ;
#22597=CONICAL_SURFACE ( 'NONE', #27172, 34.60786435723138510, 0.8559913436420825139 ) ;
#22599=CARTESIAN_POINT ( 'NONE',  ( -25.21435515916043713, 15.02493970636190745, 31.17620025257570759 ) ) ;
#22607=EDGE_CURVE ( 'NONE', #26713, #6333, #20458, .T. ) ;
#22613=CARTESIAN_POINT ( 'NONE',  ( -20.21097721712958517, 28.05863618200121934, 9.464413111084452268 ) ) ;
#22620=CARTESIAN_POINT ( 'NONE',  ( -55.24390624410018802, 0.001811362924362862900, -0.01027195578988028025 ) ) ;
#22623=EDGE_LOOP ( 'NONE', ( #3306, #12422, #11430, #24834 ) ) ;
#22625=FACE_OUTER_BOUND ( 'NONE', #27323, .T. ) ;
#22626=CARTESIAN_POINT ( 'NONE',  ( -1.619063947482197729, 2.489035965910801895, 46.30105812165545842 ) ) ;
#22639=EDGE_LOOP ( 'NONE', ( #11294, #27803, #2484, #5839 ) ) ;
#22647=ADVANCED_FACE ( 'NONE', ( #19123 ), #625, .F. ) ;
#22653=CARTESIAN_POINT ( 'NONE',  ( -1.619063947482197729, -16.67502769180532596, 43.26576862488450104 ) ) ;
#22655=VECTOR ( 'NONE', #11331, 1000.000000000000114 ) ;
#22656=AXIS2_PLACEMENT_3D ( 'NONE', #10160, #7866, #23264 ) ;
#22659=FACE_OUTER_BOUND ( 'NONE', #27488, .T. ) ;
#22660=B_SPLINE_CURVE_WITH_KNOTS ( 'NONE', 3,
 ( #2574, #19707, #9363, #11220, #13361, #26469, #10942 ),
 .UNSPECIFIED., .F., .F.,
 ( 4, 3, 4 ),
 ( 1.734723475976807094E-18, 0.009512539173626382780, 0.02506242213020817150 ),
 .UNSPECIFIED. ) ;
#22676=CIRCLE ( 'NONE', #17583, 34.60786435723138510 ) ;
#22693=CARTESIAN_POINT ( 'NONE',  ( -1.050229599974477734, 27.12684363859256109, -36.90196321294305193 ) ) ;
#22700=CARTESIAN_POINT ( 'NONE',  ( -1.463510566862821660, 25.15876608740871490, 38.76366072687751796 ) ) ;
#22707=CARTESIAN_POINT ( 'NONE',  ( -21.41427618760457463, 16.60878262545457318, 25.94789270595488517 ) ) ;
#22710=CARTESIAN_POINT ( 'NONE',  ( -9.156249394959713683, 9.022661520477768704, -53.74753343182706544 ) ) ;
#22714=CARTESIAN_POINT ( 'NONE',  ( -9.156249394959706578, -38.17928057391962682, 38.89149400288449243 ) ) ;
#22718=CARTESIAN_POINT ( 'NONE',  ( -20.37983603106074426, -27.81368274044719868, -10.62371319148630455 ) ) ;
#22729=ORIENTED_EDGE ( 'NONE', *, *, #3156, .F. ) ;
#22743=CARTESIAN_POINT ( 'NONE',  ( -1.113548883309548376, -28.52482525634917820, 35.91246368318234516 ) ) ;
#22744=EDGE_CURVE ( 'NONE', #12412, #4347, #6057, .T. ) ;
#22746=CARTESIAN_POINT ( 'NONE',  ( -25.21435515916043713, -25.00736669481004526, 23.92354251275963861 ) ) ;
#22758=ORIENTED_EDGE ( 'NONE', *, *, #27490, .F. ) ;
#22760=ORIENTED_EDGE ( 'NONE', *, *, #5328, .T. ) ;
#22761=( BOUNDED_SURFACE ( )  B_SPLINE_SURFACE ( 3, 1, ( 
 ( #27824, #23383 ),
 ( #19050, #18907 ),
 ( #12694, #16892 ),
 ( #21342, #27534 ) ),
 .UNSPECIFIED., .F., .F., .F. ) 
 B_SPLINE_SURFACE_WITH_KNOTS ( ( 4, 4 ),
 ( 2, 2 ),
 ( 0.000000000000000000, 1.000000000000000000 ),
 ( 0.000000000000000000, 1.000000000000000000 ),
 .UNSPECIFIED. ) 
 GEOMETRIC_REPRESENTATION_ITEM ( )  RATIONAL_B_SPLINE_SURFACE ( (
 ( 1.000000000000000000, 1.000000000000000000),
 ( 0.7789835883360576307, 0.9689951854195403280),
 ( 0.7789835883360576307, 0.9689951854195403280),
 ( 1.000000000000000000, 1.000000000000000000) ) ) 
 REPRESENTATION_ITEM ( '' )  SURFACE ( )  );
#22764=CARTESIAN_POINT ( 'NONE',  ( -55.24340739397742084, 0.005344433640973447058, 0.008612749836246493332 ) ) ;
#22768=CARTESIAN_POINT ( 'NONE',  ( -15.02187109954780553, 33.49412687891621232, 32.04062513125082035 ) ) ;
#22780=CARTESIAN_POINT ( 'NONE',  ( -1.048996300304514850, -45.79145529752467070, 0.7649764263856586588 ) ) ;
#22782=CARTESIAN_POINT ( 'NONE',  ( -8.786685647604885574, 6.096987947571466530E-17, -1.524246986892866633E-17 ) ) ;
#22785=CARTESIAN_POINT ( 'NONE',  ( -2.265401668238145483, -36.42007794497270368, -29.73100299756553966 ) ) ;
#22795=CARTESIAN_POINT ( 'NONE',  ( 0.000000000000000000, 0.000000000000000000, 0.000000000000000000 ) ) ;
#22798=CARTESIAN_POINT ( 'NONE',  ( -4.162674018437144241, 25.90909455705170217, 41.48630000627025538 ) ) ;
#22815=EDGE_LOOP ( 'NONE', ( #7517, #2433, #22377, #24398 ) ) ;
#22820=ORIENTED_EDGE ( 'NONE', *, *, #10563, .F. ) ;
#22825=DIRECTION ( 'NONE',  ( 0.000000000000000000, 5.223019709708233256E-21, -1.000000000000000000 ) ) ;
#22838=EDGE_CURVE ( 'NONE', #9163, #25441, #7367, .T. ) ;
#22851=CARTESIAN_POINT ( 'NONE',  ( -1.583189561560252701, 43.29471907393764951, 16.68617981233657943 ) ) ;
#22855=B_SPLINE_CURVE_WITH_KNOTS ( 'NONE', 3,
 ( #16239, #409, #840, #7478 ),
 .UNSPECIFIED., .F., .F.,
 ( 4, 4 ),
 ( 1.906343156168368086E-16, 0.001982023823822943315 ),
 .UNSPECIFIED. ) ;
#22856=CARTESIAN_POINT ( 'NONE',  ( -55.24390624410018802, -0.001811362924359030029, -0.01027195578987783083 ) ) ;
#22870=ADVANCED_FACE ( 'NONE', ( #12762 ), #3567, .F. ) ;
#22873=CARTESIAN_POINT ( 'NONE',  ( -1.050229599974468409, -14.39582765040431944, 43.47850826583067629 ) ) ;
#22876=CARTESIAN_POINT ( 'NONE',  ( -8.786685647604890903, -37.00619870957961410, -38.68584556812286479 ) ) ;
#22881=CARTESIAN_POINT ( 'NONE',  ( -55.24300891470650754, 0.007734635432136952211, -0.006048736206179535120 ) ) ;
#22882=CARTESIAN_POINT ( 'NONE',  ( -16.86833981943424376, -43.82216161736207738, 5.948101187262031964 ) ) ;
#22887=CARTESIAN_POINT ( 'NONE',  ( -1.056502255334264895, -27.33667001641194361, -36.75727364034722200 ) ) ;
#22891=CARTESIAN_POINT ( 'NONE',  ( -4.780792508754314163, -32.07473752860752825, 37.74278713234433269 ) ) ;
#22892=CARTESIAN_POINT ( 'NONE',  ( -20.24419206586953379, 28.55732805495827265, 7.929973069813099684 ) ) ;
#22899=ORIENTED_EDGE ( 'NONE', *, *, #22744, .F. ) ;
#22915=B_SPLINE_CURVE_WITH_KNOTS ( 'NONE', 3,
 ( #15877, #24685, #2775, #26236, #15288, #2185 ),
 .UNSPECIFIED., .F., .F.,
 ( 4, 2, 4 ),
 ( 4.906538933386797396E-18, 0.0004335151646191519543, 0.0008670303292382989212 ),
 .UNSPECIFIED. ) ;
#22917=CARTESIAN_POINT ( 'NONE',  ( -9.156249394959706578, -24.29252099376457608, 48.78605533024762764 ) ) ;
#22921=CARTESIAN_POINT ( 'NONE',  ( -4.178947244162635855, 3.367451375481794074, 48.81675275154071869 ) ) ;
#22927=B_SPLINE_CURVE_WITH_KNOTS ( 'NONE', 3,
 ( #15054, #14926, #24146, #17647, #4131, #13180, #26017, #21837 ),
 .UNSPECIFIED., .F., .F.,
 ( 4, 2, 2, 4 ),
 ( 0.000000000000000000, 0.002761524886576596435, 0.005523049773153192871, 0.01104609954630638054 ),
 .UNSPECIFIED. ) ;
#22928=CARTESIAN_POINT ( 'NONE',  ( -1.031422197589716205, 1.530725436378091553, 45.78027046666442601 ) ) ;
#22930=CARTESIAN_POINT ( 'NONE',  ( -1.056502255334264895, 43.72121397317241787, 13.66916755949804951 ) ) ;
#22933=ORIENTED_EDGE ( 'NONE', *, *, #4502, .T. ) ;
#22934=ORIENTED_EDGE ( 'NONE', *, *, #9136, .F. ) ;
#22937=B_SPLINE_CURVE_WITH_KNOTS ( 'NONE', 3,
 ( #21763, #13114, #9, #21900, #10962, #17563, #26353, #6654 ),
 .UNSPECIFIED., .F., .F.,
 ( 4, 2, 2, 4 ),
 ( 0.000000000000000000, 0.002761524886576660620, 0.005523049773153321240, 0.01104609954630662513 ),
 .UNSPECIFIED. ) ;
#22941=CARTESIAN_POINT ( 'NONE',  ( -7.733045908741338792, -21.80378472388456501, 47.75066202881817645 ) ) ;
#22942=CARTESIAN_POINT ( 'NONE',  ( -6.588769196390763305, 26.02756986588603993, 44.25609997968876996 ) ) ;
#22952=DIRECTION ( 'NONE',  ( 1.000000000000000000, -6.938893903907226837E-18, 1.734723475976806709E-18 ) ) ;
#22954=CARTESIAN_POINT ( 'NONE',  ( -20.57838717382308147, -25.16001208503117326, -16.28767523336112433 ) ) ;
#22964=ORIENTED_EDGE ( 'NONE', *, *, #24716, .F. ) ;
#22966=ORIENTED_EDGE ( 'NONE', *, *, #20109, .T. ) ;
#22970=ORIENTED_EDGE ( 'NONE', *, *, #4383, .F. ) ;
#22971=CARTESIAN_POINT ( 'NONE',  ( -55.24340739397742084, -0.008612749836246226184, 0.005344433640972935315 ) ) ;
#22978=CARTESIAN_POINT ( 'NONE',  ( -1.045287976400362417, -1.530335034934427574, -45.76855895860943235 ) ) ;
#22983=VERTEX_POINT ( 'NONE', #25572 ) ;
#22989=ORIENTED_EDGE ( 'NONE', *, *, #4568, .T. ) ;
#22994=ORIENTED_EDGE ( 'NONE', *, *, #6675, .T. ) ;
#23000=DIRECTION ( 'NONE',  ( 0.7563875759206388771, 0.3556158456312978888, 0.5490129373055215867 ) ) ;
#23003=ADVANCED_FACE ( 'NONE', ( #12309 ), #10551, .F. ) ;
#23008=CARTESIAN_POINT ( 'NONE',  ( -20.20700224038492721, 29.58392382092673500, 0.9908225410479544193 ) ) ;
#23012=CARTESIAN_POINT ( 'NONE',  ( -1.049817751779881680, 43.71287583013727129, -13.66628317065001674 ) ) ;
#23013=CARTESIAN_POINT ( 'NONE',  ( -25.21435515916043713, -23.92354251275954979, -25.00736669481013053 ) ) ;
#23016=VERTEX_POINT ( 'NONE', #1518 ) ;
#23017=CARTESIAN_POINT ( 'NONE',  ( -8.786685647604890903, -23.24040270374424466, -48.22796981442760256 ) ) ;
#23021=CARTESIAN_POINT ( 'NONE',  ( -20.24419206586952313, -7.929973069813210707, 28.55732805495823712 ) ) ;
#23027=CARTESIAN_POINT ( 'NONE',  ( -8.786685647604890903, -37.00619870957961410, -38.68584556812286479 ) ) ;
#23030=AXIS2_PLACEMENT_3D ( 'NONE', #4528, #26545, #21817 ) ;
#23031=CARTESIAN_POINT ( 'NONE',  ( -55.24390624410018802, 0.004572280736703349113, -0.009374879212967143077 ) ) ;
#23038=CONICAL_SURFACE ( 'NONE', #20705, 34.60786435723138510, 0.8559913436420825139 ) ;
#23043=EDGE_LOOP ( 'NONE', ( #17460, #6347, #23638, #9420 ) ) ;
#23045=ADVANCED_FACE ( 'NONE', ( #10175 ), #19362, .F. ) ;
#23053=CARTESIAN_POINT ( 'NONE',  ( -1.031422197589711764, 43.06660437151329290, 15.60268798220593034 ) ) ;
#23058=CARTESIAN_POINT ( 'NONE',  ( -55.24390624410018802, -0.004896917417127438256, -0.009209468562451287102 ) ) ;
#23066=ORIENTED_EDGE ( 'NONE', *, *, #21518, .F. ) ;
#23073=ORIENTED_EDGE ( 'NONE', *, *, #24837, .F. ) ;
#23076=CARTESIAN_POINT ( 'NONE',  ( -20.57838717382308147, 18.89542499756533545, 23.26537097894084383 ) ) ;
#23080=EDGE_CURVE ( 'NONE', #10456, #22401, #21786, .T. ) ;
#23081=ORIENTED_EDGE ( 'NONE', *, *, #12959, .F. ) ;
#23103=VERTEX_POINT ( 'NONE', #6698 ) ;
#23106=EDGE_LOOP ( 'NONE', ( #25716, #5055, #12034, #4988 ) ) ;
#23108=CARTESIAN_POINT ( 'NONE',  ( -1.050231094221210748, 27.12595454131558981, 36.90262059116437854 ) ) ;
#23109=VERTEX_POINT ( 'NONE', #21804 ) ;
#23112=VECTOR ( 'NONE', #19104, 999.9999999999998863 ) ;
#23117=DIRECTION ( 'NONE',  ( 0.000000000000000000, 5.223019709707975211E-21, -1.000000000000000000 ) ) ;
#23128=CARTESIAN_POINT ( 'NONE',  ( -1.050231094221210526, -26.71409683968590798, 37.20185272688488709 ) ) ;
#23129=EDGE_CURVE ( 'NONE', #22983, #607, #26919, .T. ) ;
#23131=CARTESIAN_POINT ( 'NONE',  ( -1.058197053496154671, 25.48582931365525184, 38.06270006878825995 ) ) ;
#23132=CARTESIAN_POINT ( 'NONE',  ( -8.259864102781671491, -22.52209142944967368, -47.98931516265586339 ) ) ;
#23137=CARTESIAN_POINT ( 'NONE',  ( -4.162674018437135359, -25.90909455705140729, -41.48630000627045433 ) ) ;
#23139=EDGE_CURVE ( 'NONE', #24558, #15270, #8729, .T. ) ;
#23141=CARTESIAN_POINT ( 'NONE',  ( -1.056502255334264895, 27.33667001641221717, 36.75727364034702305 ) ) ;
#23146=VERTEX_POINT ( 'NONE', #4190 ) ;
#23150=CARTESIAN_POINT ( 'NONE',  ( -20.38016308990357928, 7.753479680700950283, -28.74660391518346714 ) ) ;
#23157=LINE ( 'NONE', #25726, #6955 ) ;
#23158=CARTESIAN_POINT ( 'NONE',  ( -20.20612091757419648, 29.57813639663782013, 1.137293889216468790 ) ) ;
#23170=CARTESIAN_POINT ( 'NONE',  ( -25.21435515916043713, -31.17620025257576799, 15.02493970636179377 ) ) ;
#23172=CARTESIAN_POINT ( 'NONE',  ( -1.619063947482197729, -38.92136151114888776, 25.20140673341416360 ) ) ;
#23174=CARTESIAN_POINT ( 'NONE',  ( -23.79223135445719350, 30.42557260166829636, 13.25822371132262845 ) ) ;
#23177=CARTESIAN_POINT ( 'NONE',  ( -55.24271866751342941, 0.008488649505343330570, 0.004256484107795472684 ) ) ;
#23186=VERTEX_POINT ( 'NONE', #10827 ) ;
#23187=CARTESIAN_POINT ( 'NONE',  ( -4.473127245936434626, -49.22197550883367256, 3.196405119334318812 ) ) ;
#23199=CARTESIAN_POINT ( 'NONE',  ( -6.574463467970653952, 38.37705091668375701, -34.08059230520056104 ) ) ;
#23205=ADVANCED_FACE ( 'NONE', ( #19724 ), #17334, .F. ) ;
#23211=ORIENTED_EDGE ( 'NONE', *, *, #15957, .F. ) ;
#23221=CARTESIAN_POINT ( 'NONE',  ( -8.786685647604896232, -7.199674155858612146, 53.04920435127190359 ) ) ;
#23222=VERTEX_POINT ( 'NONE', #27046 ) ;
#23229=DIRECTION ( 'NONE',  ( -0.7637818620346801257, 0.6068965246771014233, -0.2198041754873946707 ) ) ;
#23230=( BOUNDED_SURFACE ( )  B_SPLINE_SURFACE ( 3, 1, ( 
 ( #9463, #7307 ),
 ( #963, #20097 ),
 ( #26861, #383 ),
 ( #816, #15784 ) ),
 .UNSPECIFIED., .F., .F., .F. ) 
 B_SPLINE_SURFACE_WITH_KNOTS ( ( 4, 4 ),
 ( 2, 2 ),
 ( 0.000000000000000000, 1.000000000000000000 ),
 ( 0.000000000000000000, 1.000000000000000000 ),
 .UNSPECIFIED. ) 
 GEOMETRIC_REPRESENTATION_ITEM ( )  RATIONAL_B_SPLINE_SURFACE ( (
 ( 1.000000000000000000, 1.000000000000000000),
 ( 0.9934239774497838349, 0.8357310067453913582),
 ( 0.9934239774497838349, 0.8357310067453913582),
 ( 1.000000000000000000, 1.000000000000000000) ) ) 
 REPRESENTATION_ITEM ( '' )  SURFACE ( )  );
#23232=CARTESIAN_POINT ( 'NONE',  ( -16.86833981943421890, -43.51541671545732015, -7.884812276281936150 ) ) ;
#23240=CARTESIAN_POINT ( 'NONE',  ( -4.473127245936431073, 47.80062405537802306, -12.17046501147532567 ) ) ;
#23241=CARTESIAN_POINT ( 'NONE',  ( -1.323830074806760848, -2.318057800980394045, 46.01435746200695576 ) ) ;
#23242=DIRECTION ( 'NONE',  ( 0.000000000000000000, 5.223019709707975211E-21, -1.000000000000000000 ) ) ;
#23243=B_SPLINE_CURVE_WITH_KNOTS ( 'NONE', 3,
 ( #27154, #11200, #25595, #5287, #5874, #14492, #5578, #8047, #23012, #7615, #12200, #16939, #10344 ),
 .UNSPECIFIED., .F., .F.,
 ( 4, 3, 3, 3, 4 ),
 ( 8.673617379884035472E-18, 0.0007657099931970570922, 0.001531419946797920890, 0.002296279302920155134, 0.003061450627205761568 ),
 .UNSPECIFIED. ) ;
#23262=CARTESIAN_POINT ( 'NONE',  ( -20.21097721712958872, 8.835581498567860237, 28.26295595852175779 ) ) ;
#23264=DIRECTION ( 'NONE',  ( 0.000000000000000000, 5.223019709708233256E-21, -1.000000000000000000 ) ) ;
#23274=ORIENTED_EDGE ( 'NONE', *, *, #2874, .T. ) ;
#23277=VERTEX_POINT ( 'NONE', #22626 ) ;
#23279=CARTESIAN_POINT ( 'NONE',  ( -6.574463467970653952, -50.12924290857544918, -11.01561683920031776 ) ) ;
#23281=EDGE_LOOP ( 'NONE', ( #23073, #25222, #21134, #12930 ) ) ;
#23282=EDGE_CURVE ( 'NONE', #3864, #26104, #27282, .T. ) ;
#23283=ORIENTED_EDGE ( 'NONE', *, *, #9716, .F. ) ;
#23285=EDGE_CURVE ( 'NONE', #2580, #15497, #19382, .T. ) ;
#23288=EDGE_CURVE ( 'NONE', #15570, #8163, #9812, .T. ) ;
#23292=CARTESIAN_POINT ( 'NONE',  ( -20.47566262905010248, 29.82700878811083811, 1.586617686065662447 ) ) ;
#23295=CARTESIAN_POINT ( 'NONE',  ( -1.048172774974269084, -13.17853518375268074, 43.86067135048633503 ) ) ;
#23297=CARTESIAN_POINT ( 'NONE',  ( -1.323439229708141207, -46.01398008004442630, 2.317790194800218195 ) ) ;
#23301=VERTEX_POINT ( 'NONE', #8088 ) ;
#23302=CARTESIAN_POINT ( 'NONE',  ( -20.90916690077960638, 7.054312691028996163, -38.93431874629079203 ) ) ;
#23310=CARTESIAN_POINT ( 'NONE',  ( -1.539763995773687499, -29.16712963492436828, 35.94321074656927095 ) ) ;
#23331=CARTESIAN_POINT ( 'NONE',  ( -8.786685647604890903, -48.22796981442785835, -23.24040270374372952 ) ) ;
#23332=ADVANCED_FACE ( 'NONE', ( #1584 ), #18446, .F. ) ;
#23333=CARTESIAN_POINT ( 'NONE',  ( -6.588769196390770411, 50.13301368233300082, -11.07780292579711556 ) ) ;
#23335=CARTESIAN_POINT ( 'NONE',  ( -21.41430102051751660, -11.22990201072297012, -28.68859753627389253 ) ) ;
#23344=DIRECTION ( 'NONE',  ( -0.7637818620346800147, -0.6451161201712181104, 0.02150485345384613861 ) ) ;
#23364=EDGE_CURVE ( 'NONE', #25194, #6927, #21742, .T. ) ;
#23372=CARTESIAN_POINT ( 'NONE',  ( -1.019300379054419947, 12.21833869579527310, 44.15350047934384747 ) ) ;
#23373=CARTESIAN_POINT ( 'NONE',  ( -1.058473599757816297, 45.77379534793244886, -1.755404039369589997 ) ) ;
#23374=CARTESIAN_POINT ( 'NONE',  ( -12.82751273423882665, 48.09651489336691554, 8.715310691359739792 ) ) ;
#23377=B_SPLINE_CURVE_WITH_KNOTS ( 'NONE', 3,
 ( #15410, #26499, #17721, #26926, #6951, #24221 ),
 .UNSPECIFIED., .F., .F.,
 ( 4, 2, 4 ),
 ( 1.550807859811640467E-16, 0.003570751334075634390, 0.007141502668151113523 ),
 .UNSPECIFIED. ) ;
#23383=CARTESIAN_POINT ( 'NONE',  ( -1.583189561560253589, 43.29471907393742214, -16.68617981233717629 ) ) ;
#23387=( BOUNDED_SURFACE ( )  B_SPLINE_SURFACE ( 3, 1, ( 
 ( #22423, #2541 ),
 ( #11191, #4421 ),
 ( #2246, #19818 ),
 ( #107, #22130 ) ),
 .UNSPECIFIED., .F., .F., .F. ) 
 B_SPLINE_SURFACE_WITH_KNOTS ( ( 4, 4 ),
 ( 2, 2 ),
 ( 0.000000000000000000, 1.000000000000000000 ),
 ( 0.000000000000000000, 1.000000000000000000 ),
 .UNSPECIFIED. ) 
 GEOMETRIC_REPRESENTATION_ITEM ( )  RATIONAL_B_SPLINE_SURFACE ( (
 ( 1.000000000000000000, 1.000000000000000000),
 ( 0.7789835883360578528, 0.9689951854195403280),
 ( 0.7789835883360578528, 0.9689951854195403280),
 ( 1.000000000000000000, 1.000000000000000000) ) ) 
 REPRESENTATION_ITEM ( '' )  SURFACE ( )  );
#23388=CARTESIAN_POINT ( 'NONE',  ( -1.046935749539996907, 25.87617179820970748, 37.78548154587966934 ) ) ;
#23395=CARTESIAN_POINT ( 'NONE',  ( -21.41430102051744910, 7.777552968935758315, -29.81033373822130628 ) ) ;
#23396=CARTESIAN_POINT ( 'NONE',  ( -55.24271866751342941, 0.001425019990782615698, -0.009388511352197861579 ) ) ;
#23397=DIRECTION ( 'NONE',  ( 0.7563875759206388771, -0.6104009704506944134, -0.2351350468682844030 ) ) ;
#23400=CARTESIAN_POINT ( 'NONE',  ( -1.050230346682673677, -14.15203301556463167, -43.55772679531845881 ) ) ;
#23403=VERTEX_POINT ( 'NONE', #10929 ) ;
#23416=EDGE_CURVE ( 'NONE', #14330, #1523, #2136, .T. ) ;
#23420=EDGE_CURVE ( 'NONE', #13048, #14557, #28241, .T. ) ;
#23433=AXIS2_PLACEMENT_3D ( 'NONE', #27454, #1400, #12207 ) ;
#23434=CARTESIAN_POINT ( 'NONE',  ( -20.57838717382308147, -1.611677988432568709, -29.92853265176830746 ) ) ;
#23446=ORIENTED_EDGE ( 'NONE', *, *, #14979, .F. ) ;
#23454=B_SPLINE_CURVE_WITH_KNOTS ( 'NONE', 3,
 ( #4458, #4599, #19716, #17416, #11230, #24338, #4326, #21890 ),
 .UNSPECIFIED., .F., .F.,
 ( 4, 2, 2, 4 ),
 ( 2.194186273941487449E-16, 0.002761568181852863766, 0.005523136363705508090, 0.01104627272741078893 ),
 .UNSPECIFIED. ) ;
#23455=CARTESIAN_POINT ( 'NONE',  ( -8.786685647604894456, 37.00619870957989832, 38.68584556812258768 ) ) ;
#23459=EDGE_CURVE ( 'NONE', #21625, #13254, #7309, .T. ) ;
#23465=ORIENTED_EDGE ( 'NONE', *, *, #3537, .F. ) ;
#23466=CARTESIAN_POINT ( 'NONE',  ( -20.57838717382308147, -18.89542499756482741, 23.26537097894125594 ) ) ;
#23469=DIRECTION ( 'NONE',  ( -0.7563875759206388771, 0.3556158456312860094, -0.5490129373055293582 ) ) ;
#23473=( BOUNDED_SURFACE ( )  B_SPLINE_SURFACE ( 3, 1, ( 
 ( #2394, #11192 ),
 ( #13626, #19966 ),
 ( #24445, #4711 ),
 ( #12191, #1244 ) ),
 .UNSPECIFIED., .F., .F., .F. ) 
 B_SPLINE_SURFACE_WITH_KNOTS ( ( 4, 4 ),
 ( 2, 2 ),
 ( 0.000000000000000000, 1.000000000000000000 ),
 ( 0.000000000000000000, 1.000000000000000000 ),
 .UNSPECIFIED. ) 
 GEOMETRIC_REPRESENTATION_ITEM ( )  RATIONAL_B_SPLINE_SURFACE ( (
 ( 1.000000000000000000, 1.000000000000000000),
 ( 0.7789835883360578528, 0.9689951854195403280),
 ( 0.7789835883360578528, 0.9689951854195403280),
 ( 1.000000000000000000, 1.000000000000000000) ) ) 
 REPRESENTATION_ITEM ( '' )  SURFACE ( )  );
#23479=CARTESIAN_POINT ( 'NONE',  ( -1.045287976400351981, 43.05558670614237116, -15.59869763335110449 ) ) ;
#23485=CARTESIAN_POINT ( 'NONE',  ( -55.24271866751342941, 0.008433070970614256479, -0.004365563123935527895 ) ) ;
#23502=CIRCLE ( 'NONE', #4601, 34.60786435723138510 ) ;
#23513=CARTESIAN_POINT ( 'NONE',  ( -8.786685647604896232, -7.199674155858612146, 53.04920435127190359 ) ) ;
#23516=AXIS2_PLACEMENT_3D ( 'NONE', #13248, #19729, #21905 ) ;
#23520=VECTOR ( 'NONE', #23827, 1000.000000000000000 ) ;
#23521=CARTESIAN_POINT ( 'NONE',  ( -9.156249394959706578, -8.027840202793560920, 53.90509764945136340 ) ) ;
#23523=CARTESIAN_POINT ( 'NONE',  ( -20.20700224038492365, 23.35150625415685255, 18.19058640100197977 ) ) ;
#23526=ORIENTED_EDGE ( 'NONE', *, *, #24837, .T. ) ;
#23534=ORIENTED_EDGE ( 'NONE', *, *, #23416, .F. ) ;
#23535=CARTESIAN_POINT ( 'NONE',  ( -1.046936909428682672, 43.93225665392633061, 12.93351869073227611 ) ) ;
#23546=CARTESIAN_POINT ( 'NONE',  ( -1.048996300304503082, -26.29666317565274980, 37.49570739463913327 ) ) ;
#23553=ORIENTED_EDGE ( 'NONE', *, *, #9861, .F. ) ;
#23556=EDGE_CURVE ( 'NONE', #2493, #8511, #5003, .T. ) ;
#23561=EDGE_CURVE ( 'NONE', #25702, #607, #17807, .T. ) ;
#23562=CARTESIAN_POINT ( 'NONE',  ( 14.74894986621300319, -1.023413983156987147E-16, 2.558534957892467869E-17 ) ) ;
#23590=CARTESIAN_POINT ( 'NONE',  ( -19.53423201713129842, 1.355459634611817431E-16, -3.388649086529543578E-17 ) ) ;
#23596=VERTEX_POINT ( 'NONE', #22439 ) ;
#23598=CARTESIAN_POINT ( 'NONE',  ( -1.058197053496177764, -44.07533330186778642, 12.47644286888561105 ) ) ;
#23605=ORIENTED_EDGE ( 'NONE', *, *, #20535, .F. ) ;
#23610=VERTEX_POINT ( 'NONE', #2706 ) ;
#23613=VERTEX_POINT ( 'NONE', #549 ) ;
#23616=CARTESIAN_POINT ( 'NONE',  ( -18.41936578851709783, -20.09935324538221479, -37.37524689996187277 ) ) ;
#23625=DIRECTION ( 'NONE',  ( -0.7563875759206388771, 0.6320336713238511317, 0.1685564395263317583 ) ) ;
#23627=ORIENTED_EDGE ( 'NONE', *, *, #25516, .T. ) ;
#23633=DIRECTION ( 'NONE',  ( 0.000000000000000000, 5.223019709707975211E-21, -1.000000000000000000 ) ) ;
#23638=ORIENTED_EDGE ( 'NONE', *, *, #18153, .F. ) ;
#23640=DIRECTION ( 'NONE',  ( -1.000000000000000000, 6.938893903907226837E-18, -1.734723475976806709E-18 ) ) ;
#23663=CARTESIAN_POINT ( 'NONE',  ( -19.53423201713129842, 1.353948732986041533E-16, 28.92774122539760384 ) ) ;
#23666=CARTESIAN_POINT ( 'NONE',  ( -25.21435515916043713, 15.02493970636190745, 31.17620025257570759 ) ) ;
#23670=CARTESIAN_POINT ( 'NONE',  ( -1.583189561560252701, -2.490696082059551397, 46.33203782964464068 ) ) ;
#23674=ORIENTED_EDGE ( 'NONE', *, *, #3907, .T. ) ;
#23679=EDGE_CURVE ( 'NONE', #17615, #4550, #21058, .T. ) ;
#23682=CARTESIAN_POINT ( 'NONE',  ( -1.045287976400365970, 44.00138577190666922, 12.68782741917247670 ) ) ;
#23689=ADVANCED_FACE ( 'NONE', ( #5294 ), #26331, .T. ) ;
#23690=CARTESIAN_POINT ( 'NONE',  ( -20.20997486282892552, 0.3303599360442536770, 29.60348406988233450 ) ) ;
#23695=CARTESIAN_POINT ( 'NONE',  ( -8.786685647604885574, 6.096987947571466530E-17, -1.524246986892866633E-17 ) ) ;
#23696=ORIENTED_EDGE ( 'NONE', *, *, #20949, .T. ) ;
#23710=CARTESIAN_POINT ( 'NONE',  ( -8.786685647604890903, -52.67761315067293282, -9.545808661480407409 ) ) ;
#23712=ORIENTED_EDGE ( 'NONE', *, *, #5648, .F. ) ;
#23715=CARTESIAN_POINT ( 'NONE',  ( -1.058197053496163109, 1.754224732379551011, -45.77356582045591438 ) ) ;
#23716=ADVANCED_FACE ( 'NONE', ( #25601 ), #28022, .F. ) ;
#23722=B_SPLINE_CURVE_WITH_KNOTS ( 'NONE', 3,
 ( #13811, #5181, #15676, #9803, #20438, #3033, #27039 ),
 .UNSPECIFIED., .F., .F.,
 ( 4, 3, 4 ),
 ( 3.469446951953614189E-18, 0.009512539173626420944, 0.02506242213020843865 ),
 .UNSPECIFIED. ) ;
#23724=FACE_OUTER_BOUND ( 'NONE', #13435, .T. ) ;
#23731=CARTESIAN_POINT ( 'NONE',  ( -20.57838717382308147, 1.611677988432778319, 29.92853265176829325 ) ) ;
#23732=DIRECTION ( 'NONE',  ( -0.7563875759206388771, -0.1685564395263341175, 0.6320336713238504656 ) ) ;
#23738=CARTESIAN_POINT ( 'NONE',  ( -8.786685647604885574, 6.096987947571466530E-17, -1.524246986892866633E-17 ) ) ;
#23743=CARTESIAN_POINT ( 'NONE',  ( -1.019300379054419947, 2.023851374322675589, -45.76814864815091255 ) ) ;
#23749=CARTESIAN_POINT ( 'NONE',  ( -7.078251931573406708, -51.82710018979472721, 5.101176922831208493 ) ) ;
#23758=CARTESIAN_POINT ( 'NONE',  ( -12.94347594948482971, 47.96504705787755540, -8.691477019903484091 ) ) ;
#23773=CARTESIAN_POINT ( 'NONE',  ( -20.24399999263414784, -28.55700515887714275, 7.930419334766489747 ) ) ;
#23776=CARTESIAN_POINT ( 'NONE',  ( -25.21435515916025594, 1.749597353048488237E-16, -4.373993382621220594E-17 ) ) ;
#23784=DIRECTION ( 'NONE',  ( -0.7637818620346801257, 0.5092696688508612235, -0.3965875333584896190 ) ) ;
#23787=DIRECTION ( 'NONE',  ( -0.7071067818211357325, 9.150583771627653840E-17, -0.7071067805519594129 ) ) ;
#23788=ORIENTED_EDGE ( 'NONE', *, *, #17702, .F. ) ;
#23802=CARTESIAN_POINT ( 'NONE',  ( -16.86833981943423666, 43.51541671545732726, 7.884812276281646604 ) ) ;
#23803=CARTESIAN_POINT ( 'NONE',  ( -1.031422197589716205, 37.93675465142509751, 25.67058493451402157 ) ) ;
#23827=DIRECTION ( 'NONE',  ( 0.7637818620346801257, -0.02150485345383945993, 0.6451161201712183324 ) ) ;
#23831=CARTESIAN_POINT ( 'NONE',  ( -55.24271866751342941, -0.001545935011626541761, -0.009369360294294543784 ) ) ;
#23836=CARTESIAN_POINT ( 'NONE',  ( -6.574463467970643293, 11.01561683920051848, -50.12924290857540655 ) ) ;
#23843=EDGE_CURVE ( 'NONE', #9585, #18375, #10609, .T. ) ;
#23845=ORIENTED_EDGE ( 'NONE', *, *, #12234, .T. ) ;
#23848=ORIENTED_EDGE ( 'NONE', *, *, #10741, .F. ) ;
#23850=VECTOR ( 'NONE', #11228, 1000.000000000000114 ) ;
#23855=CARTESIAN_POINT ( 'NONE',  ( -24.53239521893651442, -14.09666242510773948, 30.86654523348680002 ) ) ;
#23856=CARTESIAN_POINT ( 'NONE',  ( -1.113427685307002424, -38.22586258295212502, -25.34053733836516642 ) ) ;
#23858=B_SPLINE_CURVE_WITH_KNOTS ( 'NONE', 3,
 ( #4250, #26131, #11024, #10599, #10466, #25996, #8445, #6288, #15038, #23860, #4109, #17342, #2960 ),
 .UNSPECIFIED., .F., .F.,
 ( 4, 3, 3, 3, 4 ),
 ( 8.673617379884035472E-18, 0.0007657099931970526470, 0.001531419946797914385, 0.002296279302920149496, 0.003061450627205760701 ),
 .UNSPECIFIED. ) ;
#23860=CARTESIAN_POINT ( 'NONE',  ( -1.048994561756806831, 14.87838255483256233, -43.31369460697981566 ) ) ;
#23877=CARTESIAN_POINT ( 'NONE',  ( -1.031422197589711764, -37.93675465142452907, 25.67058493451483514 ) ) ;
#23878=CARTESIAN_POINT ( 'NONE',  ( -55.25719721206881729, 0.002847566758684554142, 0.01079965405819473083 ) ) ;
#23891=CARTESIAN_POINT ( 'NONE',  ( -1.050231094221214079, 37.20185272688497236, 26.71409683968576942 ) ) ;
#23894=CARTESIAN_POINT ( 'NONE',  ( -55.24340739397742794, 0.009386184976285603249, -0.003826481709800144074 ) ) ;
#23910=ORIENTED_EDGE ( 'NONE', *, *, #11989, .F. ) ;
#23916=ORIENTED_EDGE ( 'NONE', *, *, #6903, .F. ) ;
#23925=CARTESIAN_POINT ( 'NONE',  ( -1.031422197589711764, -36.13727897780146492, -28.14735071801730726 ) ) ;
#23932=CARTESIAN_POINT ( 'NONE',  ( -25.21435515916025594, 1.749597353048488237E-16, -4.373993382621220594E-17 ) ) ;
#23935=FACE_OUTER_BOUND ( 'NONE', #25374, .T. ) ;
#23946=CARTESIAN_POINT ( 'NONE',  ( -21.41427618760458884, -28.68857606049974862, -11.22988868156173581 ) ) ;
#23949=EDGE_LOOP ( 'NONE', ( #6451, #10556, #13598, #15180 ) ) ;
#23957=AXIS2_PLACEMENT_3D ( 'NONE', #2789, #635, #7130 ) ;
#23966=VECTOR ( 'NONE', #9051, 1000.000000000000114 ) ;
#23970=CARTESIAN_POINT ( 'NONE',  ( -18.41936578851709783, -29.33493038358050242, 30.66520733838684265 ) ) ;
#23972=CARTESIAN_POINT ( 'NONE',  ( -2.904412668506660467, 11.97478724945576545, 46.12477647685262383 ) ) ;
#23976=ORIENTED_EDGE ( 'NONE', *, *, #9136, .T. ) ;
#23977=CARTESIAN_POINT ( 'NONE',  ( -8.259864102781671491, 9.986657004933631399, -52.06232470801713674 ) ) ;
#23979=CARTESIAN_POINT ( 'NONE',  ( -1.048171036023496594, -36.44209502233728415, -27.73816396939552931 ) ) ;
#23982=CARTESIAN_POINT ( 'NONE',  ( -1.113548883309551929, -16.03115934825500588, 42.96943836789122173 ) ) ;
#23986=CONICAL_SURFACE ( 'NONE', #17520, 28.92774122539760384, 0.7853981625000054922 ) ;
#23989=AXIS2_PLACEMENT_3D ( 'NONE', #14749, #14608, #3527 ) ;
#23996=ORIENTED_EDGE ( 'NONE', *, *, #1496, .T. ) ;
#24002=ORIENTED_EDGE ( 'NONE', *, *, #11273, .F. ) ;
#24003=ORIENTED_EDGE ( 'NONE', *, *, #11580, .T. ) ;
#24008=CARTESIAN_POINT ( 'NONE',  ( -18.41936578851713335, 20.09935324538248480, 37.37524689996173777 ) ) ;
#24012=EDGE_LOOP ( 'NONE', ( #18697, #3120, #23526, #7151 ) ) ;
#24017=CARTESIAN_POINT ( 'NONE',  ( -8.786685647604720373, -47.14957014837338534, -25.35688121747513435 ) ) ;
#24018=ORIENTED_EDGE ( 'NONE', *, *, #18823, .T. ) ;
#24021=CARTESIAN_POINT ( 'NONE',  ( -1.539763995773691940, 46.22267697748604576, 2.469814354917652999 ) ) ;
#24029=FACE_OUTER_BOUND ( 'NONE', #1066, .T. ) ;
#24035=CARTESIAN_POINT ( 'NONE',  ( -12.82751273423880178, -23.15139349681279057, 43.04932478553559605 ) ) ;
#24041=ORIENTED_EDGE ( 'NONE', *, *, #12230, .F. ) ;
#24044=CARTESIAN_POINT ( 'NONE',  ( -16.86833981943427574, 39.83928801320588775, -19.19877306373863490 ) ) ;
#24064=CARTESIAN_POINT ( 'NONE',  ( -25.21435515916042647, 15.02493970636146692, -31.17620025257592786 ) ) ;
#24069=CARTESIAN_POINT ( 'NONE',  ( -4.162674018437135359, 31.44946543094296487, -37.46098494546600932 ) ) ;
#24070=EDGE_CURVE ( 'NONE', #7819, #1487, #9659, .T. ) ;
#24073=EDGE_CURVE ( 'NONE', #17580, #27461, #9892, .T. ) ;
#24077=DIRECTION ( 'NONE',  ( 0.000000000000000000, 5.223019709707975211E-21, -1.000000000000000000 ) ) ;
#24078=CARTESIAN_POINT ( 'NONE',  ( -1.539760825549682632, -11.93465943778483584, 44.72358953107743673 ) ) ;
#24080=CARTESIAN_POINT ( 'NONE',  ( -20.24419206586952669, 18.44224248888906814, 23.20105925399704461 ) ) ;
#24087=ORIENTED_EDGE ( 'NONE', *, *, #18923, .F. ) ;
#24108=CARTESIAN_POINT ( 'NONE',  ( -23.79223135445719706, 7.157574570129600744, 32.40779366744824586 ) ) ;
#24110=CARTESIAN_POINT ( 'NONE',  ( -9.156249394959713683, 38.17928057392048657, 38.89149400288364689 ) ) ;
#24112=CARTESIAN_POINT ( 'NONE',  ( -6.574463467970651287, -34.08059230520071736, -38.37705091668365043 ) ) ;
#24113=VERTEX_POINT ( 'NONE', #14958 ) ;
#24114=CARTESIAN_POINT ( 'NONE',  ( -55.25719721206881729, 0.01115102788683056123, 0.0006290797159205457727 ) ) ;
#24116=CARTESIAN_POINT ( 'NONE',  ( -1.050229599974486616, -36.90196321294315140, -27.12684363859242254 ) ) ;
#24123=CARTESIAN_POINT ( 'NONE',  ( -20.57838717382308147, 10.78122205917000365, -27.96569011373090063 ) ) ;
#24125=EDGE_CURVE ( 'NONE', #5967, #3087, #19166, .T. ) ;
#24133=( BOUNDED_SURFACE ( )  B_SPLINE_SURFACE ( 3, 1, ( 
 ( #28253, #21506 ),
 ( #1779, #2057 ),
 ( #10576, #15016 ),
 ( #15293, #24110 ) ),
 .UNSPECIFIED., .F., .F., .F. ) 
 B_SPLINE_SURFACE_WITH_KNOTS ( ( 4, 4 ),
 ( 2, 2 ),
 ( 0.000000000000000000, 1.000000000000000000 ),
 ( 0.000000000000000000, 1.000000000000000000 ),
 .UNSPECIFIED. ) 
 GEOMETRIC_REPRESENTATION_ITEM ( )  RATIONAL_B_SPLINE_SURFACE ( (
 ( 1.000000000000000000, 1.000000000000000000),
 ( 0.7789835883360576307, 0.9689951854195403280),
 ( 0.7789835883360576307, 0.9689951854195403280),
 ( 1.000000000000000000, 1.000000000000000000) ) ) 
 REPRESENTATION_ITEM ( '' )  SURFACE ( )  );
#24135=CARTESIAN_POINT ( 'NONE',  ( -19.53423201713129842, 1.550869255229030165E-16, 28.92774122539760384 ) ) ;
#24136=CARTESIAN_POINT ( 'NONE',  ( -28.41354790283022069, 8.345538364877077342, -21.64275480268750940 ) ) ;
#24146=CARTESIAN_POINT ( 'NONE',  ( -7.711401346138264223, -38.61705198405337569, 35.51061203065550131 ) ) ;
#24150=CARTESIAN_POINT ( 'NONE',  ( -55.25297051322618813, -0.01093108995494780980, 0.01019003092403480623 ) ) ;
#24164=CARTESIAN_POINT ( 'NONE',  ( -8.786685647604706162, -38.68584556812290032, 37.00619870957955015 ) ) ;
#24181=CARTESIAN_POINT ( 'NONE',  ( -20.24399999263414784, 1.282322917263463813, -29.60996018918694617 ) ) ;
#24205=CARTESIAN_POINT ( 'NONE',  ( -4.162674018437137136, 45.34593312138912324, 18.33413805792392992 ) ) ;
#24207=CARTESIAN_POINT ( 'NONE',  ( -1.045287976400365970, -25.66401692419961833, 37.92705037016786918 ) ) ;
#24217=CARTESIAN_POINT ( 'NONE',  ( -1.045287976400365970, 44.00138577190666922, 12.68782741917247670 ) ) ;
#24219=ORIENTED_EDGE ( 'NONE', *, *, #27770, .T. ) ;
#24221=CARTESIAN_POINT ( 'NONE',  ( -25.21435515916042647, 25.00736669481023355, -23.92354251275945742 ) ) ;
#24223=CARTESIAN_POINT ( 'NONE',  ( -1.045287976400365970, 45.76855895860946077, 1.530335034933974381 ) ) ;
#24226=EDGE_LOOP ( 'NONE', ( #22577, #1916, #16359, #22966 ) ) ;
#24235=CARTESIAN_POINT ( 'NONE',  ( -20.20700224038492010, -16.58740185276728241, -24.51628800869040958 ) ) ;
#24236=CARTESIAN_POINT ( 'NONE',  ( -1.239374126674604337, 25.08410696974298304, 38.61989855450910625 ) ) ;
#24240=CARTESIAN_POINT ( 'NONE',  ( -1.464342487929860992, 11.94843286121917814, -44.64187261869783896 ) ) ;
#24244=ORIENTED_EDGE ( 'NONE', *, *, #7854, .T. ) ;
#24245=CARTESIAN_POINT ( 'NONE',  ( -20.57838717382308147, 7.715628353034087894, 28.96176188950209962 ) ) ;
#24247=CARTESIAN_POINT ( 'NONE',  ( -1.113548883309555704, 38.22628252420811634, -25.34012683631568308 ) ) ;
#24248=CARTESIAN_POINT ( 'NONE',  ( -7.733045908741344121, 10.42750254442610114, 51.44704017882764191 ) ) ;
#24253=CARTESIAN_POINT ( 'NONE',  ( -1.049817751779885233, -26.50542916749595435, -37.35030165458165641 ) ) ;
#24255=ORIENTED_EDGE ( 'NONE', *, *, #4811, .F. ) ;
#24256=EDGE_CURVE ( 'NONE', #9585, #14332, #27410, .T. ) ;
#24257=CARTESIAN_POINT ( 'NONE',  ( -1.113427685306992876, -28.52429901637193410, -35.91272432484649357 ) ) ;
#24259=CARTESIAN_POINT ( 'NONE',  ( -8.786685647604890903, -48.22796981442753150, 23.24040270374441874 ) ) ;
#24266=CARTESIAN_POINT ( 'NONE',  ( -55.24340739397742084, 0.009842732675352565408, -0.002421372372454350108 ) ) ;
#24270=CARTESIAN_POINT ( 'NONE',  ( -20.38016308990357928, -16.25718651464962861, 24.94368798801368925 ) ) ;
#24271=CARTESIAN_POINT ( 'NONE',  ( -1.045287976400383290, 28.14015102489806708, -36.12803364096618708 ) ) ;
#24284=FACE_OUTER_BOUND ( 'NONE', #5435, .T. ) ;
#24289=CARTESIAN_POINT ( 'NONE',  ( -7.078251931573406708, -20.86696228105259365, -47.71415099571797924 ) ) ;
#24306=CARTESIAN_POINT ( 'NONE',  ( -1.583189561560252701, -11.94859433442933394, -44.83405390829668136 ) ) ;
#24318=CARTESIAN_POINT ( 'NONE',  ( -23.79248802219722947, -3.207402715357382306, -33.03370827286730105 ) ) ;
#24321=CARTESIAN_POINT ( 'NONE',  ( -20.57838717382308147, 1.611677988432361097, -29.92853265176831812 ) ) ;
#24322=ADVANCED_FACE ( 'NONE', ( #1132 ), #22321, .F. ) ;
#24331=CARTESIAN_POINT ( 'NONE',  ( -55.24728320129491266, -0.01362040845703352439, -0.005114031043468804730 ) ) ;
#24336=CARTESIAN_POINT ( 'NONE',  ( -20.24399999263415850, -18.44171895251379567, 23.20123049637386003 ) ) ;
#24338=CARTESIAN_POINT ( 'NONE',  ( -6.588769196390761529, 20.50531526814562966, -47.06982923582516065 ) ) ;
#24340=EDGE_LOOP ( 'NONE', ( #25820, #21381, #26643, #18790 ) ) ;
#24342=CARTESIAN_POINT ( 'NONE',  ( -1.045287976400362417, -1.530335034933495653, 45.76855895860946788 ) ) ;
#24343=ORIENTED_EDGE ( 'NONE', *, *, #24654, .F. ) ;
#24346=ORIENTED_EDGE ( 'NONE', *, *, #18354, .F. ) ;
#24349=CARTESIAN_POINT ( 'NONE',  ( -1.048994561756784405, -37.49601524795390617, 26.29622118251720764 ) ) ;
#24356=CARTESIAN_POINT ( 'NONE',  ( -20.20612091757425333, -24.59769958242376120, 16.46550228026422502 ) ) ;
#24359=CARTESIAN_POINT ( 'NONE',  ( -25.21435515916043713, -23.92354251275918031, 25.00736669481048224 ) ) ;
#24360=CARTESIAN_POINT ( 'NONE',  ( -55.24300891470650754, 0.003362556190412917256, 0.009225237711101274066 ) ) ;
#24366=CARTESIAN_POINT ( 'NONE',  ( -4.473127245936434626, -26.34600523034507802, 41.70021447285083127 ) ) ;
#24373=CARTESIAN_POINT ( 'NONE',  ( -1.058197053496169548, -45.77356582045592859, -1.754224732379389362 ) ) ;
#24375=DIRECTION ( 'NONE',  ( 0.000000000000000000, 5.223019709707975211E-21, -1.000000000000000000 ) ) ;
#24376=CARTESIAN_POINT ( 'NONE',  ( -12.82751273423880711, 33.78816682541337002, 35.32125660155409008 ) ) ;
#24377=B_SPLINE_CURVE_WITH_KNOTS ( 'NONE', 3,
 ( #10976, #16895, #4060, #1626, #6520, #28234, #26218, #6374 ),
 .UNSPECIFIED., .F., .F.,
 ( 4, 2, 2, 4 ),
 ( 0.000000000000000000, 0.002761524886576651079, 0.005523049773153302158, 0.01104609954630660432 ),
 .UNSPECIFIED. ) ;
#24380=( BOUNDED_SURFACE ( )  B_SPLINE_SURFACE ( 3, 1, ( 
 ( #25060, #2881 ),
 ( #2729, #11366 ),
 ( #7213, #7497 ),
 ( #572, #20432 ) ),
 .UNSPECIFIED., .F., .F., .F. ) 
 B_SPLINE_SURFACE_WITH_KNOTS ( ( 4, 4 ),
 ( 2, 2 ),
 ( 0.000000000000000000, 1.000000000000000000 ),
 ( 0.000000000000000000, 1.000000000000000000 ),
 .UNSPECIFIED. ) 
 GEOMETRIC_REPRESENTATION_ITEM ( )  RATIONAL_B_SPLINE_SURFACE ( (
 ( 1.000000000000000000, 1.000000000000000000),
 ( 0.7789835883360576307, 0.9689951854195403280),
 ( 0.7789835883360576307, 0.9689951854195403280),
 ( 1.000000000000000000, 1.000000000000000000) ) ) 
 REPRESENTATION_ITEM ( '' )  SURFACE ( )  );
#24386=AXIS2_PLACEMENT_3D ( 'NONE', #6898, #24463, #7049 ) ;
#24394=CARTESIAN_POINT ( 'NONE',  ( -20.57838717382308147, 18.89542499756500149, -23.26537097894111383 ) ) ;
#24398=ORIENTED_EDGE ( 'NONE', *, *, #23459, .F. ) ;
#24400=CARTESIAN_POINT ( 'NONE',  ( -1.058473599757816963, -28.32531354681309566, -35.99997772736203672 ) ) ;
#24407=VECTOR ( 'NONE', #20638, 1000.000000000000114 ) ;
#24422=EDGE_CURVE ( 'NONE', #12444, #17575, #22274, .T. ) ;
#24425=CARTESIAN_POINT ( 'NONE',  ( -20.21097721712959228, -28.26295595852180043, 8.835581498567762537 ) ) ;
#24440=CARTESIAN_POINT ( 'NONE',  ( -1.619063947482197729, 46.30105812165548684, 2.489035965910320503 ) ) ;
#24443=( LENGTH_UNIT ( ) NAMED_UNIT ( * ) SI_UNIT ( .MILLI., .METRE. ) );
#24444=ADVANCED_FACE ( 'NONE', ( #15435, #27756 ), #26525, .F. ) ;
#24445=CARTESIAN_POINT ( 'NONE',  ( -55.24728320129491266, -0.01453410071985230222, 0.0006547948648737443372 ) ) ;
#24449=EDGE_CURVE ( 'NONE', #25142, #9465, #12985, .T. ) ;
#24451=EDGE_CURVE ( 'NONE', #5381, #12412, #21198, .T. ) ;
#24453=CARTESIAN_POINT ( 'NONE',  ( -55.24390624410018802, 0.004572280736703349113, -0.009374879212967143077 ) ) ;
#24454=CARTESIAN_POINT ( 'NONE',  ( -55.24198130335446422, 0.008252882783650522525, -0.004276389980776339715 ) ) ;
#24463=DIRECTION ( 'NONE',  ( 1.000000000000000000, -6.938893903907226837E-18, 1.734723475976806709E-18 ) ) ;
#24476=CARTESIAN_POINT ( 'NONE',  ( -55.24198130335446422, 0.001391250620101877958, 0.009190321388310107587 ) ) ;
#24485=EDGE_CURVE ( 'NONE', #15158, #16092, #22217, .T. ) ;
#24490=CARTESIAN_POINT ( 'NONE',  ( -55.24340739397742084, 0.0007387096945740994529, -0.01010924026184336841 ) ) ;
#24491=CARTESIAN_POINT ( 'NONE',  ( -1.046935749539985583, -1.275486069320154847, 45.77872888003168583 ) ) ;
#24494=ORIENTED_EDGE ( 'NONE', *, *, #8507, .T. ) ;
#24498=CARTESIAN_POINT ( 'NONE',  ( -20.37983603106073716, 27.81368274044725553, 10.62371319148611981 ) ) ;
#24506=CARTESIAN_POINT ( 'NONE',  ( -25.21435515916043002, 31.17620025257588523, -15.02493970636157705 ) ) ;
#24513=ORIENTED_EDGE ( 'NONE', *, *, #15097, .F. ) ;
#24519=ADVANCED_FACE ( 'NONE', ( #22070 ), #4757, .T. ) ;
#24525=VECTOR ( 'NONE', #15502, 1000.000000000000114 ) ;
#24526=ORIENTED_EDGE ( 'NONE', *, *, #6043, .F. ) ;
#24535=CARTESIAN_POINT ( 'NONE',  ( -1.619063947482201282, 11.94059994246159384, -44.80407745103787676 ) ) ;
#24545=CARTESIAN_POINT ( 'NONE',  ( -8.259864102781671491, -36.24929574824938783, -38.68084189741935575 ) ) ;
#24549=ORIENTED_EDGE ( 'NONE', *, *, #20807, .F. ) ;
#24555=DIRECTION ( 'NONE',  ( 0.7637818620346800147, 0.5092696688508698832, 0.3965875333584785167 ) ) ;
#24558=VERTEX_POINT ( 'NONE', #2782 ) ;
#24562=VECTOR ( 'NONE', #25217, 1000.000000000000000 ) ;
#24564=CARTESIAN_POINT ( 'NONE',  ( -25.21435515916043357, -16.39063784838764093, -30.48034229288631991 ) ) ;
#24566=FACE_OUTER_BOUND ( 'NONE', #24012, .T. ) ;
#24567=CARTESIAN_POINT ( 'NONE',  ( -6.574463467970658392, 50.12924290857549181, 11.01561683919999091 ) ) ;
#24570=CARTESIAN_POINT ( 'NONE',  ( -55.24390624410018802, 0.01032895241566708991, 0.001451500391952845713 ) ) ;
#24571=CARTESIAN_POINT ( 'NONE',  ( -23.79223135445719706, -24.83942264280416978, -22.01133905265676916 ) ) ;
#24574=B_SPLINE_CURVE_WITH_KNOTS ( 'NONE', 3,
 ( #7624, #16823, #23021, #18683, #18544, #1545 ),
 .UNSPECIFIED., .F., .F.,
 ( 4, 2, 4 ),
 ( 1.734723475976807094E-18, 0.0004335184443140216969, 0.0008670368886280416590 ),
 .UNSPECIFIED. ) ;
#24588=CARTESIAN_POINT ( 'NONE',  ( -20.24419206586953734, -28.55732805495821225, -7.929973069813295972 ) ) ;
#24593=ORIENTED_EDGE ( 'NONE', *, *, #28376, .F. ) ;
#24596=ORIENTED_EDGE ( 'NONE', *, *, #18898, .F. ) ;
#24598=DIRECTION ( 'NONE',  ( 0.000000000000000000, 0.000000000000000000, 1.000000000000000000 ) ) ;
#24603=CARTESIAN_POINT ( 'NONE',  ( -25.21435515916043713, 6.169479169075932745, 34.05351380035326514 ) ) ;
#24607=CARTESIAN_POINT ( 'NONE',  ( -55.24271866751342941, 0.006671293903669565407, -0.006757859501006440936 ) ) ;
#24610=ORIENTED_EDGE ( 'NONE', *, *, #18734, .F. ) ;
#24615=CARTESIAN_POINT ( 'NONE',  ( -1.056502255334265339, 37.35734037467636171, -26.51074901220517432 ) ) ;
#24619=CARTESIAN_POINT ( 'NONE',  ( -20.20612091757423912, 1.137293889216362874, -29.57813639663777039 ) ) ;
#24627=CARTESIAN_POINT ( 'NONE',  ( -5.986830583229505898, 43.56094206392996426, 26.01297580803277754 ) ) ;
#24630=ORIENTED_EDGE ( 'NONE', *, *, #10070, .F. ) ;
#24632=CARTESIAN_POINT ( 'NONE',  ( -55.24271866751342941, -0.001545935011630300039, 0.009369360294295641864 ) ) ;
#24644=CARTESIAN_POINT ( 'NONE',  ( -1.019300379054419725, 28.53917295602949977, 35.83762006677368106 ) ) ;
#24650=CARTESIAN_POINT ( 'NONE',  ( -20.57838717382308147, 28.96176188950229502, 7.715628353033378239 ) ) ;
#24653=CARTESIAN_POINT ( 'NONE',  ( -1.050231094221219408, 14.39477892760360689, 43.47885872350340009 ) ) ;
#24654=EDGE_CURVE ( 'NONE', #3225, #13021, #15782, .T. ) ;
#24658=CARTESIAN_POINT ( 'NONE',  ( -20.37983603106074071, 16.25728007463443703, 24.94323704205420000 ) ) ;
#24666=CARTESIAN_POINT ( 'NONE',  ( -1.155031165708884533, 44.25214473648929925, 12.20332162035416879 ) ) ;
#24673=CARTESIAN_POINT ( 'NONE',  ( -20.57838717382308147, 29.92853265176831812, -1.611677988432464126 ) ) ;
#24682=CARTESIAN_POINT ( 'NONE',  ( -28.13707043255157103, -12.83104814250440029, 18.96624908365860662 ) ) ;
#24683=CARTESIAN_POINT ( 'NONE',  ( -2.904412668506655582, -44.35433137608953302, -17.42365698954681719 ) ) ;
#24685=CARTESIAN_POINT ( 'NONE',  ( -20.47566262905010248, -23.19796652405687709, -18.81547655725238499 ) ) ;
#24688=DIRECTION ( 'NONE',  ( 0.7637818620346800147, -0.3965875333584803486, 0.5092696688508683289 ) ) ;
#24701=CARTESIAN_POINT ( 'NONE',  ( -10.86508079875780552, -6.877801422380434460, 50.67624451685642839 ) ) ;
#24708=CARTESIAN_POINT ( 'NONE',  ( -8.786685647604885574, 6.096987947571466530E-17, -1.524246986892866633E-17 ) ) ;
#24713=CARTESIAN_POINT ( 'NONE',  ( -25.21435515916025594, 1.749597353048488237E-16, -4.373993382621220594E-17 ) ) ;
#24714=CARTESIAN_POINT ( 'NONE',  ( -20.57838717382308147, -29.92853265176832878, -1.611677988432255848 ) ) ;
#24716=EDGE_CURVE ( 'NONE', #10555, #4266, #17171, .T. ) ;
#24717=ORIENTED_EDGE ( 'NONE', *, *, #7165, .T. ) ;
#24720=CARTESIAN_POINT ( 'NONE',  ( -6.574463467970464770, -44.27173031830730565, -25.96726214983177528 ) ) ;
#24721=CARTESIAN_POINT ( 'NONE',  ( -23.79248802219722947, 3.207402715357613676, 33.03370827286725842 ) ) ;
#24743=CARTESIAN_POINT ( 'NONE',  ( -21.41427618760458174, 23.81423075802610967, 19.54551635498102158 ) ) ;
#24744=CARTESIAN_POINT ( 'NONE',  ( -1.323830074806771062, 16.42382241777537644, -43.04593525292974476 ) ) ;
#24766=ORIENTED_EDGE ( 'NONE', *, *, #8507, .F. ) ;
#24771=CARTESIAN_POINT ( 'NONE',  ( -1.463510566862822770, 11.94877850058565727, 44.64091840826476698 ) ) ;
#24774=ORIENTED_EDGE ( 'NONE', *, *, #9684, .T. ) ;
#24786=CARTESIAN_POINT ( 'NONE',  ( -1.259972190295298944, 43.01178231151332909, -16.33417789844387968 ) ) ;
#24789=CARTESIAN_POINT ( 'NONE',  ( -20.20700224038492010, 27.82980252387833886, 10.08426345511560207 ) ) ;
#24792=CARTESIAN_POINT ( 'NONE',  ( -1.619063947482197729, -44.80407745103793360, -11.94059994246142331 ) ) ;
#24793=DIRECTION ( 'NONE',  ( 0.000000000000000000, 5.223019709708233256E-21, -1.000000000000000000 ) ) ;
#24805=VERTEX_POINT ( 'NONE', #14383 ) ;
#24808=CARTESIAN_POINT ( 'NONE',  ( -55.24728320129491266, 0.008013189884952347936, 0.01214321324517130159 ) ) ;
#24809=B_SPLINE_CURVE_WITH_KNOTS ( 'NONE', 3,
 ( #18744, #27517, #7827, #7382 ),
 .UNSPECIFIED., .F., .F.,
 ( 4, 4 ),
 ( 1.895855152355442610E-16, 0.001982023823822946784 ),
 .UNSPECIFIED. ) ;
#24810=CARTESIAN_POINT ( 'NONE',  ( -25.21435515916043713, 30.48034229288662544, 16.39063784838709736 ) ) ;
#24813=CARTESIAN_POINT ( 'NONE',  ( -1.464342487929843450, 2.431462367721978435, 46.14921266389554688 ) ) ;
#24834=ORIENTED_EDGE ( 'NONE', *, *, #21808, .F. ) ;
#24837=EDGE_CURVE ( 'NONE', #25524, #7798, #19138, .T. ) ;
#24838=DIRECTION ( 'NONE',  ( 0.7637818620346802367, -0.2198041754873842346, 0.6068965246771050870 ) ) ;
#24845=CARTESIAN_POINT ( 'NONE',  ( -1.049817751779888342, 27.33161971822197955, -36.75003908324300994 ) ) ;
#24847=ORIENTED_EDGE ( 'NONE', *, *, #8005, .F. ) ;
#24855=ORIENTED_EDGE ( 'NONE', *, *, #23364, .T. ) ;
#24857=CARTESIAN_POINT ( 'NONE',  ( -22.23342874802668589, 16.78332232459680640, 26.81018246605520972 ) ) ;
#24860=CARTESIAN_POINT ( 'NONE',  ( -20.57838717382308147, -7.715628353033886278, -28.96176188950215646 ) ) ;
#24867=CIRCLE ( 'NONE', #5541, 34.60786435723138510 ) ;
#24869=EDGE_LOOP ( 'NONE', ( #270, #28286, #11692, #6357 ) ) ;
#24872=EDGE_CURVE ( 'NONE', #23610, #27689, #18442, .T. ) ;
#24875=LINE ( 'NONE', #386, #12907 ) ;
#24890=CARTESIAN_POINT ( 'NONE',  ( -28.13707043255157103, -12.83104814250467562, -18.96624908365841478 ) ) ;
#24892=CARTESIAN_POINT ( 'NONE',  ( -24.53237795827023859, -3.868415699415882258, -33.71192251888856362 ) ) ;
#24895=CARTESIAN_POINT ( 'NONE',  ( -1.045287976400386842, -28.14015102489780062, 36.12803364096639314 ) ) ;
#24896=ORIENTED_EDGE ( 'NONE', *, *, #2038, .T. ) ;
#24899=CIRCLE ( 'NONE', #12001, 28.92774122539760384 ) ;
#24900=DIRECTION ( 'NONE',  ( -5.541455922705464902E-20, 5.223019709708320524E-21, -1.000000000000000000 ) ) ;
#24908=DIRECTION ( 'NONE',  ( 0.000000000000000000, -5.223019709708233256E-21, 1.000000000000000000 ) ) ;
#24916=EDGE_CURVE ( 'NONE', #13041, #20671, #12572, .T. ) ;
#24924=CARTESIAN_POINT ( 'NONE',  ( -1.049817751779889008, -43.39729912094389874, -14.63752841325032250 ) ) ;
#24930=ORIENTED_EDGE ( 'NONE', *, *, #12850, .T. ) ;
#24934=CARTESIAN_POINT ( 'NONE',  ( -1.323830074806768176, 44.47857376182273015, -12.01461446423216906 ) ) ;
#24945=ORIENTED_EDGE ( 'NONE', *, *, #22535, .T. ) ;
#24964=B_SPLINE_CURVE_WITH_KNOTS ( 'NONE', 3,
 ( #6164, #19515, #17346, #26136, #2085, #15177 ),
 .UNSPECIFIED., .F., .F.,
 ( 4, 2, 4 ),
 ( 3.607901639910057446E-16, 0.003576372551511165700, 0.007152745103021970578 ),
 .UNSPECIFIED. ) ;
#24972=CARTESIAN_POINT ( 'NONE',  ( -20.20612091757420359, 23.26073043121660433, 18.30568244821352408 ) ) ;
#24980=ORIENTED_EDGE ( 'NONE', *, *, #13312, .T. ) ;
#24988=B_SPLINE_CURVE_WITH_KNOTS ( 'NONE', 3,
 ( #2520, #2226, #13603, #24720, #9445, #4969, #22404, #20217 ),
 .UNSPECIFIED., .F., .F.,
 ( 4, 2, 2, 4 ),
 ( 0.000000000000000000, 0.002761524886576556103, 0.005523049773153112206, 0.01104609954630622441 ),
 .UNSPECIFIED. ) ;
#24990=CARTESIAN_POINT ( 'NONE',  ( -7.078251931573406708, 38.93060825814230697, -34.59014398252930533 ) ) ;
#24995=CARTESIAN_POINT ( 'NONE',  ( -1.619063947482197729, 25.20140673341430571, 38.92136151114879539 ) ) ;
#25008=ORIENTED_EDGE ( 'NONE', *, *, #27691, .F. ) ;
#25024=ORIENTED_EDGE ( 'NONE', *, *, #24872, .F. ) ;
#25031=LINE ( 'NONE', #15174, #5208 ) ;
#25037=DIRECTION ( 'NONE',  ( 0.000000000000000000, 5.223019709707975211E-21, -1.000000000000000000 ) ) ;
#25038=CARTESIAN_POINT ( 'NONE',  ( -55.24340739397742084, 0.008612749836246956503, -0.005344433640973183380 ) ) ;
#25041=CARTESIAN_POINT ( 'NONE',  ( -1.045287976400365970, 1.530335034933814731, -45.76855895860946788 ) ) ;
#25043=CARTESIAN_POINT ( 'NONE',  ( -1.019300379054419725, -35.83762006677378764, 28.53917295602937187 ) ) ;
#25054=ADVANCED_FACE ( 'NONE', ( #7458 ), #13916, .T. ) ;
#25057=VERTEX_POINT ( 'NONE', #18223 ) ;
#25060=CARTESIAN_POINT ( 'NONE',  ( -55.24390624410018802, -0.001811362924362171613, 0.01027195578988007209 ) ) ;
#25067=ORIENTED_EDGE ( 'NONE', *, *, #21812, .F. ) ;
#25068=ORIENTED_EDGE ( 'NONE', *, *, #11705, .T. ) ;
#25080=CARTESIAN_POINT ( 'NONE',  ( -55.24198130335446422, 0.001516807524708540730, -0.009170435128245290474 ) ) ;
#25085=ORIENTED_EDGE ( 'NONE', *, *, #16035, .F. ) ;
#25092=CARTESIAN_POINT ( 'NONE',  ( -28.41354790283022069, -14.62505768302813713, -18.00456980371894744 ) ) ;
#25109=EDGE_CURVE ( 'NONE', #6415, #18758, #18365, .T. ) ;
#25114=ORIENTED_EDGE ( 'NONE', *, *, #4811, .T. ) ;
#25117=CARTESIAN_POINT ( 'NONE',  ( -1.239374126674604337, 11.92219841463829333, -44.48112152129351671 ) ) ;
#25119=CARTESIAN_POINT ( 'NONE',  ( -20.20700224038492721, -18.19058640100206503, 23.35150625415678860 ) ) ;
#25121=CARTESIAN_POINT ( 'NONE',  ( -1.155031165708883867, -2.068616213631259804, -45.85732438018710155 ) ) ;
#25124=B_SPLINE_CURVE_WITH_KNOTS ( 'NONE', 3,
 ( #27625, #23335, #17108, #16705, #3734, #12503 ),
 .UNSPECIFIED., .F., .F.,
 ( 4, 2, 4 ),
 ( 1.396102177145585797E-16, 0.003570751334075633089, 0.007141502668151126533 ),
 .UNSPECIFIED. ) ;
#25126=CARTESIAN_POINT ( 'NONE',  ( -20.57838717382308147, -7.715628353033481268, 28.96176188950225949 ) ) ;
#25134=CARTESIAN_POINT ( 'NONE',  ( -4.178947244162639407, -18.28784278438482858, -45.38689110596713050 ) ) ;
#25138=CARTESIAN_POINT ( 'NONE',  ( -22.34422965417122242, 27.39717383755282043, -26.20925041532862920 ) ) ;
#25140=EDGE_CURVE ( 'NONE', #5543, #19578, #9172, .T. ) ;
#25142=VERTEX_POINT ( 'NONE', #14484 ) ;
#25144=CARTESIAN_POINT ( 'NONE',  ( -1.259972190295303385, -16.33417789844404666, -43.01178231151323672 ) ) ;
#25147=LINE ( 'NONE', #27286, #11976 ) ;
#25157=CARTESIAN_POINT ( 'NONE',  ( -20.21097721650786383, 28.05863614620939472, -9.464413208035171721 ) ) ;
#25158=ORIENTED_EDGE ( 'NONE', *, *, #27106, .T. ) ;
#25163=ORIENTED_EDGE ( 'NONE', *, *, #3907, .F. ) ;
#25178=CARTESIAN_POINT ( 'NONE',  ( -20.57838717382308147, 28.96176188950229502, 7.715628353033378239 ) ) ;
#25179=CARTESIAN_POINT ( 'NONE',  ( -8.786685647604885574, 6.096987947571466530E-17, -1.524246986892866633E-17 ) ) ;
#25194=VERTEX_POINT ( 'NONE', #14337 ) ;
#25202=CARTESIAN_POINT ( 'NONE',  ( -7.078251931573400491, -20.86696228105191864, 47.71415099571825635 ) ) ;
#25217=DIRECTION ( 'NONE',  ( 0.7637818620346801257, 0.1788995134688915190, 0.6201872550346635427 ) ) ;
#25222=ORIENTED_EDGE ( 'NONE', *, *, #11835, .F. ) ;
#25223=CARTESIAN_POINT ( 'NONE',  ( -1.583189561560252701, -25.21827308671259615, -38.94740041318285506 ) ) ;
#25227=ADVANCED_FACE ( 'NONE', ( #12323 ), #13473, .F. ) ;
#25230=CARTESIAN_POINT ( 'NONE',  ( -1.619063947482197729, 25.20140673341430571, 38.92136151114879539 ) ) ;
#25232=CARTESIAN_POINT ( 'NONE',  ( -1.045287976400365970, 1.530335034934747318, 45.76855895860941814 ) ) ;
#25235=CARTESIAN_POINT ( 'NONE',  ( -1.259972190295296057, 45.95417440459617353, -2.243354636025928439 ) ) ;
#25241=CARTESIAN_POINT ( 'NONE',  ( -20.20700224038492721, 18.19058640100257662, 23.35150625415638714 ) ) ;
#25244=LINE ( 'NONE', #764, #21990 ) ;
#25249=ORIENTED_EDGE ( 'NONE', *, *, #26965, .F. ) ;
#25255=ORIENTED_EDGE ( 'NONE', *, *, #15511, .F. ) ;
#25256=ORIENTED_EDGE ( 'NONE', *, *, #19568, .T. ) ;
#25261=CARTESIAN_POINT ( 'NONE',  ( -1.031422197589711764, 44.01264471863847660, -12.69107518035516691 ) ) ;
#25270=CARTESIAN_POINT ( 'NONE',  ( 180.4657679828686980, 20.00000000000000000, 2.618615375249201539E-15 ) ) ;
#25276=CARTESIAN_POINT ( 'NONE',  ( -20.24399999263415140, -7.930419334766389383, -28.55700515887716762 ) ) ;
#25279=ORIENTED_EDGE ( 'NONE', *, *, #14289, .F. ) ;
#25285=CARTESIAN_POINT ( 'NONE',  ( -1.539760825549682410, -29.16712717142786460, -35.94320866319479535 ) ) ;
#25287=ORIENTED_EDGE ( 'NONE', *, *, #15140, .F. ) ;
#25289=DIRECTION ( 'NONE',  ( 0.7563875759206388771, -0.3556158456312938365, -0.5490129373055243622 ) ) ;
#25313=CARTESIAN_POINT ( 'NONE',  ( -12.94347594948484037, 33.69581619287875895, -35.22469990145616237 ) ) ;
#25324=CARTESIAN_POINT ( 'NONE',  ( -1.619063947482201282, 38.92136151114908671, -25.20140673341387227 ) ) ;
#25325=CIRCLE ( 'NONE', #40, 28.92774122539760384 ) ;
#25329=CARTESIAN_POINT ( 'NONE',  ( -1.239374126674604337, -28.97829083655465254, -35.79060836339803586 ) ) ;
#25339=EDGE_CURVE ( 'NONE', #10065, #9585, #22528, .T. ) ;
#25343=AXIS2_PLACEMENT_3D ( 'NONE', #11795, #8957, #5306 ) ;
#25345=AXIS2_PLACEMENT_3D ( 'NONE', #19989, #26600, #24900 ) ;
#25374=EDGE_LOOP ( 'NONE', ( #25691, #15439, #12815, #7282 ) ) ;
#25386=CARTESIAN_POINT ( 'NONE',  ( -20.20700224038492721, -27.82980252387812570, 10.08426345511618649 ) ) ;
#25396=EDGE_LOOP ( 'NONE', ( #15289, #27965, #1790, #8990 ) ) ;
#25403=VERTEX_POINT ( 'NONE', #9568 ) ;
#25404=EDGE_CURVE ( 'NONE', #13800, #21625, #2578, .T. ) ;
#25409=( BOUNDED_SURFACE ( )  B_SPLINE_SURFACE ( 3, 1, ( 
 ( #26449, #7042 ),
 ( #24454, #2119 ),
 ( #11058, #17803 ),
 ( #10791, #15218 ) ),
 .UNSPECIFIED., .F., .F., .F. ) 
 B_SPLINE_SURFACE_WITH_KNOTS ( ( 4, 4 ),
 ( 2, 2 ),
 ( 0.000000000000000000, 1.000000000000000000 ),
 ( 0.000000000000000000, 1.000000000000000000 ),
 .UNSPECIFIED. ) 
 GEOMETRIC_REPRESENTATION_ITEM ( )  RATIONAL_B_SPLINE_SURFACE ( (
 ( 1.000000000000000000, 1.000000000000000000),
 ( 0.9593753223639863714, 0.9995975284513187731),
 ( 0.9593753223639863714, 0.9995975284513187731),
 ( 1.000000000000000000, 1.000000000000000000) ) ) 
 REPRESENTATION_ITEM ( '' )  SURFACE ( )  );
#25413=CARTESIAN_POINT ( 'NONE',  ( -25.21435515916043713, -31.17620025257598471, -15.02493970636134613 ) ) ;
#25420=CARTESIAN_POINT ( 'NONE',  ( -1.049817751779873687, -13.66628317065018017, -43.71287583013722156 ) ) ;
#25421=CARTESIAN_POINT ( 'NONE',  ( -25.21435515916043357, -6.169479169075226643, 34.05351380035340014 ) ) ;
#25434=CARTESIAN_POINT ( 'NONE',  ( -7.078251931573400491, -51.82710018979479116, -5.101176922830485516 ) ) ;
#25441=VERTEX_POINT ( 'NONE', #3095 ) ;
#25444=( BOUNDED_SURFACE ( )  B_SPLINE_SURFACE ( 3, 1, ( 
 ( #15399, #2446 ),
 ( #13379, #6649 ),
 ( #26623, #22330 ),
 ( #2592, #8799 ) ),
 .UNSPECIFIED., .F., .F., .F. ) 
 B_SPLINE_SURFACE_WITH_KNOTS ( ( 4, 4 ),
 ( 2, 2 ),
 ( 0.000000000000000000, 1.000000000000000000 ),
 ( 0.000000000000000000, 1.000000000000000000 ),
 .UNSPECIFIED. ) 
 GEOMETRIC_REPRESENTATION_ITEM ( )  RATIONAL_B_SPLINE_SURFACE ( (
 ( 1.000000000000000000, 1.000000000000000000),
 ( 0.7789835883360576307, 0.9689951854195403280),
 ( 0.7789835883360576307, 0.9689951854195403280),
 ( 1.000000000000000000, 1.000000000000000000) ) ) 
 REPRESENTATION_ITEM ( '' )  SURFACE ( )  );
#25454=CARTESIAN_POINT ( 'NONE',  ( -55.24340739397742794, -0.007744344507854267548, 0.006539691034608354631 ) ) ;
#25462=CARTESIAN_POINT ( 'NONE',  ( -1.619063947482194177, -46.30105812165547974, 2.489035965910640247 ) ) ;
#25463=CARTESIAN_POINT ( 'NONE',  ( -1.113548883309550153, 28.52482525634944821, -35.91246368318211069 ) ) ;
#25468=CARTESIAN_POINT ( 'NONE',  ( -22.23226125620943705, -29.33577758406442726, 11.82389163795241593 ) ) ;
#25470=CARTESIAN_POINT ( 'NONE',  ( -1.050231094221204753, -43.47885872350344982, 14.39477892760344879 ) ) ;
#25474=CARTESIAN_POINT ( 'NONE',  ( -55.24390624410018802, 0.01027195578988056128, 0.001811362924362418811 ) ) ;
#25475=ORIENTED_EDGE ( 'NONE', *, *, #22050, .F. ) ;
#25476=CARTESIAN_POINT ( 'NONE',  ( -12.94347594948482438, 42.93165645342861581, -23.08810053288705078 ) ) ;
#25481=CARTESIAN_POINT ( 'NONE',  ( -55.24728320129491266, 0.01137345571546872526, -0.009072670231975240793 ) ) ;
#25482=CARTESIAN_POINT ( 'NONE',  ( -1.045287976400379737, -25.66401692420040703, -37.92705037016734337 ) ) ;
#25485=CARTESIAN_POINT ( 'NONE',  ( -10.86508079875781263, -22.20099862734791074, 46.07061504567109012 ) ) ;
#25487=ADVANCED_FACE ( 'NONE', ( #14594 ), #11153, .T. ) ;
#25500=( BOUNDED_SURFACE ( )  B_SPLINE_SURFACE ( 3, 1, ( 
 ( #3908, #21031 ),
 ( #16739, #5494 ),
 ( #8237, #18740 ),
 ( #1321, #10117 ) ),
 .UNSPECIFIED., .F., .F., .F. ) 
 B_SPLINE_SURFACE_WITH_KNOTS ( ( 4, 4 ),
 ( 2, 2 ),
 ( 0.000000000000000000, 1.000000000000000000 ),
 ( 0.000000000000000000, 1.000000000000000000 ),
 .UNSPECIFIED. ) 
 GEOMETRIC_REPRESENTATION_ITEM ( )  RATIONAL_B_SPLINE_SURFACE ( (
 ( 1.000000000000000000, 1.000000000000000000),
 ( 0.7789835883360576307, 0.9689951854195403280),
 ( 0.7789835883360576307, 0.9689951854195403280),
 ( 1.000000000000000000, 1.000000000000000000) ) ) 
 REPRESENTATION_ITEM ( '' )  SURFACE ( )  );
#25507=CARTESIAN_POINT ( 'NONE',  ( -1.239374126674604337, -45.98822239537607715, 2.406737988131604666 ) ) ;
#25509=CARTESIAN_POINT ( 'NONE',  ( -25.21435515916025594, 1.749597353048488237E-16, -4.373993382621220594E-17 ) ) ;
#25510=CARTESIAN_POINT ( 'NONE',  ( -7.733045908741344121, 38.67583825854200086, 35.49239760110631181 ) ) ;
#25511=CARTESIAN_POINT ( 'NONE',  ( -1.045287976400365970, 28.14015102489882736, 36.12803364096558312 ) ) ;
#25516=EDGE_CURVE ( 'NONE', #7819, #27747, #2877, .T. ) ;
#25519=EDGE_LOOP ( 'NONE', ( #20431, #14784, #2108, #11753 ) ) ;
#25524=VERTEX_POINT ( 'NONE', #17980 ) ;
#25531=CARTESIAN_POINT ( 'NONE',  ( -1.539760825549689072, 46.22267384399381740, -2.469813586483248447 ) ) ;
#25537=CARTESIAN_POINT ( 'NONE',  ( -7.078251931573400491, 50.86685171665412497, -11.16394717458693897 ) ) ;
#25539=CARTESIAN_POINT ( 'NONE',  ( -1.323830074806772394, 35.86387698262958423, 28.92190886481825274 ) ) ;
#25542=CARTESIAN_POINT ( 'NONE',  ( -20.57838717382308147, -16.28767523336139078, -25.16001208503099917 ) ) ;
#25549=ORIENTED_EDGE ( 'NONE', *, *, #17095, .T. ) ;
#25553=CARTESIAN_POINT ( 'NONE',  ( -24.53237795827024570, -33.25734978085267102, -6.738475012719991497 ) ) ;
#25555=CARTESIAN_POINT ( 'NONE',  ( -20.38016308990357928, 1.509191766064626128, 29.73560196176844173 ) ) ;
#25560=CARTESIAN_POINT ( 'NONE',  ( -22.23226125620928784, -7.677408153693816573, 30.68305173820434462 ) ) ;
#25561=EDGE_CURVE ( 'NONE', #25524, #600, #14970, .T. ) ;
#25562=ORIENTED_EDGE ( 'NONE', *, *, #13875, .T. ) ;
#25572=CARTESIAN_POINT ( 'NONE',  ( -1.045287976400362417, -28.14015102489855735, -36.12803364096578207 ) ) ;
#25574=ORIENTED_EDGE ( 'NONE', *, *, #21702, .T. ) ;
#25576=( BOUNDED_SURFACE ( )  B_SPLINE_SURFACE ( 3, 1, ( 
 ( #9418, #5080 ),
 ( #9270, #9550 ),
 ( #20339, #11852 ),
 ( #20189, #20622 ) ),
 .UNSPECIFIED., .F., .F., .F. ) 
 B_SPLINE_SURFACE_WITH_KNOTS ( ( 4, 4 ),
 ( 2, 2 ),
 ( 0.000000000000000000, 1.000000000000000000 ),
 ( 0.000000000000000000, 1.000000000000000000 ),
 .UNSPECIFIED. ) 
 GEOMETRIC_REPRESENTATION_ITEM ( )  RATIONAL_B_SPLINE_SURFACE ( (
 ( 1.000000000000000000, 1.000000000000000000),
 ( 0.9593753223639863714, 0.9995975284513187731),
 ( 0.9593753223639863714, 0.9995975284513187731),
 ( 1.000000000000000000, 1.000000000000000000) ) ) 
 REPRESENTATION_ITEM ( '' )  SURFACE ( )  );
#25583=CARTESIAN_POINT ( 'NONE',  ( -55.25719721206881729, 0.006045473558784871665, -0.009391134844733287426 ) ) ;
#25595=CARTESIAN_POINT ( 'NONE',  ( -1.048172774974303278, 43.23017713506524728, -15.11899685083838030 ) ) ;
#25596=LINE ( 'NONE', #8308, #25807 ) ;
#25601=FACE_OUTER_BOUND ( 'NONE', #12287, .T. ) ;
#25612=CARTESIAN_POINT ( 'NONE',  ( -1.031422197589716205, 15.60268798220698017, 43.06660437151292342 ) ) ;
#25616=CARTESIAN_POINT ( 'NONE',  ( -55.24728320129491266, -0.0006547948648734058493, -0.01453410071985278100 ) ) ;
#25620=CARTESIAN_POINT ( 'NONE',  ( -1.583189561560256253, -29.24830400313190637, -36.01941156322777715 ) ) ;
#25629=CARTESIAN_POINT ( 'NONE',  ( -4.780792508754330150, 48.13366140756558309, -11.68149851467477340 ) ) ;
#25632=ADVANCED_FACE ( 'NONE', ( #14192 ), #12233, .F. ) ;
#25636=CARTESIAN_POINT ( 'NONE',  ( -1.058473599757817185, 28.32531354681336566, 35.99997772736180224 ) ) ;
#25647=ORIENTED_EDGE ( 'NONE', *, *, #2038, .F. ) ;
#25651=CARTESIAN_POINT ( 'NONE',  ( -7.078251931573406708, 50.86685171665428840, 11.16394717458623731 ) ) ;
#25656=B_SPLINE_CURVE_WITH_KNOTS ( 'NONE', 3,
 ( #27512, #7821, #10676, #1561, #2144, #19582 ),
 .UNSPECIFIED., .F., .F.,
 ( 4, 2, 4 ),
 ( 1.607967956875964627E-16, 0.003570751334075640028, 0.007141502668151118727 ),
 .UNSPECIFIED. ) ;
#25658=EDGE_LOOP ( 'NONE', ( #11375, #9515, #2503, #17804 ) ) ;
#25660=B_SPLINE_CURVE_WITH_KNOTS ( 'NONE', 3,
 ( #6719, #4835, #4401, #363, #13462, #9150, #657, #22260 ),
 .UNSPECIFIED., .F., .F.,
 ( 4, 2, 2, 4 ),
 ( 0.000000000000000000, 0.002761524886576657151, 0.005523049773153314301, 0.01104609954630661819 ),
 .UNSPECIFIED. ) ;
#25664=CARTESIAN_POINT ( 'NONE',  ( -55.24728320129491266, 0.01362040845703093098, -0.005114031043466513160 ) ) ;
#25673=EDGE_CURVE ( 'NONE', #19718, #27068, #3548, .T. ) ;
#25676=CARTESIAN_POINT ( 'NONE',  ( -20.47566338032530808, 25.06314818626709240, 16.24827550219793437 ) ) ;
#25685=EDGE_LOOP ( 'NONE', ( #22729, #4820, #5411, #19468 ) ) ;
#25691=ORIENTED_EDGE ( 'NONE', *, *, #4573, .T. ) ;
#25692=EDGE_CURVE ( 'NONE', #21703, #7846, #19705, .T. ) ;
#25697=CARTESIAN_POINT ( 'NONE',  ( -12.82751273423880356, -6.573887447703164355, -48.43568301531138331 ) ) ;
#25699=CARTESIAN_POINT ( 'NONE',  ( -1.155031165708891860, -44.25214473648919977, -12.20332162035446366 ) ) ;
#25702=VERTEX_POINT ( 'NONE', #6017 ) ;
#25704=CARTESIAN_POINT ( 'NONE',  ( -21.81686047589428057, -26.62923599424948407, 27.83628745321478704 ) ) ;
#25705=CARTESIAN_POINT ( 'NONE',  ( -8.786685647604890903, -52.67761315067279781, 9.545808661481174795 ) ) ;
#25712=B_SPLINE_CURVE_WITH_KNOTS ( 'NONE', 3,
 ( #22653, #1043, #16001, #22500, #14120, #5062, #22941, #3063 ),
 .UNSPECIFIED., .F., .F.,
 ( 4, 2, 2, 4 ),
 ( 2.169948783056603995E-16, 0.002761568181852859429, 0.005523136363705502018, 0.01104627272741079240 ),
 .UNSPECIFIED. ) ;
#25716=ORIENTED_EDGE ( 'NONE', *, *, #14428, .F. ) ;
#25725=DIRECTION ( 'NONE',  ( 1.000000000000000000, -6.938893903907226837E-18, 1.734723475976806709E-18 ) ) ;
#25726=CARTESIAN_POINT ( 'NONE',  ( -28.13707043255157103, 14.07296284901332761, -18.06394523322457957 ) ) ;
#25727=CARTESIAN_POINT ( 'NONE',  ( -24.53237795827033807, 22.94498492516385468, 24.99972053297880947 ) ) ;
#25731=LINE ( 'NONE', #3846, #10182 ) ;
#25736=CARTESIAN_POINT ( 'NONE',  ( -8.786685647604898008, 48.22796981442802178, 23.24040270374343464 ) ) ;
#25740=CARTESIAN_POINT ( 'NONE',  ( -1.259920593601976613, -44.39818421957808425, 12.06711544331609609 ) ) ;
#25741=EDGE_LOOP ( 'NONE', ( #2587, #1220, #2279, #25647 ) ) ;
#25743=CARTESIAN_POINT ( 'NONE',  ( 180.4657679828686980, -1.252232817320263489E-15, 3.130582043300658722E-16 ) ) ;
#25747=ORIENTED_EDGE ( 'NONE', *, *, #21882, .T. ) ;
#25748=CARTESIAN_POINT ( 'NONE',  ( -9.156249394959713683, -53.90509764945124971, 8.027840202794504165 ) ) ;
#25754=B_SPLINE_CURVE_WITH_KNOTS ( 'NONE', 3,
 ( #1515, #12445, #1229, #23137, #16489, #16637, #21235, #21510 ),
 .UNSPECIFIED., .F., .F.,
 ( 4, 2, 2, 4 ),
 ( 2.214340075454938295E-16, 0.002761568181852865067, 0.005523136363705508090, 0.01104627272741079587 ),
 .UNSPECIFIED. ) ;
#25770=ORIENTED_EDGE ( 'NONE', *, *, #15644, .T. ) ;
#25773=DIRECTION ( 'NONE',  ( 0.000000000000000000, 5.223019709708233256E-21, -1.000000000000000000 ) ) ;
#25775=DIRECTION ( 'NONE',  ( -0.7637818620346800147, -0.1788995134688828315, 0.6201872550346662072 ) ) ;
#25779=ORIENTED_EDGE ( 'NONE', *, *, #8610, .T. ) ;
#25782=VECTOR ( 'NONE', #27543, 1000.000000000000114 ) ;
#25783=DIRECTION ( 'NONE',  ( 1.000000000000000000, -6.938893903907226837E-18, 1.734723475976806709E-18 ) ) ;
#25784=DIRECTION ( 'NONE',  ( 1.000000000000000000, -6.938893903907226837E-18, 1.734723475976806709E-18 ) ) ;
#25787=CARTESIAN_POINT ( 'NONE',  ( -5.986830583229484581, -11.27873876172107437, 49.46736940480268174 ) ) ;
#25788=VERTEX_POINT ( 'NONE', #24135 ) ;
#25793=CIRCLE ( 'NONE', #16580, 34.60786435723138510 ) ;
#25801=CARTESIAN_POINT ( 'NONE',  ( 0.000000000000000000, 0.000000000000000000, 0.000000000000000000 ) ) ;
#25803=CARTESIAN_POINT ( 'NONE',  ( -8.786685647604896232, 52.67761315067299677, 9.545808661480061019 ) ) ;
#25806=CIRCLE ( 'NONE', #18902, 34.60786435723138510 ) ;
#25807=VECTOR ( 'NONE', #1393, 1000.000000000000000 ) ;
#25813=AXIS2_PLACEMENT_3D ( 'NONE', #25801, #8112, #14267 ) ;
#25815=CARTESIAN_POINT ( 'NONE',  ( -1.058473599757810746, 38.06357893967467731, 25.48501014712358881 ) ) ;
#25818=EDGE_CURVE ( 'NONE', #2997, #15661, #4614, .T. ) ;
#25820=ORIENTED_EDGE ( 'NONE', *, *, #21812, .T. ) ;
#25837=CARTESIAN_POINT ( 'NONE',  ( -20.20700224038492721, -24.51628800869059432, -16.58740185276701951 ) ) ;
#25839=CARTESIAN_POINT ( 'NONE',  ( -55.24198130335446422, -0.009190321388309828296, 0.001391250620101365347 ) ) ;
#25848=ORIENTED_EDGE ( 'NONE', *, *, #2318, .T. ) ;
#25850=DIRECTION ( 'NONE',  ( 0.000000000000000000, -5.223019709708190374E-21, 1.000000000000000000 ) ) ;
#25856=ORIENTED_EDGE ( 'NONE', *, *, #13514, .F. ) ;
#25863=VECTOR ( 'NONE', #23397, 1000.000000000000000 ) ;
#25868=EDGE_LOOP ( 'NONE', ( #2054, #11512, #26198, #16121 ) ) ;
#25870=CARTESIAN_POINT ( 'NONE',  ( -8.786685647604889127, 9.545808661480615243, -52.67761315067287597 ) ) ;
#25872=DIRECTION ( 'NONE',  ( -0.7637818620346801257, 0.3965875333584876761, 0.5092696688508626668 ) ) ;
#25876=CARTESIAN_POINT ( 'NONE',  ( -21.41430102051751305, -19.54553566814603016, -23.81424706376357392 ) ) ;
#25886=ADVANCED_FACE ( 'NONE', ( #11554 ), #8533, .F. ) ;
#25892=B_SPLINE_CURVE_WITH_KNOTS ( 'NONE', 3,
 ( #3482, #1324, #7540, #16742, #4461, #16117 ),
 .UNSPECIFIED., .F., .F.,
 ( 4, 2, 4 ),
 ( 6.505213034913026604E-19, 0.0004335151646191473464, 0.0008670303292382940423 ),
 .UNSPECIFIED. ) ;
#25907=CARTESIAN_POINT ( 'NONE',  ( -55.25719721206881729, 0.007063345920777610795, -0.008651607285660192076 ) ) ;
#25910=VERTEX_POINT ( 'NONE', #6823 ) ;
#25912=ORIENTED_EDGE ( 'NONE', *, *, #26374, .F. ) ;
#25914=CARTESIAN_POINT ( 'NONE',  ( -22.34422965417126861, 34.15536449444089584, -16.46028608106120572 ) ) ;
#25918=CARTESIAN_POINT ( 'NONE',  ( -20.20700224038492365, 23.35150625415685255, 18.19058640100197977 ) ) ;
#25919=CARTESIAN_POINT ( 'NONE',  ( -55.25297051322618813, -0.006313402748432862636, 0.01354497706059893877 ) ) ;
#25932=ORIENTED_EDGE ( 'NONE', *, *, #26734, .F. ) ;
#25939=CARTESIAN_POINT ( 'NONE',  ( -1.019300379054419725, 35.83762006677400791, -28.53917295602911253 ) ) ;
#25946=CARTESIAN_POINT ( 'NONE',  ( -1.046936909428679563, -1.275306677858562221, -45.77873603877005593 ) ) ;
#25950=CARTESIAN_POINT ( 'NONE',  ( -20.20612091757422135, -10.22177757278296184, 27.77903622052264865 ) ) ;
#25955=CARTESIAN_POINT ( 'NONE',  ( -1.045287976400362417, 37.92705037016796155, 25.66401692419947977 ) ) ;
#25961=CARTESIAN_POINT ( 'NONE',  ( -1.056502255334264895, -26.51074901220476576, 37.35734037467662461 ) ) ;
#25975=CARTESIAN_POINT ( 'NONE',  ( -1.056502255334264895, 43.40574022158773460, -14.64009593116116292 ) ) ;
#25978=( BOUNDED_SURFACE ( )  B_SPLINE_SURFACE ( 3, 1, ( 
 ( #9435, #22538 ),
 ( #16183, #16325 ),
 ( #27105, #24990 ),
 ( #18325, #2805 ) ),
 .UNSPECIFIED., .F., .F., .F. ) 
 B_SPLINE_SURFACE_WITH_KNOTS ( ( 4, 4 ),
 ( 2, 2 ),
 ( 0.000000000000000000, 1.000000000000000000 ),
 ( 0.000000000000000000, 1.000000000000000000 ),
 .UNSPECIFIED. ) 
 GEOMETRIC_REPRESENTATION_ITEM ( )  RATIONAL_B_SPLINE_SURFACE ( (
 ( 1.000000000000000000, 1.000000000000000000),
 ( 0.7789835883360576307, 0.9689951854195403280),
 ( 0.7789835883360576307, 0.9689951854195403280),
 ( 1.000000000000000000, 1.000000000000000000) ) ) 
 REPRESENTATION_ITEM ( '' )  SURFACE ( )  );
#25979=ORIENTED_EDGE ( 'NONE', *, *, #23285, .F. ) ;
#25981=CARTESIAN_POINT ( 'NONE',  ( -8.259864102781673267, -25.58601832199047266, 46.42816643551597622 ) ) ;
#25983=ORIENTED_EDGE ( 'NONE', *, *, #21152, .T. ) ;
#25985=CARTESIAN_POINT ( 'NONE',  ( -2.904412668506660911, -11.97478724945543860, -46.12477647685269488 ) ) ;
#25987=CARTESIAN_POINT ( 'NONE',  ( -20.90916690077964546, -35.64494649500671386, 17.17795951644694341 ) ) ;
#25996=CARTESIAN_POINT ( 'NONE',  ( -1.050231094221210082, 13.91061116148191878, -43.63617436699743024 ) ) ;
#25999=CARTESIAN_POINT ( 'NONE',  ( -20.24399999263415140, 7.930419334766598993, 28.55700515887712854 ) ) ;
#26001=CARTESIAN_POINT ( 'NONE',  ( -20.20700224038492721, 24.51628800869048419, -16.58740185276719359 ) ) ;
#26004=VERTEX_POINT ( 'NONE', #12141 ) ;
#26017=CARTESIAN_POINT ( 'NONE',  ( -2.911734481061372115, -36.84482841982624990, 30.23325065583398441 ) ) ;
#26021=CARTESIAN_POINT ( 'NONE',  ( -55.25719721206881729, -0.01079965405819840671, -0.002847566758682798602 ) ) ;
#26034=CARTESIAN_POINT ( 'NONE',  ( -20.20700224038492010, 27.82980252387833886, 10.08426345511560207 ) ) ;
#26038=DIRECTION ( 'NONE',  ( 1.000000000000000000, -6.938893903907226837E-18, 1.734723475976806709E-18 ) ) ;
#26041=EDGE_LOOP ( 'NONE', ( #4059, #18133, #16986, #4485 ) ) ;
#26042=ORIENTED_EDGE ( 'NONE', *, *, #22744, .T. ) ;
#26055=DIRECTION ( 'NONE',  ( -0.7071067818211357325, 4.902845705138444274E-18, 0.7071067805519594129 ) ) ;
#26059=EDGE_LOOP ( 'NONE', ( #366, #27245, #1935, #28213 ) ) ;
#26061=VERTEX_POINT ( 'NONE', #18200 ) ;
#26068=DIRECTION ( 'NONE',  ( -1.000000000000000000, 6.938893903907226837E-18, -1.734723475976806709E-18 ) ) ;
#26080=CARTESIAN_POINT ( 'NONE',  ( -20.57838717382308147, -16.28767523336139078, -25.16001208503099917 ) ) ;
#26084=DIRECTION ( 'NONE',  ( 0.7563875759206388771, -0.5490129373055229189, 0.3556158456312960015 ) ) ;
#26085=VERTEX_POINT ( 'NONE', #18338 ) ;
#26091=B_SPLINE_CURVE_WITH_KNOTS ( 'NONE', 3,
 ( #2641, #18033, #15885, #9850 ),
 .UNSPECIFIED., .F., .F.,
 ( 4, 4 ),
 ( 1.906343156168367839E-16, 0.0009910334943225120648 ),
 .UNSPECIFIED. ) ;
#26094=CARTESIAN_POINT ( 'NONE',  ( -23.79223135445720771, 28.60983116549966354, -16.82181692922826599 ) ) ;
#26104=VERTEX_POINT ( 'NONE', #26843 ) ;
#26105=EDGE_LOOP ( 'NONE', ( #16317, #16898, #19417, #10354 ) ) ;
#26107=CARTESIAN_POINT ( 'NONE',  ( -55.24271866751342941, -0.006671293903668846365, 0.006757859501006202411 ) ) ;
#26109=CARTESIAN_POINT ( 'NONE',  ( -9.156249394959706578, 38.89149400288462033, 38.17928057391947760 ) ) ;
#26111=CARTESIAN_POINT ( 'NONE',  ( -20.57838717382308147, -25.16001208503093522, 16.28767523336148315 ) ) ;
#26113=CARTESIAN_POINT ( 'NONE',  ( -8.786685647604889127, 9.545808661480615243, -52.67761315067287597 ) ) ;
#26118=CARTESIAN_POINT ( 'NONE',  ( -1.031422197589716205, 12.69107518035502835, -44.01264471863851924 ) ) ;
#26128=CARTESIAN_POINT ( 'NONE',  ( 2.078045971014549723E-18, -1.958632391140620919E-19, 37.50000000000001421 ) ) ;
#26130=CARTESIAN_POINT ( 'NONE',  ( -8.786685647604720373, -47.14957014837338534, -25.35688121747513435 ) ) ;
#26131=CARTESIAN_POINT ( 'NONE',  ( -1.046936909428696882, 12.93351869073272908, -43.93225665392618851 ) ) ;
#26136=CARTESIAN_POINT ( 'NONE',  ( -22.23342874802670011, -31.55488258420090375, -2.180636882146402833 ) ) ;
#26139=ORIENTED_EDGE ( 'NONE', *, *, #1745, .F. ) ;
#26144=B_SPLINE_CURVE_WITH_KNOTS ( 'NONE', 3,
 ( #16937, #19514, #2082, #25999, #3843, #1803 ),
 .UNSPECIFIED., .F., .F.,
 ( 4, 2, 4 ),
 ( 4.906538933386797396E-18, 0.0004335151646191504906, 0.0008670303292382959938 ),
 .UNSPECIFIED. ) ;
#26145=DIRECTION ( 'NONE',  ( 0.000000000000000000, 1.000000000000000000, 0.000000000000000000 ) ) ;
#26147=B_SPLINE_CURVE_WITH_KNOTS ( 'NONE', 3,
 ( #5302, #27017, #18550, #27317, #22891, #27171, #16384, #14076 ),
 .UNSPECIFIED., .F., .F.,
 ( 4, 2, 2, 4 ),
 ( 2.196627850418165012E-16, 0.002761568181852864633, 0.005523136363705508957, 0.01104627272741078546 ),
 .UNSPECIFIED. ) ;
#26149=CARTESIAN_POINT ( 'NONE',  ( -1.031422197589711764, -1.530725436377143867, 45.78027046666444022 ) ) ;
#26166=CARTESIAN_POINT ( 'NONE',  ( -20.57838717382308147, -10.78122205916981358, 27.96569011373096814 ) ) ;
#26185=ORIENTED_EDGE ( 'NONE', *, *, #27846, .T. ) ;
#26198=ORIENTED_EDGE ( 'NONE', *, *, #140, .T. ) ;
#26205=CARTESIAN_POINT ( 'NONE',  ( -1.048996300304493978, -43.78665266739846373, -13.42280206896960060 ) ) ;
#26212=CARTESIAN_POINT ( 'NONE',  ( -1.239374126674604337, -38.61989855450958231, -25.08410696974230092 ) ) ;
#26218=CARTESIAN_POINT ( 'NONE',  ( -2.911734481061388990, -47.57875121082950898, 2.802366807346684308 ) ) ;
#26224=ORIENTED_EDGE ( 'NONE', *, *, #15387, .T. ) ;
#26227=PRODUCT_DEFINITION_SHAPE ( 'NONE', 'NONE',  #28439 ) ;
#26233=CARTESIAN_POINT ( 'NONE',  ( -23.77929240705206126, 25.06639637888459404, 26.20227034809527211 ) ) ;
#26236=CARTESIAN_POINT ( 'NONE',  ( -20.24399999263414429, -23.20123049637379253, -18.44171895251388094 ) ) ;
#26237=CONICAL_SURFACE ( 'NONE', #1878, 34.60786435723138510, 0.8559913436420825139 ) ;
#26238=EDGE_CURVE ( 'NONE', #12584, #25403, #14342, .T. ) ;
#26242=DIRECTION ( 'NONE',  ( 1.000000000000000000, -6.938893903907226837E-18, 1.734723475976806709E-18 ) ) ;
#26243=CARTESIAN_POINT ( 'NONE',  ( -22.23342874802668234, 7.677086057585391643, 30.68433055777672180 ) ) ;
#26244=CARTESIAN_POINT ( 'NONE',  ( -55.24271866751342941, -0.009369360294295350430, -0.001545935011630812216 ) ) ;
#26245=CARTESIAN_POINT ( 'NONE',  ( -55.24728320129491266, -0.01137345571546789259, 0.009072670231975133240 ) ) ;
#26249=CARTESIAN_POINT ( 'NONE',  ( -55.24728320129491266, 0.009072670231975488858, 0.01137345571546827770 ) ) ;
#26256=CARTESIAN_POINT ( 'NONE',  ( -1.045287976400362417, -28.14015102489855735, -36.12803364096578207 ) ) ;
#26264=CONICAL_SURFACE ( 'NONE', #12013, 34.60786435723138510, 0.8559913436420825139 ) ;
#26273=DIRECTION ( 'NONE',  ( 0.000000000000000000, 5.223019709707975211E-21, -1.000000000000000000 ) ) ;
#26275=ORIENTED_EDGE ( 'NONE', *, *, #261, .F. ) ;
#26283=CARTESIAN_POINT ( 'NONE',  ( -25.21435515916043713, 16.39063784838786475, 30.48034229288620622 ) ) ;
#26290=CARTESIAN_POINT ( 'NONE',  ( -1.583189561560255143, -38.94740041318274848, 25.21827308671275247 ) ) ;
#26292=CARTESIAN_POINT ( 'NONE',  ( -5.986830583229479252, 33.39046620690970002, 38.20088153919464702 ) ) ;
#26297=DIRECTION ( 'NONE',  ( 0.000000000000000000, 5.223019709708233256E-21, -1.000000000000000000 ) ) ;
#26302=( BOUNDED_SURFACE ( )  B_SPLINE_SURFACE ( 3, 1, ( 
 ( #15519, #9205 ),
 ( #24331, #4593 ),
 ( #15663, #19852 ),
 ( #11081, #11222 ) ),
 .UNSPECIFIED., .F., .F., .F. ) 
 B_SPLINE_SURFACE_WITH_KNOTS ( ( 4, 4 ),
 ( 2, 2 ),
 ( 0.000000000000000000, 1.000000000000000000 ),
 ( 0.000000000000000000, 1.000000000000000000 ),
 .UNSPECIFIED. ) 
 GEOMETRIC_REPRESENTATION_ITEM ( )  RATIONAL_B_SPLINE_SURFACE ( (
 ( 1.000000000000000000, 1.000000000000000000),
 ( 0.7789835883360576307, 0.9689951854195403280),
 ( 0.7789835883360576307, 0.9689951854195403280),
 ( 1.000000000000000000, 1.000000000000000000) ) ) 
 REPRESENTATION_ITEM ( '' )  SURFACE ( )  );
#26303=CARTESIAN_POINT ( 'NONE',  ( -55.24390624410018802, -0.004572280736701530256, -0.009374879212970928244 ) ) ;
#26311=CARTESIAN_POINT ( 'NONE',  ( -28.13707043255157103, 14.07296284901359051, 18.06394523322437706 ) ) ;
#26323=CARTESIAN_POINT ( 'NONE',  ( -1.031422197589716205, -43.06660437151320053, -15.60268798220621633 ) ) ;
#26331=CONICAL_SURFACE ( 'NONE', #8003, 34.60786435723138510, 0.8559913436420825139 ) ;
#26334=ORIENTED_EDGE ( 'NONE', *, *, #2462, .T. ) ;
#26336=VERTEX_POINT ( 'NONE', #7258 ) ;
#26337=CARTESIAN_POINT ( 'NONE',  ( -20.47566262905009538, -18.81547655725230328, 23.19796652405694459 ) ) ;
#26340=CARTESIAN_POINT ( 'NONE',  ( -1.583189561560255143, -36.01941156322808979, -29.24830400313152623 ) ) ;
#26341=( BOUNDED_SURFACE ( )  B_SPLINE_SURFACE ( 3, 1, ( 
 ( #28021, #21275 ),
 ( #10358, #8321 ),
 ( #21546, #14789 ),
 ( #17087, #25612 ) ),
 .UNSPECIFIED., .F., .F., .F. ) 
 B_SPLINE_SURFACE_WITH_KNOTS ( ( 4, 4 ),
 ( 2, 2 ),
 ( 0.000000000000000000, 1.000000000000000000 ),
 ( 0.000000000000000000, 1.000000000000000000 ),
 .UNSPECIFIED. ) 
 GEOMETRIC_REPRESENTATION_ITEM ( )  RATIONAL_B_SPLINE_SURFACE ( (
 ( 1.000000000000000000, 1.000000000000000000),
 ( 0.9593753223639863714, 0.9995975284513187731),
 ( 0.9593753223639863714, 0.9995975284513187731),
 ( 1.000000000000000000, 1.000000000000000000) ) ) 
 REPRESENTATION_ITEM ( '' )  SURFACE ( )  );
#26346=CARTESIAN_POINT ( 'NONE',  ( -1.050230347699840694, -0.0002315326057593219944, 45.79907861674081460 ) ) ;
#26353=CARTESIAN_POINT ( 'NONE',  ( -2.911734481061415636, 25.69892591260268588, -40.13920818157085080 ) ) ;
#26355=CARTESIAN_POINT ( 'NONE',  ( -20.47566262905009538, -25.06314747784824348, 16.24827521404678521 ) ) ;
#26368=B_SPLINE_CURVE_WITH_KNOTS ( 'NONE', 3,
 ( #2036, #21347, #17019, #10426, #23946, #15125 ),
 .UNSPECIFIED., .F., .F.,
 ( 4, 2, 4 ),
 ( 3.525929482785130599E-16, 0.003576372551511158761, 0.007152745103021965374 ),
 .UNSPECIFIED. ) ;
#26371=CARTESIAN_POINT ( 'NONE',  ( -1.539763995773681726, -25.17088606276573515, -38.84665165401054310 ) ) ;
#26372=ADVANCED_FACE ( 'NONE', ( #27234 ), #20419, .F. ) ;
#26374=EDGE_CURVE ( 'NONE', #12467, #9726, #25892, .T. ) ;
#26376=CARTESIAN_POINT ( 'NONE',  ( -24.53239521893627995, 33.25736993155740606, -6.738460611583019677 ) ) ;
#26380=CARTESIAN_POINT ( 'NONE',  ( -1.323439229708141429, 12.01475235539445485, -44.47813215539048315 ) ) ;
#26383=VERTEX_POINT ( 'NONE', #23172 ) ;
#26388=CARTESIAN_POINT ( 'NONE',  ( -1.044557008772707407, 37.98985164565329598, -25.56990300676994821 ) ) ;
#26389=B_SPLINE_CURVE_WITH_KNOTS ( 'NONE', 3,
 ( #22954, #904, #14274, #11710, #26948, #16013 ),
 .UNSPECIFIED., .F., .F.,
 ( 4, 2, 4 ),
 ( 1.552747097607904257E-16, 0.003570751334075639161, 0.007141502668151123064 ),
 .UNSPECIFIED. ) ;
#26390=CARTESIAN_POINT ( 'NONE',  ( -1.031422197589716205, -45.78027046666443312, 1.530725436377931237 ) ) ;
#26393=B_SPLINE_CURVE_WITH_KNOTS ( 'NONE', 3,
 ( #13200, #6463, #2401, #13074, #17668, #24035, #4149 ),
 .UNSPECIFIED., .F., .F.,
 ( 4, 3, 4 ),
 ( 0.000000000000000000, 0.006568092053401791003, 0.02506242213020846987 ),
 .UNSPECIFIED. ) ;
#26394=ORIENTED_EDGE ( 'NONE', *, *, #1493, .T. ) ;
#26396=VERTEX_POINT ( 'NONE', #11633 ) ;
#26398=CARTESIAN_POINT ( 'NONE',  ( -1.048172774974297949, -37.64158596421231096, -26.08722459372772562 ) ) ;
#26399=ORIENTED_EDGE ( 'NONE', *, *, #13703, .T. ) ;
#26414=CARTESIAN_POINT ( 'NONE',  ( -28.41354790283022069, 23.16239616762931064, 1.249099604787156981 ) ) ;
#26416=CARTESIAN_POINT ( 'NONE',  ( -20.37983603106074426, -29.73529213200290400, -1.508851015062473211 ) ) ;
#26424=CARTESIAN_POINT ( 'NONE',  ( -20.57838717382308147, 25.16001208503129760, 16.28767523336092893 ) ) ;
#26425=ORIENTED_EDGE ( 'NONE', *, *, #19618, .F. ) ;
#26431=CARTESIAN_POINT ( 'NONE',  ( -1.583189561560252701, 25.21827308671288392, 38.94740041318267032 ) ) ;
#26439=EDGE_CURVE ( 'NONE', #25441, #18255, #9753, .T. ) ;
#26447=CARTESIAN_POINT ( 'NONE',  ( -55.24390624410018802, 0.009374879212967415429, 0.004572280736702902422 ) ) ;
#26449=CARTESIAN_POINT ( 'NONE',  ( -55.24271866751342941, 0.006671293903669565407, -0.006757859501006440936 ) ) ;
#26454=CARTESIAN_POINT ( 'NONE',  ( -16.86833981943413363, 43.82216161736224791, -5.948101187261743306 ) ) ;
#26464=CARTESIAN_POINT ( 'NONE',  ( -55.24271866751342941, 0.009388511352200529583, -0.001425019990779194824 ) ) ;
#26467=B_SPLINE_CURVE_WITH_KNOTS ( 'NONE', 3,
 ( #15035, #23855, #12873, #10747, #28275, #17338 ),
 .UNSPECIFIED., .F., .F.,
 ( 4, 2, 4 ),
 ( 4.296969928001729735E-16, 0.003576372551511233788, 0.007152745103022037365 ),
 .UNSPECIFIED. ) ;
#26469=CARTESIAN_POINT ( 'NONE',  ( -21.81686047589415622, 38.17230180719270294, 5.181745222995608025 ) ) ;
#26470=FACE_OUTER_BOUND ( 'NONE', #661, .T. ) ;
#26481=CARTESIAN_POINT ( 'NONE',  ( -1.259920593601969729, -12.06711544331594865, -44.39818421957811978 ) ) ;
#26488=CARTESIAN_POINT ( 'NONE',  ( -1.619063947482197729, 16.67502769180622835, 43.26576862488415287 ) ) ;
#26498=ORIENTED_EDGE ( 'NONE', *, *, #9684, .F. ) ;
#26499=CARTESIAN_POINT ( 'NONE',  ( -21.41430102051752016, 23.81424706376365918, -19.54553566814595200 ) ) ;
#26510=CARTESIAN_POINT ( 'NONE',  ( -20.57838717382308147, -18.89542499756516847, -23.26537097894098594 ) ) ;
#26512=CARTESIAN_POINT ( 'NONE',  ( -1.619063947482197729, -25.20140673341401438, -38.92136151114898723 ) ) ;
#26514=FACE_OUTER_BOUND ( 'NONE', #8159, .T. ) ;
#26515=CARTESIAN_POINT ( 'NONE',  ( -1.155001620486242553, 42.97366440495935080, 16.13799328198379257 ) ) ;
#26517=CARTESIAN_POINT ( 'NONE',  ( -1.058473599757823180, 12.47539220917862934, -44.07591602137159725 ) ) ;
#26518=CARTESIAN_POINT ( 'NONE',  ( -55.25719721206881729, -0.009391134844732829459, -0.006045473558784549006 ) ) ;
#26525=PLANE ( 'NONE',  #1532 ) ;
#26526=CARTESIAN_POINT ( 'NONE',  ( -20.20700224038492721, 10.08426345511588984, -27.82980252387822517 ) ) ;
#26528=EDGE_CURVE ( 'NONE', #9465, #26085, #14220, .T. ) ;
#26530=CARTESIAN_POINT ( 'NONE',  ( -2.904412668506672457, -2.864640348250298008, 47.56768199507434502 ) ) ;
#26536=B_SPLINE_CURVE_WITH_KNOTS ( 'NONE', 3,
 ( #6542, #8988, #23972, #4373, #15294, #10861, #24248, #28393 ),
 .UNSPECIFIED., .F., .F.,
 ( 4, 2, 2, 4 ),
 ( 2.237231151233565423E-16, 0.002761568181852865501, 0.005523136363705507222, 0.01104627272741080454 ),
 .UNSPECIFIED. ) ;
#26537=CARTESIAN_POINT ( 'NONE',  ( -1.619063947482197729, -16.67502769180532596, 43.26576862488450104 ) ) ;
#26542=EDGE_CURVE ( 'NONE', #22192, #20045, #18503, .T. ) ;
#26543=CARTESIAN_POINT ( 'NONE',  ( -8.786685647604890903, 38.68584556812300690, -37.00619870957947910 ) ) ;
#26544=( BOUNDED_SURFACE ( )  B_SPLINE_SURFACE ( 3, 1, ( 
 ( #502, #15594 ),
 ( #4531, #5104 ),
 ( #4828, #26969 ),
 ( #2510, #18053 ) ),
 .UNSPECIFIED., .F., .F., .F. ) 
 B_SPLINE_SURFACE_WITH_KNOTS ( ( 4, 4 ),
 ( 2, 2 ),
 ( 0.000000000000000000, 1.000000000000000000 ),
 ( 0.000000000000000000, 1.000000000000000000 ),
 .UNSPECIFIED. ) 
 GEOMETRIC_REPRESENTATION_ITEM ( )  RATIONAL_B_SPLINE_SURFACE ( (
 ( 1.000000000000000000, 1.000000000000000000),
 ( 0.9934239774497837239, 0.8357310067453919133),
 ( 0.9934239774497837239, 0.8357310067453919133),
 ( 1.000000000000000000, 1.000000000000000000) ) ) 
 REPRESENTATION_ITEM ( '' )  SURFACE ( )  );
#26545=DIRECTION ( 'NONE',  ( 1.000000000000000000, -6.938893903907226837E-18, 1.734723475976806709E-18 ) ) ;
#26560=CARTESIAN_POINT ( 'NONE',  ( -8.786685647604894456, 7.199674155859698388, 53.04920435127174017 ) ) ;
#26561=CARTESIAN_POINT ( 'NONE',  ( -12.94347594948475333, -48.30328466416771960, -6.555928820869143969 ) ) ;
#26565=CARTESIAN_POINT ( 'NONE',  ( -4.473127245936434626, -18.25038884639903003, -45.82513704981538183 ) ) ;
#26566=EDGE_CURVE ( 'NONE', #22983, #1293, #12338, .T. ) ;
#26571=LINE ( 'NONE', #6873, #17021 ) ;
#26584=CARTESIAN_POINT ( 'NONE',  ( -20.20700224038492721, 29.58392382092673500, -0.9908225410479557516 ) ) ;
#26590=CARTESIAN_POINT ( 'NONE',  ( -28.41354790283022069, 18.00456980371900784, -14.62505768302807319 ) ) ;
#26593=CARTESIAN_POINT ( 'NONE',  ( -1.050230347360791017, 0.0004630652117437840452, -45.79907861464602092 ) ) ;
#26600=DIRECTION ( 'NONE',  ( 1.000000000000000000, -6.938893903907226837E-18, -5.541455922705464902E-20 ) ) ;
#26610=ORIENTED_EDGE ( 'NONE', *, *, #12158, .T. ) ;
#26616=CARTESIAN_POINT ( 'NONE',  ( -55.24271866751342941, 0.006671293903668397071, 0.006757859501010046559 ) ) ;
#26620=EDGE_LOOP ( 'NONE', ( #16912, #21007, #14027, #1315 ) ) ;
#26623=CARTESIAN_POINT ( 'NONE',  ( -55.25297051322618813, 0.01019003092403740832, -0.01093108995495187946 ) ) ;
#26630=B_SPLINE_CURVE_WITH_KNOTS ( 'NONE', 3,
 ( #4004, #4677, #13449, #6190, #23616, #6997, #24564 ),
 .UNSPECIFIED., .F., .F.,
 ( 4, 3, 4 ),
 ( 2.453269466693398621E-17, 0.009512539173626417474, 0.02506242213020847681 ),
 .UNSPECIFIED. ) ;
#26633=B_SPLINE_CURVE_WITH_KNOTS ( 'NONE', 3,
 ( #27710, #6540, #24108, #26243, #18027, #24245 ),
 .UNSPECIFIED., .F., .F.,
 ( 4, 2, 4 ),
 ( 4.286557520396696095E-16, 0.003576372551511235957, 0.007152745103022043437 ),
 .UNSPECIFIED. ) ;
#26634=CARTESIAN_POINT ( 'NONE',  ( -55.24271866751342941, -0.004365563123935077734, -0.008433070970613952902 ) ) ;
#26636=CARTESIAN_POINT ( 'NONE',  ( -55.24271866751342941, -0.009369360294294061531, 0.001545935011626861600 ) ) ;
#26638=VERTEX_POINT ( 'NONE', #17496 ) ;
#26643=ORIENTED_EDGE ( 'NONE', *, *, #20899, .F. ) ;
#26665=CARTESIAN_POINT ( 'NONE',  ( -1.619063947482197729, -43.26576862488445130, -16.67502769180545386 ) ) ;
#26667=ORIENTED_EDGE ( 'NONE', *, *, #11972, .T. ) ;
#26672=CARTESIAN_POINT ( 'NONE',  ( -20.57838717382308147, -29.92853265176830746, 1.611677988432673070 ) ) ;
#26673=ADVANCED_FACE ( 'NONE', ( #13044 ), #14536, .F. ) ;
#26686=CARTESIAN_POINT ( 'NONE',  ( -55.24271866751342941, 0.008488649505346581442, -0.004256484107793381474 ) ) ;
#26694=ORIENTED_EDGE ( 'NONE', *, *, #11864, .F. ) ;
#26708=AXIS2_PLACEMENT_3D ( 'NONE', #8096, #23640, #4166 ) ;
#26713=VERTEX_POINT ( 'NONE', #15766 ) ;
#26718=CARTESIAN_POINT ( 'NONE',  ( -20.20700224038492721, 16.58740185276746359, 24.51628800869029234 ) ) ;
#26719=CARTESIAN_POINT ( 'NONE',  ( -21.81686047589426991, 6.867757412721210208, 37.90526371014249918 ) ) ;
#26734=EDGE_CURVE ( 'NONE', #9765, #9035, #6116, .T. ) ;
#26735=CARTESIAN_POINT ( 'NONE',  ( -1.048994561756802391, 0.7655149579823430361, -45.79144455904140187 ) ) ;
#26736=CARTESIAN_POINT ( 'NONE',  ( -25.21435515916043713, 16.39063784838786475, 30.48034229288620622 ) ) ;
#26746=EDGE_LOOP ( 'NONE', ( #20135, #3751, #20660, #18993 ) ) ;
#26750=ORIENTED_EDGE ( 'NONE', *, *, #28081, .F. ) ;
#26754=B_SPLINE_CURVE_WITH_KNOTS ( 'NONE', 3,
 ( #3268, #21094, #18802, #20668, #14049, #18950 ),
 .UNSPECIFIED., .F., .F.,
 ( 4, 2, 4 ),
 ( 1.504716382203053018E-16, 0.003570751334075636125, 0.007141502668151121329 ),
 .UNSPECIFIED. ) ;
#26763=CARTESIAN_POINT ( 'NONE',  ( -8.786685647604898008, 48.22796981442802178, 23.24040270374343464 ) ) ;
#26764=ORIENTED_EDGE ( 'NONE', *, *, #17287, .T. ) ;
#26767=EDGE_LOOP ( 'NONE', ( #20003, #21225, #7579, #18768 ) ) ;
#26779=CARTESIAN_POINT ( 'NONE',  ( -8.786685647604887350, -38.68584556812326980, -37.00619870957918778 ) ) ;
#26782=ORIENTED_EDGE ( 'NONE', *, *, #11580, .F. ) ;
#26783=ORIENTED_EDGE ( 'NONE', *, *, #5469, .T. ) ;
#26784=CARTESIAN_POINT ( 'NONE',  ( -1.619063947482197729, -43.26576862488421682, 16.67502769180607203 ) ) ;
#26790=CARTESIAN_POINT ( 'NONE',  ( -20.38016308990358638, 29.73560196176844528, -1.509191766064308382 ) ) ;
#26803=CARTESIAN_POINT ( 'NONE',  ( -25.21435515916043357, -6.169479169075226643, 34.05351380035340014 ) ) ;
#26804=CARTESIAN_POINT ( 'NONE',  ( -1.058197053496172213, 42.99116279335175506, 15.81317659443640444 ) ) ;
#26809=CARTESIAN_POINT ( 'NONE',  ( -1.044556982611273277, 12.57890920527776224, -44.03203163107531282 ) ) ;
#26815=CARTESIAN_POINT ( 'NONE',  ( -1.045287976400383290, 36.12803364096649972, 28.14015102489766917 ) ) ;
#26817=CARTESIAN_POINT ( 'NONE',  ( -1.464342487929851222, 16.57334911911573982, 43.13914623307943685 ) ) ;
#26818=ADVANCED_FACE ( 'NONE', ( #15787 ), #23387, .F. ) ;
#26819=ORIENTED_EDGE ( 'NONE', *, *, #20722, .T. ) ;
#26820=CARTESIAN_POINT ( 'NONE',  ( -1.019300379054419947, 16.06793277091992067, -42.90269154183433642 ) ) ;
#26822=CARTESIAN_POINT ( 'NONE',  ( -25.21435515916025594, 1.749597353048488237E-16, -4.373993382621220594E-17 ) ) ;
#26826=VERTEX_POINT ( 'NONE', #27259 ) ;
#26831=EDGE_CURVE ( 'NONE', #22079, #9286, #5991, .T. ) ;
#26839=CARTESIAN_POINT ( 'NONE',  ( -1.045287976400351981, -15.59869763335126436, -43.05558670614231431 ) ) ;
#26843=CARTESIAN_POINT ( 'NONE',  ( -1.045287976400379737, -37.92705037016725100, 25.66401692420055269 ) ) ;
#26859=ORIENTED_EDGE ( 'NONE', *, *, #21634, .F. ) ;
#26861=CARTESIAN_POINT ( 'NONE',  ( -55.24340739397742084, -0.003826481709803442217, 0.009386184976286439385 ) ) ;
#26869=CARTESIAN_POINT ( 'NONE',  ( -1.155001620486262759, 16.13799328198422245, -42.97366440495917317 ) ) ;
#26874=CARTESIAN_POINT ( 'NONE',  ( -55.24198130335446422, -0.006617369590171728877, 0.006527480770973505091 ) ) ;
#26875=CARTESIAN_POINT ( 'NONE',  ( -23.77929240705205771, -25.06639637888440220, -26.20227034809546041 ) ) ;
#26876=VERTEX_POINT ( 'NONE', #10851 ) ;
#26881=CARTESIAN_POINT ( 'NONE',  ( -1.155001620486248548, -38.31519699443482097, 25.28075036143263077 ) ) ;
#26885=CARTESIAN_POINT ( 'NONE',  ( -20.47566262905010603, 1.586617686065558974, -29.82700878811084522 ) ) ;
#26905=DIRECTION ( 'NONE',  ( -5.541455922705464902E-20, 5.223019709708320524E-21, -1.000000000000000000 ) ) ;
#26912=CARTESIAN_POINT ( 'NONE',  ( -55.24271866751342941, 0.008433070970614256479, -0.004365563123935527895 ) ) ;
#26913=CARTESIAN_POINT ( 'NONE',  ( -1.464342487929863212, 43.13914623307960738, -16.57334911911526731 ) ) ;
#26919=B_SPLINE_CURVE_WITH_KNOTS ( 'NONE', 3,
 ( #11147, #8699, #2063, #12861, #21654, #19768, #21941, #11007, #24253, #19629, #8560, #27989, #17326 ),
 .UNSPECIFIED., .F., .F.,
 ( 4, 3, 3, 3, 4 ),
 ( 9.813077866773594792E-18, 0.0007657099931970512375, 0.001531419946797918071, 0.002296279302920157302, 0.003061450627205767206 ),
 .UNSPECIFIED. ) ;
#26920=CARTESIAN_POINT ( 'NONE',  ( -6.588769196390753535, -38.42957692275866322, -34.04709086065298607 ) ) ;
#26923=ORIENTED_EDGE ( 'NONE', *, *, #19615, .F. ) ;
#26926=CARTESIAN_POINT ( 'NONE',  ( -23.79248802219730052, 24.83956736572410051, -22.01156985585177495 ) ) ;
#26927=VERTEX_POINT ( 'NONE', #17176 ) ;
#26928=ORIENTED_EDGE ( 'NONE', *, *, #8376, .T. ) ;
#26932=CARTESIAN_POINT ( 'NONE',  ( -1.045287976400351981, 36.12803364096590997, -28.14015102489844011 ) ) ;
#26934=CARTESIAN_POINT ( 'NONE',  ( -1.045287976400362417, 43.05558670614268379, 15.59869763335023229 ) ) ;
#26937=CARTESIAN_POINT ( 'NONE',  ( -20.21097721712959938, -24.14932359587277233, 17.13687106192370280 ) ) ;
#26948=CARTESIAN_POINT ( 'NONE',  ( -24.53237795827027767, -29.54731592868574808, -16.68575684089485023 ) ) ;
#26951=CARTESIAN_POINT ( 'NONE',  ( -1.044556982611269502, 15.70482750345296452, 43.01635920718332784 ) ) ;
#26954=EDGE_CURVE ( 'NONE', #12126, #4463, #464, .T. ) ;
#26955=ORIENTED_EDGE ( 'NONE', *, *, #14433, .F. ) ;
#26965=EDGE_CURVE ( 'NONE', #17046, #10778, #16904, .T. ) ;
#26969=CARTESIAN_POINT ( 'NONE',  ( -1.019300379054419947, -28.53917295602871818, 35.83762006677432055 ) ) ;
#26972=CARTESIAN_POINT ( 'NONE',  ( -1.050231094221210082, 26.71409683968617799, -37.20185272688468814 ) ) ;
#26984=ORIENTED_EDGE ( 'NONE', *, *, #17412, .F. ) ;
#26985=B_SPLINE_CURVE_WITH_KNOTS ( 'NONE', 3,
 ( #14590, #23395, #19328, #8266, #10431, #14873 ),
 .UNSPECIFIED., .F., .F.,
 ( 4, 2, 4 ),
 ( 7.757919228897728493E-18, 0.003570751334075633956, 0.007141502668151267913 ),
 .UNSPECIFIED. ) ;
#26987=EDGE_CURVE ( 'NONE', #4463, #21774, #7684, .T. ) ;
#26988=ORIENTED_EDGE ( 'NONE', *, *, #17095, .F. ) ;
#27004=CARTESIAN_POINT ( 'NONE',  ( -7.762687761849950397E-17, 3.022826910523253725E-17, 44.74884827092600403 ) ) ;
#27005=DIRECTION ( 'NONE',  ( 0.7637818620346801257, 0.5345501402766276167, -0.3617919495470772184 ) ) ;
#27011=CARTESIAN_POINT ( 'NONE',  ( -20.57838717382308147, -1.611677988432568709, -29.92853265176830746 ) ) ;
#27012=CARTESIAN_POINT ( 'NONE',  ( -8.786685647604887350, 53.04920435127183254, 7.199674155859139724 ) ) ;
#27015=ORIENTED_EDGE ( 'NONE', *, *, #18346, .F. ) ;
#27017=CARTESIAN_POINT ( 'NONE',  ( -2.265401668238146371, -29.73100299756539755, 36.42007794497283157 ) ) ;
#27027=EDGE_CURVE ( 'NONE', #11830, #11861, #22676, .T. ) ;
#27029=EDGE_LOOP ( 'NONE', ( #27344, #20920, #15346, #24593 ) ) ;
#27032=ORIENTED_EDGE ( 'NONE', *, *, #2319, .T. ) ;
#27039=CARTESIAN_POINT ( 'NONE',  ( -25.21435515916042647, 15.02493970636146692, -31.17620025257592786 ) ) ;
#27041=EDGE_CURVE ( 'NONE', #6478, #10003, #13560, .T. ) ;
#27043=ORIENTED_EDGE ( 'NONE', *, *, #3123, .F. ) ;
#27044=ORIENTED_EDGE ( 'NONE', *, *, #20876, .F. ) ;
#27046=CARTESIAN_POINT ( 'NONE',  ( -25.21435515916044423, -16.39063784838720395, 30.48034229288656505 ) ) ;
#27059=CARTESIAN_POINT ( 'NONE',  ( -1.044557008772706297, 44.03203053429572833, -12.57891310333364210 ) ) ;
#27061=EDGE_CURVE ( 'NONE', #13776, #14553, #12802, .T. ) ;
#27068=VERTEX_POINT ( 'NONE', #6678 ) ;
#27073=CARTESIAN_POINT ( 'NONE',  ( -1.539760825549686185, 2.469813586483733392, 46.22267384399377477 ) ) ;
#27078=EDGE_CURVE ( 'NONE', #13021, #24113, #5637, .T. ) ;
#27079=CARTESIAN_POINT ( 'NONE',  ( -23.77929240705206482, 17.17389748746964173, -31.93650644494346835 ) ) ;
#27083=ADVANCED_FACE ( 'NONE', ( #26514 ), #9326, .T. ) ;
#27091=CARTESIAN_POINT ( 'NONE',  ( -1.583189561560255143, 16.68617981233701997, -43.29471907393748609 ) ) ;
#27105=CARTESIAN_POINT ( 'NONE',  ( -55.25297051322618813, -0.007247191603131164853, -0.01306918787467609838 ) ) ;
#27106=EDGE_CURVE ( 'NONE', #2997, #5380, #7251, .T. ) ;
#27123=CARTESIAN_POINT ( 'NONE',  ( -20.20700224038492365, -8.199606986804534259, -28.44216453106533748 ) ) ;
#27126=ORIENTED_EDGE ( 'NONE', *, *, #25692, .F. ) ;
#27128=ORIENTED_EDGE ( 'NONE', *, *, #26374, .T. ) ;
#27134=ORIENTED_EDGE ( 'NONE', *, *, #17635, .F. ) ;
#27135=CARTESIAN_POINT ( 'NONE',  ( -1.155031165708878094, -16.13806347973029176, -42.97366960678595404 ) ) ;
#27138=CARTESIAN_POINT ( 'NONE',  ( -7.078251931573400491, -34.59014398252887190, 38.93060825814266934 ) ) ;
#27139=VECTOR ( 'NONE', #11505, 999.9999999999998863 ) ;
#27140=EDGE_LOOP ( 'NONE', ( #8701, #23627, #15012, #16517 ) ) ;
#27149=CARTESIAN_POINT ( 'NONE',  ( -15.02187109954782507, 8.264310930413024892, 45.60876405941875333 ) ) ;
#27154=CARTESIAN_POINT ( 'NONE',  ( -1.045287976400351981, 43.05558670614237116, -15.59869763335110449 ) ) ;
#27161=CARTESIAN_POINT ( 'NONE',  ( -25.21435515916025594, 1.749597353048488237E-16, -4.373993382621220594E-17 ) ) ;
#27165=FACE_OUTER_BOUND ( 'NONE', #6204, .T. ) ;
#27171=CARTESIAN_POINT ( 'NONE',  ( -6.588769196390751759, -34.04709086065287238, 38.42957692275880532 ) ) ;
#27172=AXIS2_PLACEMENT_3D ( 'NONE', #11783, #14065, #25037 ) ;
#27173=CARTESIAN_POINT ( 'NONE',  ( -20.38016308990357928, 28.74660391518355951, 7.753479680700641197 ) ) ;
#27175=CARTESIAN_POINT ( 'NONE',  ( -1.583189561560252701, 2.490696082059875138, -46.33203782964461936 ) ) ;
#27179=VERTEX_POINT ( 'NONE', #16709 ) ;
#27188=ORIENTED_EDGE ( 'NONE', *, *, #6380, .T. ) ;
#27189=CARTESIAN_POINT ( 'NONE',  ( -55.24300891470650754, -0.0003472257464211635897, -0.009812809446892990090 ) ) ;
#27197=CARTESIAN_POINT ( 'NONE',  ( -1.050229599974473516, -37.20249516760156183, 26.71319688967675177 ) ) ;
#27199=ADVANCED_FACE ( 'NONE', ( #9409 ), #1045, .T. ) ;
#27201=CARTESIAN_POINT ( 'NONE',  ( -2.904412668506661355, 36.79926976721492338, 30.27712468694946679 ) ) ;
#27203=CARTESIAN_POINT ( 'NONE',  ( -1.048171036023517466, -45.78635789057865679, -1.020520027228972504 ) ) ;
#27206=DIRECTION ( 'NONE',  ( 1.000000000000000000, -6.938893903907226837E-18, 1.734723475976806709E-18 ) ) ;
#27220=ADVANCED_FACE ( 'NONE', ( #19004 ), #3867, .F. ) ;
#27222=CARTESIAN_POINT ( 'NONE',  ( -2.265401668238147259, 25.45016726748371738, 39.53028715828205009 ) ) ;
#27227=EDGE_CURVE ( 'NONE', #4347, #1523, #7515, .T. ) ;
#27228=DIRECTION ( 'NONE',  ( 0.7563875759206388771, -0.6531865459554681008, -0.03500244528122332249 ) ) ;
#27234=FACE_OUTER_BOUND ( 'NONE', #456, .T. ) ;
#27240=CARTESIAN_POINT ( 'NONE',  ( -55.24340739397742794, 0.003826481709800397344, 0.009386184976285138343 ) ) ;
#27244=VECTOR ( 'NONE', #14800, 1000.000000000000000 ) ;
#27245=ORIENTED_EDGE ( 'NONE', *, *, #21152, .F. ) ;
#27251=DIRECTION ( 'NONE',  ( 1.000000000000000000, -6.938893903907226837E-18, 1.734723475976806709E-18 ) ) ;
#27256=EDGE_CURVE ( 'NONE', #11627, #1639, #21737, .T. ) ;
#27259=CARTESIAN_POINT ( 'NONE',  ( -20.20700224038492721, 28.44216453106548315, 8.199606986804035103 ) ) ;
#27263=AXIS2_PLACEMENT_3D ( 'NONE', #6878, #24598, #15623 ) ;
#27264=CARTESIAN_POINT ( 'NONE',  ( -21.41430102051745266, 30.75470819672112199, -1.815007301162081088 ) ) ;
#27275=CARTESIAN_POINT ( 'NONE',  ( -8.786685647604898008, 48.22796981442765940, -23.24040270374399952 ) ) ;
#27278=CARTESIAN_POINT ( 'NONE',  ( -20.90916690077959927, 28.59207721780146727, -27.35210456531384082 ) ) ;
#27281=CARTESIAN_POINT ( 'NONE',  ( -20.20700224038492010, 18.19058640100223556, -23.35150625415664649 ) ) ;
#27282=B_SPLINE_CURVE_WITH_KNOTS ( 'NONE', 3,
 ( #2741, #18419, #5187, #13963, #11818, #867, #9654, #27197, #2593, #24349, #15683, #17842, #15979 ),
 .UNSPECIFIED., .F., .F.,
 ( 4, 3, 3, 3, 4 ),
 ( 1.551583845779545699E-17, 0.0007657099931970551407, 0.001531419946797920239, 0.002296279302920158170, 0.003061450627205758099 ),
 .UNSPECIFIED. ) ;
#27286=CARTESIAN_POINT ( 'NONE',  ( -28.13707043255157103, -18.96624908365855688, -12.83104814250447134 ) ) ;
#27290=CARTESIAN_POINT ( 'NONE',  ( -20.20700224038492365, 8.199606986804329978, -28.44216453106539078 ) ) ;
#27295=CARTESIAN_POINT ( 'NONE',  ( -55.25719721206881729, 0.0006290797159235729736, 0.01115102788683339750 ) ) ;
#27301=CARTESIAN_POINT ( 'NONE',  ( -1.044556982611275053, -45.76404732357875815, 1.643392503293194862 ) ) ;
#27304=VERTEX_POINT ( 'NONE', #1842 ) ;
#27317=CARTESIAN_POINT ( 'NONE',  ( -4.162674018437125589, -31.44946543094270197, 37.46098494546626512 ) ) ;
#27321=CARTESIAN_POINT ( 'NONE',  ( -20.20612091757424267, 16.46550228026431384, 24.59769958242370436 ) ) ;
#27323=EDGE_LOOP ( 'NONE', ( #8398, #5918, #6222, #27862 ) ) ;
#27329=B_SPLINE_CURVE_WITH_KNOTS ( 'NONE', 3,
 ( #17193, #25981, #3821, #4377, #6271, #19213, #17613, #13151 ),
 .UNSPECIFIED., .F., .F.,
 ( 4, 2, 2, 4 ),
 ( 0.000000000000000000, 0.002761524886576655416, 0.005523049773153310832, 0.01104609954630660432 ),
 .UNSPECIFIED. ) ;
#27344=ORIENTED_EDGE ( 'NONE', *, *, #1689, .F. ) ;
#27352=CARTESIAN_POINT ( 'NONE',  ( -1.050229599974462413, -45.79907399707869331, -0.2556477501657915541 ) ) ;
#27354=FACE_OUTER_BOUND ( 'NONE', #10794, .T. ) ;
#27361=CARTESIAN_POINT ( 'NONE',  ( -1.045287976400386842, -28.14015102489780062, 36.12803364096639314 ) ) ;
#27362=B_SPLINE_CURVE_WITH_KNOTS ( 'NONE', 3,
 ( #16034, #9567, #9141, #24567, #5387, #20070, #6999, #15754 ),
 .UNSPECIFIED., .F., .F.,
 ( 4, 2, 2, 4 ),
 ( 0.000000000000000000, 0.002761524886576655416, 0.005523049773153310832, 0.01104609954630662166 ),
 .UNSPECIFIED. ) ;
#27363=CARTESIAN_POINT ( 'NONE',  ( -28.41354790283022069, -8.345538364876929904, 21.64275480268756269 ) ) ;
#27371=CARTESIAN_POINT ( 'NONE',  ( -7.078251931573400491, -26.33626633876254886, -44.92740138729156030 ) ) ;
#27380=CARTESIAN_POINT ( 'NONE',  ( -20.24419206586952313, -27.76448493191437095, 10.37009329716794248 ) ) ;
#27383=CARTESIAN_POINT ( 'NONE',  ( -20.57838717382308147, 29.92853265176831812, 1.611677988432465014 ) ) ;
#27391=FACE_OUTER_BOUND ( 'NONE', #16629, .T. ) ;
#27393=CARTESIAN_POINT ( 'NONE',  ( -1.045287976400362417, 25.66401692420069125, 37.92705037016716574 ) ) ;
#27394=ORIENTED_EDGE ( 'NONE', *, *, #18156, .T. ) ;
#27405=CARTESIAN_POINT ( 'NONE',  ( -55.24300891470648622, -0.006048736206180239418, 0.007734635432132643158 ) ) ;
#27410=B_SPLINE_CURVE_WITH_KNOTS ( 'NONE', 3,
 ( #24321, #26885, #11350, #24181, #24619, #19842 ),
 .UNSPECIFIED., .F., .F.,
 ( 4, 2, 4 ),
 ( 5.135960789613967459E-18, 0.0004335151646191499485, 0.0008670303292382946928 ),
 .UNSPECIFIED. ) ;
#27413=ORIENTED_EDGE ( 'NONE', *, *, #11379, .T. ) ;
#27414=ORIENTED_EDGE ( 'NONE', *, *, #28360, .T. ) ;
#27415=CARTESIAN_POINT ( 'NONE',  ( -1.048172774974295285, -26.08722459372758706, 37.64158596421241043 ) ) ;
#27436=ORIENTED_EDGE ( 'NONE', *, *, #26987, .F. ) ;
#27444=CARTESIAN_POINT ( 'NONE',  ( -1.045287976400362417, -12.68782741917263657, 44.00138577190661948 ) ) ;
#27452=DIRECTION ( 'NONE',  ( 0.000000000000000000, 5.223019709707975211E-21, -1.000000000000000000 ) ) ;
#27453=CARTESIAN_POINT ( 'NONE',  ( -23.77929240705206482, -35.93174012244168836, 4.877832571065307654 ) ) ;
#27454=CARTESIAN_POINT ( 'NONE',  ( -8.786685647604885574, 6.096987947571466530E-17, -1.524246986892866633E-17 ) ) ;
#27455=DIRECTION ( 'NONE',  ( 0.000000000000000000, 5.223019709707975211E-21, -1.000000000000000000 ) ) ;
#27457=ORIENTED_EDGE ( 'NONE', *, *, #5328, .F. ) ;
#27461=VERTEX_POINT ( 'NONE', #18962 ) ;
#27470=CARTESIAN_POINT ( 'NONE',  ( -55.24271866751342941, 0.001425019990779439203, 0.009388511352200054269 ) ) ;
#27471=AXIS2_PLACEMENT_3D ( 'NONE', #22782, #874, #16131 ) ;
#27475=ORIENTED_EDGE ( 'NONE', *, *, #20880, .F. ) ;
#27486=EDGE_LOOP ( 'NONE', ( #27946, #6984, #3546, #3672 ) ) ;
#27488=EDGE_LOOP ( 'NONE', ( #1994, #7121, #19073, #11135 ) ) ;
#27489=CARTESIAN_POINT ( 'NONE',  ( -1.239374126674604337, -45.98822239537608425, -2.406737988130961181 ) ) ;
#27490=EDGE_CURVE ( 'NONE', #2493, #16646, #20708, .T. ) ;
#27491=CARTESIAN_POINT ( 'NONE',  ( -55.24271866751342941, 0.008433070970614317194, 0.004365563123939311327 ) ) ;
#27493=CARTESIAN_POINT ( 'NONE',  ( -1.046935749540006011, 12.93334586714240331, 43.93230528057167561 ) ) ;
#27494=LINE ( 'NONE', #13824, #2802 ) ;
#27498=CARTESIAN_POINT ( 'NONE',  ( -55.24390624410018802, -0.009209468562452135382, -0.004896917417131697002 ) ) ;
#27500=DIRECTION ( 'NONE',  ( 0.7637818620346800147, -0.1788995134688871336, -0.6201872550346648749 ) ) ;
#27511=VERTEX_POINT ( 'NONE', #10342 ) ;
#27512=CARTESIAN_POINT ( 'NONE',  ( -20.57838717382308147, -16.28767523336102130, 25.16001208503123365 ) ) ;
#27517=CARTESIAN_POINT ( 'NONE',  ( -20.21097721712958517, 17.13687106192379161, 24.14932359587270483 ) ) ;
#27519=CARTESIAN_POINT ( 'NONE',  ( -1.031422197589711987, 45.78027046666443312, -1.530725436377622151 ) ) ;
#27523=CIRCLE ( 'NONE', #27471, 53.53553390275978785 ) ;
#27524=CARTESIAN_POINT ( 'NONE',  ( -20.57838717382308147, 25.16001208503129760, 16.28767523336092893 ) ) ;
#27529=EDGE_CURVE ( 'NONE', #13048, #23610, #25031, .T. ) ;
#27531=CARTESIAN_POINT ( 'NONE',  ( -1.619063947482197729, -2.489035965909835557, 46.30105812165550816 ) ) ;
#27534=CARTESIAN_POINT ( 'NONE',  ( -9.156249394959713683, 48.78605533024740737, -24.29252099376508056 ) ) ;
#27543=DIRECTION ( 'NONE',  ( 0.7637818620346800147, -0.5345501402766247301, 0.3617919495470812152 ) ) ;
#27544=CARTESIAN_POINT ( 'NONE',  ( -1.239374126674604337, -42.99367564261267916, 16.50008610789344488 ) ) ;
#27549=CARTESIAN_POINT ( 'NONE',  ( -1.619063947482201282, 35.99532424477380488, -29.22875152547769062 ) ) ;
#27550=CARTESIAN_POINT ( 'NONE',  ( -1.046935749540007343, -12.93334586714209777, -43.93230528057176798 ) ) ;
#27552=EDGE_CURVE ( 'NONE', #18479, #3085, #26144, .T. ) ;
#27555=CARTESIAN_POINT ( 'NONE',  ( -1.050229599974477512, -27.12684363859229109, 36.90196321294325799 ) ) ;
#27564=CARTESIAN_POINT ( 'NONE',  ( -55.25719721206881729, -0.006045473558784178643, -0.009391134844729129294 ) ) ;
#27566=ORIENTED_EDGE ( 'NONE', *, *, #10241, .F. ) ;
#27571=ORIENTED_EDGE ( 'NONE', *, *, #947, .T. ) ;
#27573=ORIENTED_EDGE ( 'NONE', *, *, #20102, .T. ) ;
#27578=CARTESIAN_POINT ( 'NONE',  ( -25.21435515916043713, 23.92354251275973809, 25.00736669480994934 ) ) ;
#27585=CARTESIAN_POINT ( 'NONE',  ( -1.323830074806772172, 28.92190886481864709, -35.86387698262922186 ) ) ;
#27589=CARTESIAN_POINT ( 'NONE',  ( -23.77929240705205771, 6.464423883190382192, -35.68044874544699496 ) ) ;
#27594=CARTESIAN_POINT ( 'NONE',  ( -25.21435515916043002, 23.92354251275938992, -25.00736669481030106 ) ) ;
#27599=CARTESIAN_POINT ( 'NONE',  ( -55.24300891470648622, 0.005486913146696770563, 0.008142823778062024953 ) ) ;
#27602=CIRCLE ( 'NONE', #23030, 37.50000000000001421 ) ;
#27608=CARTESIAN_POINT ( 'NONE',  ( -1.583189561560253589, -46.33203782964459805, 2.490696082060356531 ) ) ;
#27623=B_SPLINE_CURVE_WITH_KNOTS ( 'NONE', 3,
 ( #5750, #18832, #25476, #16830, #1552, #9924, #5888 ),
 .UNSPECIFIED., .F., .F.,
 ( 4, 3, 4 ),
 ( 3.469446951953614189E-18, 0.009512539173626381045, 0.02506242213020843518 ),
 .UNSPECIFIED. ) ;
#27625=CARTESIAN_POINT ( 'NONE',  ( -20.57838717382308147, -10.78122205917020437, -27.96569011373082603 ) ) ;
#27635=CARTESIAN_POINT ( 'NONE',  ( -1.155031165708881646, -42.97366960678589720, 16.13806347973043387 ) ) ;
#27640=CARTESIAN_POINT ( 'NONE',  ( -8.259864102781671491, 52.60025989855203221, -6.590267880897108022 ) ) ;
#27646=CARTESIAN_POINT ( 'NONE',  ( -28.13707043255157103, -18.06394523322443035, 14.07296284901352479 ) ) ;
#27654=VERTEX_POINT ( 'NONE', #7148 ) ;
#27658=( BOUNDED_SURFACE ( )  B_SPLINE_SURFACE ( 3, 1, ( 
 ( #17502, #26290 ),
 ( #3990, #6587 ),
 ( #12761, #1819 ),
 ( #10618, #23877 ) ),
 .UNSPECIFIED., .F., .F., .F. ) 
 B_SPLINE_SURFACE_WITH_KNOTS ( ( 4, 4 ),
 ( 2, 2 ),
 ( 0.000000000000000000, 1.000000000000000000 ),
 ( 0.000000000000000000, 1.000000000000000000 ),
 .UNSPECIFIED. ) 
 GEOMETRIC_REPRESENTATION_ITEM ( )  RATIONAL_B_SPLINE_SURFACE ( (
 ( 1.000000000000000000, 1.000000000000000000),
 ( 0.9934239774497837239, 0.8357310067453919133),
 ( 0.9934239774497837239, 0.8357310067453919133),
 ( 1.000000000000000000, 1.000000000000000000) ) ) 
 REPRESENTATION_ITEM ( '' )  SURFACE ( )  );
#27663=CARTESIAN_POINT ( 'NONE',  ( -1.058473599757824735, 1.755404039370064950, 45.77379534793241334 ) ) ;
#27664=ORIENTED_EDGE ( 'NONE', *, *, #10806, .T. ) ;
#27682=EDGE_LOOP ( 'NONE', ( #3639, #7262, #8851, #26955 ) ) ;
#27689=VERTEX_POINT ( 'NONE', #13594 ) ;
#27690=EDGE_CURVE ( 'NONE', #20457, #7798, #22016, .T. ) ;
#27691=EDGE_CURVE ( 'NONE', #25194, #23301, #18226, .T. ) ;
#27699=CARTESIAN_POINT ( 'NONE',  ( -21.41430102051745266, -29.81033373822133470, -7.777552968935644628 ) ) ;
#27710=CARTESIAN_POINT ( 'NONE',  ( -25.21435515916043713, 6.169479169075932745, 34.05351380035326514 ) ) ;
#27717=AXIS2_PLACEMENT_3D ( 'NONE', #19009, #16856, #27790 ) ;
#27720=ORIENTED_EDGE ( 'NONE', *, *, #3330, .F. ) ;
#27729=ADVANCED_FACE ( 'NONE', ( #18195 ), #14868, .T. ) ;
#27733=CARTESIAN_POINT ( 'NONE',  ( -7.078251931573406708, 51.82710018979476985, -5.101176922830847893 ) ) ;
#27734=VECTOR ( 'NONE', #509, 999.9999999999998863 ) ;
#27736=CARTESIAN_POINT ( 'NONE',  ( -28.41354790283022069, 18.00456980371921034, 14.62505768302780851 ) ) ;
#27737=CARTESIAN_POINT ( 'NONE',  ( -25.21435515916025594, 1.749597353048488237E-16, -4.373993382621220594E-17 ) ) ;
#27743=CARTESIAN_POINT ( 'NONE',  ( -55.25719721206881729, -0.01041086141212241994, -0.004044147484874939351 ) ) ;
#27744=CARTESIAN_POINT ( 'NONE',  ( -20.20700224038492010, -0.9908225410480588913, -29.58392382092672435 ) ) ;
#27745=ORIENTED_EDGE ( 'NONE', *, *, #12823, .F. ) ;
#27746=ORIENTED_EDGE ( 'NONE', *, *, #21292, .T. ) ;
#27747=VERTEX_POINT ( 'NONE', #2809 ) ;
#27756=FACE_OUTER_BOUND ( 'NONE', #8260, .T. ) ;
#27764=CARTESIAN_POINT ( 'NONE',  ( -55.24728320129491266, 0.01402509393918179546, 0.003868537197316780987 ) ) ;
#27770=EDGE_CURVE ( 'NONE', #23613, #19718, #5195, .T. ) ;
#27774=ORIENTED_EDGE ( 'NONE', *, *, #20614, .F. ) ;
#27787=VERTEX_POINT ( 'NONE', #27549 ) ;
#27790=DIRECTION ( 'NONE',  ( 0.000000000000000000, 5.223019709707975211E-21, -1.000000000000000000 ) ) ;
#27803=ORIENTED_EDGE ( 'NONE', *, *, #3156, .T. ) ;
#27815=CARTESIAN_POINT ( 'NONE',  ( -1.155031165708874097, 45.85732438018715129, -2.068616213631106593 ) ) ;
#27824=CARTESIAN_POINT ( 'NONE',  ( -55.24390624410018802, -0.009209468562452135382, -0.004896917417131697002 ) ) ;
#27825=EDGE_CURVE ( 'NONE', #3085, #20088, #12731, .T. ) ;
#27831=VERTEX_POINT ( 'NONE', #24995 ) ;
#27832=( BOUNDED_SURFACE ( )  B_SPLINE_SURFACE ( 3, 1, ( 
 ( #23485, #12520 ),
 ( #8221, #4088 ),
 ( #2193, #17319 ),
 ( #19761, #26390 ) ),
 .UNSPECIFIED., .F., .F., .F. ) 
 B_SPLINE_SURFACE_WITH_KNOTS ( ( 4, 4 ),
 ( 2, 2 ),
 ( 0.000000000000000000, 1.000000000000000000 ),
 ( 0.000000000000000000, 1.000000000000000000 ),
 .UNSPECIFIED. ) 
 GEOMETRIC_REPRESENTATION_ITEM ( )  RATIONAL_B_SPLINE_SURFACE ( (
 ( 1.000000000000000000, 1.000000000000000000),
 ( 0.9593753223639863714, 0.9995975284513187731),
 ( 0.9593753223639863714, 0.9995975284513187731),
 ( 1.000000000000000000, 1.000000000000000000) ) ) 
 REPRESENTATION_ITEM ( '' )  SURFACE ( )  );
#27834=VERTEX_POINT ( 'NONE', #5250 ) ;
#27835=CARTESIAN_POINT ( 'NONE',  ( -28.13707043255157103, -18.96624908365836859, 12.83104814250474668 ) ) ;
#27839=CARTESIAN_POINT ( 'NONE',  ( -20.20700224038492721, 0.9908225410482660589, 29.58392382092671724 ) ) ;
#27844=CARTESIAN_POINT ( 'NONE',  ( -1.539760825549682188, -44.72358953107742252, -11.93465943778497262 ) ) ;
#27846=EDGE_CURVE ( 'NONE', #20232, #4864, #4519, .T. ) ;
#27853=CARTESIAN_POINT ( 'NONE',  ( -21.81686047589429833, -37.90526371014251339, 6.867757412721077870 ) ) ;
#27858=ORIENTED_EDGE ( 'NONE', *, *, #1361, .T. ) ;
#27862=ORIENTED_EDGE ( 'NONE', *, *, #21877, .F. ) ;
#27868=DIRECTION ( 'NONE',  ( 1.000000000000000000, -6.938893903907226837E-18, 1.734723475976806709E-18 ) ) ;
#27871=CARTESIAN_POINT ( 'NONE',  ( -9.156249394959713683, -38.89149400288378899, 38.17928057392034447 ) ) ;
#27878=CARTESIAN_POINT ( 'NONE',  ( -20.47566338032517663, -1.586617869344095322, -29.82700953060487592 ) ) ;
#27881=DIRECTION ( 'NONE',  ( 1.000000000000000000, -6.938893903907226837E-18, 1.734723475976806709E-18 ) ) ;
#27884=CARTESIAN_POINT ( 'NONE',  ( -4.162674018437145129, -47.46216648493545875, 11.82104147411610207 ) ) ;
#27886=CARTESIAN_POINT ( 'NONE',  ( -25.21435515916025594, 1.749597353048488237E-16, -4.373993382621220594E-17 ) ) ;
#27889=DIRECTION ( 'NONE',  ( -1.000000000000000000, 6.938893903907226837E-18, 5.541455922705464902E-20 ) ) ;
#27896=CARTESIAN_POINT ( 'NONE',  ( -9.156249394959706578, -38.89149400288433611, -38.17928057391977603 ) ) ;
#27904=B_SPLINE_CURVE_WITH_KNOTS ( 'NONE', 3,
 ( #20005, #19865, #22473, #24205, #6926, #2149, #17419, #26763 ),
 .UNSPECIFIED., .F., .F.,
 ( 4, 2, 2, 4 ),
 ( 2.194186273941487696E-16, 0.002761568181852869838, 0.005523136363705520233, 0.01104627272741081495 ),
 .UNSPECIFIED. ) ;
#27905=LINE ( 'NONE', #14804, #11650 ) ;
#27910=CARTESIAN_POINT ( 'NONE',  ( -8.786685647604890903, 38.68584556812300690, -37.00619870957947910 ) ) ;
#27912=CARTESIAN_POINT ( 'NONE',  ( -1.155031165708883423, 28.62780465193363355, 35.88345263711016031 ) ) ;
#27913=ORIENTED_EDGE ( 'NONE', *, *, #7800, .T. ) ;
#27914=ORIENTED_EDGE ( 'NONE', *, *, #7388, .T. ) ;
#27919=CARTESIAN_POINT ( 'NONE',  ( -28.13707043255157103, 21.52861750560939313, -7.802116958609079056 ) ) ;
#27923=CARTESIAN_POINT ( 'NONE',  ( -1.583189561560253589, -44.83405390829680215, -11.94859433442884189 ) ) ;
#27934=ORIENTED_EDGE ( 'NONE', *, *, #21518, .T. ) ;
#27937=CARTESIAN_POINT ( 'NONE',  ( -9.156249394959706578, -25.18996226954649131, -48.32878616081000445 ) ) ;
#27946=ORIENTED_EDGE ( 'NONE', *, *, #7300, .T. ) ;
#27951=CARTESIAN_POINT ( 'NONE',  ( -1.031422197589716205, 36.13727897780168519, 28.14735071801704436 ) ) ;
#27954=CARTESIAN_POINT ( 'NONE',  ( -20.47566262905010248, -10.72601569609877536, 27.87687924095557435 ) ) ;
#27956=FACE_OUTER_BOUND ( 'NONE', #23106, .T. ) ;
#27958=ORIENTED_EDGE ( 'NONE', *, *, #20876, .T. ) ;
#27962=CARTESIAN_POINT ( 'NONE',  ( -1.046936909428679119, 45.77873603877006303, -1.275306677858401905 ) ) ;
#27965=ORIENTED_EDGE ( 'NONE', *, *, #26528, .F. ) ;
#27967=B_SPLINE_CURVE_WITH_KNOTS ( 'NONE', 3,
 ( #10161, #1084, #25560, #18929, #1501, #25421 ),
 .UNSPECIFIED., .F., .F.,
 ( 4, 2, 4 ),
 ( 0.000000000000000000, 0.003570751334075638293, 0.007141502668151276587 ),
 .UNSPECIFIED. ) ;
#27976=EDGE_CURVE ( 'NONE', #2725, #23109, #392, .T. ) ;
#27985=( BOUNDED_SURFACE ( )  B_SPLINE_SURFACE ( 3, 1, ( 
 ( #1857, #27923 ),
 ( #16862, #8630 ),
 ( #25919, #19563 ),
 ( #10660, #6212 ) ),
 .UNSPECIFIED., .F., .F., .F. ) 
 B_SPLINE_SURFACE_WITH_KNOTS ( ( 4, 4 ),
 ( 2, 2 ),
 ( 0.000000000000000000, 1.000000000000000000 ),
 ( 0.000000000000000000, 1.000000000000000000 ),
 .UNSPECIFIED. ) 
 GEOMETRIC_REPRESENTATION_ITEM ( )  RATIONAL_B_SPLINE_SURFACE ( (
 ( 1.000000000000000000, 1.000000000000000000),
 ( 0.7789835883360576307, 0.9689951854195403280),
 ( 0.7789835883360576307, 0.9689951854195403280),
 ( 1.000000000000000000, 1.000000000000000000) ) ) 
 REPRESENTATION_ITEM ( '' )  SURFACE ( )  );
#27989=CARTESIAN_POINT ( 'NONE',  ( -1.046935749539997573, -25.87617179820943036, -37.78548154587986119 ) ) ;
#27993=ORIENTED_EDGE ( 'NONE', *, *, #10633, .T. ) ;
#27997=ORIENTED_EDGE ( 'NONE', *, *, #16647, .T. ) ;
#27999=CARTESIAN_POINT ( 'NONE',  ( -20.37983603106073005, 18.69865230096527142, -23.16947629293368038 ) ) ;
#28000=EDGE_CURVE ( 'NONE', #10778, #15181, #14108, .T. ) ;
#28003=CARTESIAN_POINT ( 'NONE',  ( -55.25719721206881729, 0.009391134844733637840, 0.006045473558784292267 ) ) ;
#28006=CARTESIAN_POINT ( 'NONE',  ( -55.24271866751342941, -0.004256484107795216812, 0.008488649505342837909 ) ) ;
#28011=B_SPLINE_CURVE_WITH_KNOTS ( 'NONE', 3,
 ( #10636, #28313, #2653, #3876, #22247, #23891, #21427, #1835, #19405, #11297, #21709, #28038, #6457 ),
 .UNSPECIFIED., .F., .F.,
 ( 4, 3, 3, 3, 4 ),
 ( 1.250926888277100303E-17, 0.0007657099931970619711, 0.001531419946797935418, 0.002296279302920161639, 0.003061450627205739884 ),
 .UNSPECIFIED. ) ;
#28017=ORIENTED_EDGE ( 'NONE', *, *, #21964, .F. ) ;
#28020=ORIENTED_EDGE ( 'NONE', *, *, #7419, .T. ) ;
#28021=CARTESIAN_POINT ( 'NONE',  ( -55.24271866751342941, -0.006757859501005985571, -0.006671293903669251422 ) ) ;
#28022=( BOUNDED_SURFACE ( )  B_SPLINE_SURFACE ( 3, 1, ( 
 ( #9616, #12066 ),
 ( #22881, #20841 ),
 ( #25038, #20970 ),
 ( #1125, #18378 ) ),
 .UNSPECIFIED., .F., .F., .F. ) 
 B_SPLINE_SURFACE_WITH_KNOTS ( ( 4, 4 ),
 ( 2, 2 ),
 ( 0.000000000000000000, 1.000000000000000000 ),
 ( 0.000000000000000000, 1.000000000000000000 ),
 .UNSPECIFIED. ) 
 GEOMETRIC_REPRESENTATION_ITEM ( )  RATIONAL_B_SPLINE_SURFACE ( (
 ( 1.000000000000000000, 1.000000000000000000),
 ( 0.9934239774497838349, 0.8357310067453913582),
 ( 0.9934239774497838349, 0.8357310067453913582),
 ( 1.000000000000000000, 1.000000000000000000) ) ) 
 REPRESENTATION_ITEM ( '' )  SURFACE ( )  );
#28032=EDGE_CURVE ( 'NONE', #27179, #12283, #2432, .T. ) ;
#28033=CARTESIAN_POINT ( 'NONE',  ( -1.259920593601977057, -35.85909937955943860, -28.82601305773640732 ) ) ;
#28035=B_SPLINE_CURVE_WITH_KNOTS ( 'NONE', 3,
 ( #4391, #6151, #23715, #15034, #2211, #4105, #12871, #6416, #4211, #17029 ),
 .UNSPECIFIED., .F., .F.,
 ( 4, 2, 2, 2, 4 ),
 ( 2.877728285596781101E-16, 0.0003346187017559061659, 0.0006692374035115240425, 0.001003856105267141811, 0.001338474807022759687 ),
 .UNSPECIFIED. ) ;
#28038=CARTESIAN_POINT ( 'NONE',  ( -1.046935749539997129, 36.28605774377803073, 27.93995161054655085 ) ) ;
#28043=CARTESIAN_POINT ( 'NONE',  ( -23.79248802219730052, 16.82188324679482605, -28.61009539422389381 ) ) ;
#28046=EDGE_CURVE ( 'NONE', #14332, #26638, #7835, .T. ) ;
#28053=CARTESIAN_POINT ( 'NONE',  ( -1.259972190295305827, -43.01178231151318698, 16.33417789844418522 ) ) ;
#28055=DIRECTION ( 'NONE',  ( -0.7637818620346800147, -0.6068965246771030886, 0.2198041754873903408 ) ) ;
#28058=DIRECTION ( 'NONE',  ( 1.000000000000000000, -6.938893903907226837E-18, 1.734723475976806709E-18 ) ) ;
#28062=DIRECTION ( 'NONE',  ( 1.000000000000000000, -6.938893903907226837E-18, 1.734723475976806709E-18 ) ) ;
#28067=CARTESIAN_POINT ( 'NONE',  ( -20.57838717382308147, -1.611677988432151709, 29.92853265176832878 ) ) ;
#28075=EDGE_CURVE ( 'NONE', #14894, #25403, #7984, .T. ) ;
#28076=CARTESIAN_POINT ( 'NONE',  ( -20.47566338032525124, 10.72601609985066062, 27.87687989047296711 ) ) ;
#28081=EDGE_CURVE ( 'NONE', #11834, #17615, #8316, .T. ) ;
#28090=CARTESIAN_POINT ( 'NONE',  ( -55.25719721206881729, -0.009391134844728631428, 0.006045473558784497832 ) ) ;
#28098=ORIENTED_EDGE ( 'NONE', *, *, #2602, .F. ) ;
#28107=CARTESIAN_POINT ( 'NONE',  ( -55.24198130335446422, 0.006617369590172447053, -0.006527480770973747085 ) ) ;
#28125=CARTESIAN_POINT ( 'NONE',  ( -1.049817751779873909, -36.75003908324312363, -27.33161971822185876 ) ) ;
#28141=CARTESIAN_POINT ( 'NONE',  ( -55.24300891470648622, -0.008142823778061756071, 0.005486913146696262289 ) ) ;
#28153=CARTESIAN_POINT ( 'NONE',  ( -1.619063947482201282, -44.80407745103776307, 11.94059994246206635 ) ) ;
#28158=ORIENTED_EDGE ( 'NONE', *, *, #14661, .T. ) ;
#28160=EDGE_CURVE ( 'NONE', #22027, #11495, #18179, .T. ) ;
#28162=CARTESIAN_POINT ( 'NONE',  ( -8.259864102781676820, 36.24929574824966494, 38.68084189741909995 ) ) ;
#28165=EDGE_CURVE ( 'NONE', #9286, #2734, #15788, .T. ) ;
#28169=ORIENTED_EDGE ( 'NONE', *, *, #21877, .T. ) ;
#28178=CARTESIAN_POINT ( 'NONE',  ( -12.82751273423883198, -35.32125660155422509, 33.78816682541326344 ) ) ;
#28179=CARTESIAN_POINT ( 'NONE',  ( -55.24271866751342941, 0.009369360294294836952, -0.001545935011626992572 ) ) ;
#28194=DIRECTION ( 'NONE',  ( 0.000000000000000000, 5.223019709707975211E-21, -1.000000000000000000 ) ) ;
#28199=CARTESIAN_POINT ( 'NONE',  ( -20.57838717382308147, -23.26537097894090778, 18.89542499756525729 ) ) ;
#28210=CARTESIAN_POINT ( 'NONE',  ( -7.711401346138398338, -10.36923727626085423, 51.42722225669433556 ) ) ;
#28213=ORIENTED_EDGE ( 'NONE', *, *, #6738, .F. ) ;
#28214=ORIENTED_EDGE ( 'NONE', *, *, #24916, .F. ) ;
#28215=DIRECTION ( 'NONE',  ( 0.000000000000000000, 5.223019709707975211E-21, -1.000000000000000000 ) ) ;
#28218=ORIENTED_EDGE ( 'NONE', *, *, #14754, .T. ) ;
#28219=B_SPLINE_CURVE_WITH_KNOTS ( 'NONE', 3,
 ( #23710, #3826, #18797, #23279, #5716, #7741, #14326, #8157 ),
 .UNSPECIFIED., .F., .F.,
 ( 4, 2, 2, 4 ),
 ( 0.000000000000000000, 0.002761524886576652380, 0.005523049773153304760, 0.01104609954630660952 ),
 .UNSPECIFIED. ) ;
#28226=CARTESIAN_POINT ( 'NONE',  ( -1.583189561560255143, 36.01941156322830295, 29.24830400313125267 ) ) ;
#28227=EDGE_CURVE ( 'NONE', #20045, #26004, #4112, .T. ) ;
#28228=CARTESIAN_POINT ( 'NONE',  ( -25.21435515916043713, -4.655591116594118617, 34.29329011225960500 ) ) ;
#28233=ORIENTED_EDGE ( 'NONE', *, *, #10002, .F. ) ;
#28234=CARTESIAN_POINT ( 'NONE',  ( -4.178947244162641184, -48.81675275154074001, 3.367451375481625320 ) ) ;
#28241=B_SPLINE_CURVE_WITH_KNOTS ( 'NONE', 3,
 ( #15368, #21867, #11065, #4021, #15224, #12935 ),
 .UNSPECIFIED., .F., .F.,
 ( 4, 2, 4 ),
 ( 4.982613841084487634E-18, 0.0004335151646191476174, 0.0008670303292382917654 ),
 .UNSPECIFIED. ) ;
#28242=CARTESIAN_POINT ( 'NONE',  ( -1.619063947482194177, 25.20140673341374438, -38.92136151114915066 ) ) ;
#28244=CARTESIAN_POINT ( 'NONE',  ( -25.21435515916043002, -4.655591116594591128, -34.29329011225954105 ) ) ;
#28247=CARTESIAN_POINT ( 'NONE',  ( -25.21435515916043002, 4.655591116594353984, -34.29329011225956947 ) ) ;
#28253=CARTESIAN_POINT ( 'NONE',  ( -55.24390624410018802, 0.001811362924362862900, -0.01027195578988028025 ) ) ;
#28256=LINE ( 'NONE', #15019, #21547 ) ;
#28258=CARTESIAN_POINT ( 'NONE',  ( -2.265401668238151256, -2.645701981445478079, 46.93990709177546705 ) ) ;
#28275=CARTESIAN_POINT ( 'NONE',  ( -21.41427618760458174, -11.22988868156165410, 28.68857606049978415 ) ) ;
#28277=CARTESIAN_POINT ( 'NONE',  ( -16.86833981943428640, -38.94907963570735632, -20.94590537750593739 ) ) ;
#28286=ORIENTED_EDGE ( 'NONE', *, *, #13025, .F. ) ;
#28294=ORIENTED_EDGE ( 'NONE', *, *, #20336, .F. ) ;
#28298=CARTESIAN_POINT ( 'NONE',  ( -24.53237795827023859, -33.71192251888856362, 3.868415699416008380 ) ) ;
#28309=VERTEX_POINT ( 'NONE', #7495 ) ;
#28313=CARTESIAN_POINT ( 'NONE',  ( -1.046936909428679785, 37.78538189376546086, 25.87632113675119427 ) ) ;
#28314=DIRECTION ( 'NONE',  ( 0.000000000000000000, 5.223019709707975211E-21, -1.000000000000000000 ) ) ;
#28324=ORIENTED_EDGE ( 'NONE', *, *, #7553, .F. ) ;
#28327=CARTESIAN_POINT ( 'NONE',  ( -25.21435515916043713, -15.02493970636168896, -31.17620025257581062 ) ) ;
#28345=CARTESIAN_POINT ( 'NONE',  ( -20.37983603106074426, -18.69865230096510444, 23.16947629293382960 ) ) ;
#28347=CARTESIAN_POINT ( 'NONE',  ( -55.24340739397742084, -0.009842732675351817742, 0.002421372372454084262 ) ) ;
#28348=( BOUNDED_SURFACE ( )  B_SPLINE_SURFACE ( 3, 1, ( 
 ( #7355, #3175 ),
 ( #18418, #27489 ),
 ( #13962, #583 ),
 ( #26912, #20296 ) ),
 .UNSPECIFIED., .F., .F., .F. ) 
 B_SPLINE_SURFACE_WITH_KNOTS ( ( 4, 4 ),
 ( 2, 2 ),
 ( 0.000000000000000000, 1.000000000000000000 ),
 ( 0.000000000000000000, 1.000000000000000000 ),
 .UNSPECIFIED. ) 
 GEOMETRIC_REPRESENTATION_ITEM ( )  RATIONAL_B_SPLINE_SURFACE ( (
 ( 1.000000000000000000, 1.000000000000000000),
 ( 0.9934239774497837239, 0.8357310067453919133),
 ( 0.9934239774497837239, 0.8357310067453919133),
 ( 1.000000000000000000, 1.000000000000000000) ) ) 
 REPRESENTATION_ITEM ( '' )  SURFACE ( )  );
#28356=CARTESIAN_POINT ( 'NONE',  ( -1.048172774974286403, -43.86067135048628529, -13.17853518375281041 ) ) ;
#28357=CARTESIAN_POINT ( 'NONE',  ( -55.24271866751342941, -0.004365563123939053720, 0.008433070970613821063 ) ) ;
#28360=EDGE_CURVE ( 'NONE', #23301, #15242, #27905, .T. ) ;
#28361=CARTESIAN_POINT ( 'NONE',  ( -55.24271866751342941, -0.009388511352197387999, -0.001425019990782294558 ) ) ;
#28362=CARTESIAN_POINT ( 'NONE',  ( -1.323439229708142983, -35.86372896917450959, 28.92147054731879408 ) ) ;
#28364=CARTESIAN_POINT ( 'NONE',  ( -20.24399999263415140, -10.36954246768226717, 27.76448601145551009 ) ) ;
#28376=EDGE_CURVE ( 'NONE', #8934, #26396, #13382, .T. ) ;
#28378=B_SPLINE_CURVE_WITH_KNOTS ( 'NONE', 3,
 ( #13276, #10855, #22061, #10717, #11133, #19617, #28247 ),
 .UNSPECIFIED., .F., .F.,
 ( 4, 3, 4 ),
 ( 2.299948302575412283E-16, 0.009512539173626367167, 0.02506242213020821313 ),
 .UNSPECIFIED. ) ;
#28393=CARTESIAN_POINT ( 'NONE',  ( -8.786685647604896232, 9.545808661481343549, 52.67761315067276229 ) ) ;
#28394=CARTESIAN_POINT ( 'NONE',  ( -1.463510566862828766, -43.13857742234517190, -16.57250862017402682 ) ) ;
#28397=CARTESIAN_POINT ( 'NONE',  ( -9.156249394959706578, 38.17928057391991103, -38.89149400288420111 ) ) ;
#28399=CARTESIAN_POINT ( 'NONE',  ( -20.57838717382308502, 23.26537097894105699, -18.89542499756508320 ) ) ;
#28402=CARTESIAN_POINT ( 'NONE',  ( -1.463510566862834761, -16.57250862017389892, 43.13857742234520032 ) ) ;
#28406=AXIS2_PLACEMENT_3D ( 'NONE', #18822, #3004, #3428 ) ;
#28425=B_SPLINE_CURVE_WITH_KNOTS ( 'NONE', 3,
 ( #27290, #10335, #16357, #23150, #20955, #19094 ),
 .UNSPECIFIED., .F., .F.,
 ( 4, 2, 4 ),
 ( 1.734723475976807094E-18, 0.0004335184443140231605, 0.0008670368886280445863 ),
 .UNSPECIFIED. ) ;
#28428=CARTESIAN_POINT ( 'NONE',  ( -1.048171036023499925, -43.86077206077059998, 13.17819047681649103 ) ) ;
#28433=CARTESIAN_POINT ( 'NONE',  ( -20.20700224038492721, -23.35150625415671755, -18.19058640100215385 ) ) ;
#28435=ORIENTED_EDGE ( 'NONE', *, *, #9034, .F. ) ;
#28436=CARTESIAN_POINT ( 'NONE',  ( -55.24728320129491266, -0.01362040845703012606, 0.005114031043466422087 ) ) ;
#28439=PRODUCT_DEFINITION ( 'UNKNOWN', '', #13478, #18602 ) ;
#28442=ORIENTED_EDGE ( 'NONE', *, *, #10878, .F. ) ;
#28443=CARTESIAN_POINT ( 'NONE',  ( -1.463510566862834983, -35.90603835816524025, -29.09194585123821497 ) ) ;
#28447=DIRECTION ( 'NONE',  ( 1.000000000000000000, -6.938893903907226837E-18, 1.734723475976806709E-18 ) ) ;
#28460=CARTESIAN_POINT ( 'NONE',  ( -20.20612091757422490, -28.48192249925583752, 8.058516044219494745 ) ) ;
#28465=EDGE_LOOP ( 'NONE', ( #1754, #19977, #13946, #15607 ) ) ;
#28469=CARTESIAN_POINT ( 'NONE',  ( -1.031422197589716205, -37.93675465142454328, 25.67058493451484225 ) ) ;
#28522=COLOUR_RGB('Off White',0.89,0.88,0.83);
#28523=FILL_AREA_STYLE_COLOUR('',#28522);
#28524=FILL_AREA_STYLE('',(#28523));
#28525=SURFACE_STYLE_FILL_AREA(#28524);
#28526=SURFACE_SIDE_STYLE('',(#28525));
#28527=SURFACE_STYLE_USAGE(.BOTH.,#28526);
#28528=PRESENTATION_STYLE_ASSIGNMENT((#28527));
ENDSEC;
END-ISO-10303-21;
